ISO-10303-21;
HEADER;
FILE_DESCRIPTION (('STEP AP203'),
    '1' );
FILE_NAME ('PruningShears-Part2_Predeterminado.step',
    '2026-10-08T11:28:20',
    ( '' ),
    ( '' ),
    'SwSTEP 2.0',
    'SolidWorks 2024',
    '' );
FILE_SCHEMA (( 'AUTOMOTIVE_DESIGN' ));
ENDSEC;

DATA;
#4=DIRECTION ( 'NONE',  ( -0.9961255586397056438, 0.000000000000000000, 0.08794243244722428632 ) ) ;
#5=CARTESIAN_POINT ( 'NONE',  ( -4.239466046644367658, 10.19338654090241114, -48.02051031032586081 ) ) ;
#8=DIRECTION ( 'NONE',  ( 0.003262051938530752433, 0.000000000000000000, 0.9999946794944213346 ) ) ;
#12=CARTESIAN_POINT ( 'NONE',  ( -25.82983890416511841, 9.999999999999998224, -142.4527639562402328 ) ) ;
#13=CARTESIAN_POINT ( 'NONE',  ( -65.21690963830255328, 14.66435712545321657, -194.0246706955119009 ) ) ;
#15=ORIENTED_EDGE ( 'NONE', *, *, #9512, .T. ) ;
#17=CARTESIAN_POINT ( 'NONE',  ( -6.279162092933343153, 2.500000000000000444, -108.6370948588273535 ) ) ;
#26=CIRCLE ( 'NONE', #8661, 3.250000000000003553 ) ;
#27=CARTESIAN_POINT ( 'NONE',  ( -46.17421409260412446, 15.00000000000000000, -147.1483150044805939 ) ) ;
#35=ORIENTED_EDGE ( 'NONE', *, *, #13499, .F. ) ;
#36=CARTESIAN_POINT ( 'NONE',  ( -8.661991262811106651, 15.00000000000000000, -130.6821289911104316 ) ) ;
#38=AXIS2_PLACEMENT_3D ( 'NONE', #940, #8979, #1799 ) ;
#44=ORIENTED_EDGE ( 'NONE', *, *, #4143, .F. ) ;
#53=CARTESIAN_POINT ( 'NONE',  ( -48.96897228669091362, 15.00000000000000178, -150.1829960677724500 ) ) ;
#56=EDGE_CURVE ( 'NONE', #9845, #1534, #14253, .T. ) ;
#57=DIRECTION ( 'NONE',  ( 0.08794243244723005948, 0.000000000000000000, 0.9961255586397049777 ) ) ;
#58=ADVANCED_FACE ( 'NONE', ( #12392 ), #3118, .T. ) ;
#61=CARTESIAN_POINT ( 'NONE',  ( -67.60837051205176351, 11.42435839016798838, -204.0214325388246266 ) ) ;
#62=CARTESIAN_POINT ( 'NONE',  ( 0.5457951471881908878, 3.606183382230925272, -138.3638248956704047 ) ) ;
#66=CARTESIAN_POINT ( 'NONE',  ( -29.69515346086419427, 5.000000000000000888, -156.7390981038714983 ) ) ;
#67=CARTESIAN_POINT ( 'NONE',  ( -17.09940774937029317, 0.4261086865563343262, -130.4730999849509203 ) ) ;
#72=CARTESIAN_POINT ( 'NONE',  ( -63.46632602869123474, 15.00000000000000000, -179.6775508400713477 ) ) ;
#74=ORIENTED_EDGE ( 'NONE', *, *, #3541, .T. ) ;
#75=CARTESIAN_POINT ( 'NONE',  ( -5.117107008692297399, 9.999999999999998224, -113.5915292474705893 ) ) ;
#76=EDGE_CURVE ( 'NONE', #2801, #15277, #3494, .T. ) ;
#86=CARTESIAN_POINT ( 'NONE',  ( 1.062740323768540662, 12.59030360039310636, 5.094619354848065385 ) ) ;
#89=LINE ( 'NONE', #4800, #3326 ) ;
#92=CARTESIAN_POINT ( 'NONE',  ( -63.21422130130005712, 10.26968228116884596, -203.6040552426024988 ) ) ;
#95=CARTESIAN_POINT ( 'NONE',  ( -4.723546506723169003, 4.336808689942017736E-16, -121.1708306026675501 ) ) ;
#104=CARTESIAN_POINT ( 'NONE',  ( -54.45540687895485377, 9.999999999999998224, -149.0501727870129685 ) ) ;
#112=CARTESIAN_POINT ( 'NONE',  ( -0.5447792503669787179, 14.99999999999999467, -117.0548960884185732 ) ) ;
#114=VERTEX_POINT ( 'NONE', #6524 ) ;
#119=VERTEX_POINT ( 'NONE', #1731 ) ;
#121=CIRCLE ( 'NONE', #7519, 4.999999999999995559 ) ;
#123=CARTESIAN_POINT ( 'NONE',  ( -7.332173456847238313, 0.07668794466513038921, -104.2603615701598869 ) ) ;
#124=CARTESIAN_POINT ( 'NONE',  ( -62.71861979978048396, 10.00000000000000000, -198.6004802465432135 ) ) ;
#125=AXIS2_PLACEMENT_3D ( 'NONE', #9268, #6866, #11579 ) ;
#127=CARTESIAN_POINT ( 'NONE',  ( -52.99646050385619844, 15.00000000000000000, -155.6021463114098253 ) ) ;
#134=CARTESIAN_POINT ( 'NONE',  ( -63.23239576043733479, 10.46432717375524213, -203.5646039687676705 ) ) ;
#135=CARTESIAN_POINT ( 'NONE',  ( 0.5065669489467078401, 5.000000000003537615, 5.737893198614711032 ) ) ;
#141=CARTESIAN_POINT ( 'NONE',  ( 1.855481649321436777, 15.00000000000000000, -35.83830032691820122 ) ) ;
#146=CARTESIAN_POINT ( 'NONE',  ( -9.240119717473294969, 2.324218168632100845, -104.6630069163585972 ) ) ;
#149=ORIENTED_EDGE ( 'NONE', *, *, #4890, .T. ) ;
#150=CARTESIAN_POINT ( 'NONE',  ( -5.893421222731322295, 9.999999999999998224, -117.5694263798337005 ) ) ;
#152=CARTESIAN_POINT ( 'NONE',  ( 1.818681402055029483, 15.00000000000000000, -137.3269588978979243 ) ) ;
#159=CARTESIAN_POINT ( 'NONE',  ( 0.9143209798285035772, 12.53633980243307100, 2.514521240264253166 ) ) ;
#168=CARTESIAN_POINT ( 'NONE',  ( -64.38825976928389139, 13.56900998018364213, -200.2675612624753398 ) ) ;
#171=EDGE_LOOP ( 'NONE', ( #12222, #10076, #8001, #12391 ) ) ;
#172=CARTESIAN_POINT ( 'NONE',  ( -6.790118584858316986, 2.500000000000000444, -107.8021323224912464 ) ) ;
#177=ORIENTED_EDGE ( 'NONE', *, *, #10342, .F. ) ;
#179=CARTESIAN_POINT ( 'NONE',  ( -69.61556017177876754, 9.999999999999998224, -198.3353672694111083 ) ) ;
#188=CARTESIAN_POINT ( 'NONE',  ( -1.260792021077014269, 15.00000000000000178, -107.5178971017766258 ) ) ;
#195=ORIENTED_EDGE ( 'NONE', *, *, #5701, .F. ) ;
#198=CARTESIAN_POINT ( 'NONE',  ( -9.222297982611349809, 2.161611222164042001, -104.6591137165734864 ) ) ;
#199=CARTESIAN_POINT ( 'NONE',  ( -33.91109452337774854, 10.00000000000000178, -156.1716796081737471 ) ) ;
#200=CARTESIAN_POINT ( 'NONE',  ( -45.43402158771803556, 15.00000000000000355, -154.4665057826428267 ) ) ;
#202=CARTESIAN_POINT ( 'NONE',  ( -62.77354874813351415, 14.99999999999999822, -176.9788886477732035 ) ) ;
#207=CARTESIAN_POINT ( 'NONE',  ( -67.63619164393119831, 12.59430211938552802, -202.7040278164101323 ) ) ;
#214=ORIENTED_EDGE ( 'NONE', *, *, #4803, .T. ) ;
#217=CARTESIAN_POINT ( 'NONE',  ( -63.86794096056340209, 10.00000000000000000, -165.1728739221729825 ) ) ;
#221=CARTESIAN_POINT ( 'NONE',  ( -0.5758322980023804494, 15.00000000000000000, -117.2003571699043221 ) ) ;
#223=CARTESIAN_POINT ( 'NONE',  ( 6.020998550613693823, 15.00000000000000000, -132.6181299100952629 ) ) ;
#224=EDGE_CURVE ( 'NONE', #10778, #11957, #683, .T. ) ;
#228=CARTESIAN_POINT ( 'NONE',  ( -4.160651409637847742, 10.31235003438523989, -46.92824181062579214 ) ) ;
#230=CARTESIAN_POINT ( 'NONE',  ( 1.674841001514616012, 13.54983687837186146, 4.356007712918980701 ) ) ;
#231=CARTESIAN_POINT ( 'NONE',  ( -3.806000526524415672, 10.67725751578602633, -43.60682525637299989 ) ) ;
#233=FACE_OUTER_BOUND ( 'NONE', #599, .T. ) ;
#238=CARTESIAN_POINT ( 'NONE',  ( 9.939878312292623974, 5.000000000000000888, -115.2320631035898373 ) ) ;
#240=ORIENTED_EDGE ( 'NONE', *, *, #10815, .T. ) ;
#244=CARTESIAN_POINT ( 'NONE',  ( -4.448900195745486563, 0.000000000000000000, -120.6207097488509703 ) ) ;
#248=CIRCLE ( 'NONE', #2460, 11.99999999999995559 ) ;
#249=CARTESIAN_POINT ( 'NONE',  ( -17.72297831578844196, 1.105884851291182525, -129.7878113374480904 ) ) ;
#252=ADVANCED_FACE ( 'NONE', ( #14573 ), #14420, .T. ) ;
#254=CARTESIAN_POINT ( 'NONE',  ( -69.46795959494568251, 14.99999999999999645, -199.1268727653549320 ) ) ;
#266=DIRECTION ( 'NONE',  ( -0.08794243244722425856, -0.000000000000000000, -0.9961255586397054218 ) ) ;
#280=CARTESIAN_POINT ( 'NONE',  ( -8.229629558439073733, 0.4823876599422149414, -104.4461881430476069 ) ) ;
#289=LINE ( 'NONE', #1755, #10684 ) ;
#290=AXIS2_PLACEMENT_3D ( 'NONE', #10491, #9174, #1135 ) ;
#292=CARTESIAN_POINT ( 'NONE',  ( -65.37429515991448170, 15.36281861597759502, -204.5121470880695256 ) ) ;
#293=DIRECTION ( 'NONE',  ( 0.000000000000000000, 0.000000000000000000, -1.000000000000000000 ) ) ;
#301=ORIENTED_EDGE ( 'NONE', *, *, #10792, .F. ) ;
#304=CARTESIAN_POINT ( 'NONE',  ( -8.846059151020902789, 1.095509632927770260, -104.9965497395157854 ) ) ;
#307=CARTESIAN_POINT ( 'NONE',  ( -5.187227155190234029, 9.999999999999998224, -114.5705604395994044 ) ) ;
#308=CARTESIAN_POINT ( 'NONE',  ( 1.126705156255721763, 12.88850925732717556, 2.355817795760899447 ) ) ;
#313=CARTESIAN_POINT ( 'NONE',  ( -3.686354355357802426, 9.944922017739179054, -47.56185035043098708 ) ) ;
#315=CARTESIAN_POINT ( 'NONE',  ( 3.580916657172306117, 14.85449318919366846, 1.548757939767684721 ) ) ;
#319=CARTESIAN_POINT ( 'NONE',  ( -8.886921396801785278, 2.331427915607008572, -105.5168766094550534 ) ) ;
#320=EDGE_CURVE ( 'NONE', #2721, #6383, #11005, .T. ) ;
#324=CARTESIAN_POINT ( 'NONE',  ( 4.047901358979359543, 5.000000000000000888, -106.4041221358673113 ) ) ;
#328=CARTESIAN_POINT ( 'NONE',  ( -2.880881586774806546, 8.673617379884035472E-16, -116.0176383781107461 ) ) ;
#333=VERTEX_POINT ( 'NONE', #2504 ) ;
#337=CARTESIAN_POINT ( 'NONE',  ( -64.88161843510579274, 15.00000000000000000, -196.1685357079028620 ) ) ;
#341=DIRECTION ( 'NONE',  ( 0.000000000000000000, 0.000000000000000000, 1.000000000000000000 ) ) ;
#346=AXIS2_PLACEMENT_3D ( 'NONE', #9220, #2189, #4657 ) ;
#350=EDGE_LOOP ( 'NONE', ( #5092, #7181, #10098, #3066 ) ) ;
#359=VECTOR ( 'NONE', #9016, 1000.000000000000227 ) ;
#363=CARTESIAN_POINT ( 'NONE',  ( -63.60348060676458459, 15.00000000000000000, -180.2685449772604045 ) ) ;
#368=EDGE_CURVE ( 'NONE', #9693, #10703, #2656, .T. ) ;
#374=B_SPLINE_CURVE_WITH_KNOTS ( 'NONE', 3,
 ( #12760, #7878, #3398, #5716 ),
 .UNSPECIFIED., .F., .F.,
 ( 4, 4 ),
 ( 0.000000000000000000, 0.01415222705959193195 ),
 .UNSPECIFIED. ) ;
#377=CARTESIAN_POINT ( 'NONE',  ( -67.63566299370725687, 12.50589072862690898, -202.8433208949320488 ) ) ;
#381=CARTESIAN_POINT ( 'NONE',  ( -66.58084616437841419, 14.78522502373413694, -192.0328052694261487 ) ) ;
#386=CARTESIAN_POINT ( 'NONE',  ( -8.867224457307584018, 1.189964233207651878, -104.5821247736135717 ) ) ;
#389=CARTESIAN_POINT ( 'NONE',  ( -47.48189921986827500, 5.000000000000000000, -141.5723758807981483 ) ) ;
#395=CARTESIAN_POINT ( 'NONE',  ( -3.954519906357485404, 10.53291419278240149, -44.70356096009636104 ) ) ;
#397=CARTESIAN_POINT ( 'NONE',  ( 2.135536195681809968, 14.03964673803787377, 3.771597406321472334 ) ) ;
#403=ORIENTED_EDGE ( 'NONE', *, *, #14661, .F. ) ;
#410=CARTESIAN_POINT ( 'NONE',  ( -17.53857915289978209, 0.8419440609433440637, -129.9988674391065047 ) ) ;
#411=VERTEX_POINT ( 'NONE', #1650 ) ;
#415=CARTESIAN_POINT ( 'NONE',  ( -69.57949925788119572, 9.999999999999998224, -184.9351518006301660 ) ) ;
#423=ORIENTED_EDGE ( 'NONE', *, *, #468, .F. ) ;
#424=CARTESIAN_POINT ( 'NONE',  ( -29.69515346086420138, 15.00000000000000000, -156.7390981038714983 ) ) ;
#429=DIRECTION ( 'NONE',  ( -0.000000000000000000, 1.000000000000000000, -0.000000000000000000 ) ) ;
#435=LINE ( 'NONE', #7296, #14161 ) ;
#440=CARTESIAN_POINT ( 'NONE',  ( -36.44277747304521853, 10.00000000000000355, -156.3629325348109376 ) ) ;
#441=FACE_OUTER_BOUND ( 'NONE', #3722, .T. ) ;
#444=ORIENTED_EDGE ( 'NONE', *, *, #15170, .F. ) ;
#447=VERTEX_POINT ( 'NONE', #7825 ) ;
#449=ADVANCED_FACE ( 'NONE', ( #4058 ), #14960, .T. ) ;
#456=CARTESIAN_POINT ( 'NONE',  ( -67.58382170693633384, 10.13932288468602039, -204.5178482451962338 ) ) ;
#460=CARTESIAN_POINT ( 'NONE',  ( -8.133653642740192424, 0.3980376946237794700, -104.7021510399676174 ) ) ;
#463=CARTESIAN_POINT ( 'NONE',  ( -8.605705957304479625, 14.99999999998180122, -105.7466801460949171 ) ) ;
#464=CARTESIAN_POINT ( 'NONE',  ( 7.432103217121470706, 5.104710470816895551, -26.33708262891812879 ) ) ;
#468=EDGE_CURVE ( 'NONE', #1674, #6553, #14959, .T. ) ;
#470=CARTESIAN_POINT ( 'NONE',  ( 0.1113706952913113279, 2.624400893789762268, 1.261497925137973652 ) ) ;
#485=CARTESIAN_POINT ( 'NONE',  ( -3.625354560620934752, 10.18683717591091842, -47.21077240160808230 ) ) ;
#486=ORIENTED_EDGE ( 'NONE', *, *, #6759, .F. ) ;
#489=CARTESIAN_POINT ( 'NONE',  ( -65.08324626441498140, 15.00000000000000000, -193.5244750848175386 ) ) ;
#499=ORIENTED_EDGE ( 'NONE', *, *, #8183, .T. ) ;
#508=CARTESIAN_POINT ( 'NONE',  ( -47.48189921986828210, 15.00000000000000000, -141.5723758807981483 ) ) ;
#514=DIRECTION ( 'NONE',  ( 0.000000000000000000, 0.000000000000000000, -1.000000000000000000 ) ) ;
#515=CIRCLE ( 'NONE', #2242, 5.000000000000002665 ) ;
#516=ORIENTED_EDGE ( 'NONE', *, *, #2307, .T. ) ;
#525=CARTESIAN_POINT ( 'NONE',  ( 3.211135607724114660, 3.697509922049161180, 5.038955779812875235 ) ) ;
#527=CIRCLE ( 'NONE', #15081, 2.000000000000016431 ) ;
#532=EDGE_CURVE ( 'NONE', #7071, #4481, #12762, .T. ) ;
#535=DIRECTION ( 'NONE',  ( 0.6182966555592912528, 0.000000000000000000, 0.7859448108640934016 ) ) ;
#539=CARTESIAN_POINT ( 'NONE',  ( -8.605705957300969544, 9.999999999999998224, -105.7466801460984840 ) ) ;
#540=CARTESIAN_POINT ( 'NONE',  ( -11.47368464600194571, 2.500000000000000444, -126.3895689751090856 ) ) ;
#545=CARTESIAN_POINT ( 'NONE',  ( -3.625372539825013618, 10.18678395325208719, -47.21086670346684855 ) ) ;
#547=CARTESIAN_POINT ( 'NONE',  ( 4.900580087367143456, 14.89515687054757365, -1.231267350884497125 ) ) ;
#554=CARTESIAN_POINT ( 'NONE',  ( 3.235167919141237913, 8.673617379884037444E-16, -114.6791120453068942 ) ) ;
#556=CARTESIAN_POINT ( 'NONE',  ( -39.01706460773457508, 9.999999999999998224, -156.9624841732276650 ) ) ;
#557=EDGE_CURVE ( 'NONE', #4897, #14271, #1403, .T. ) ;
#564=CARTESIAN_POINT ( 'NONE',  ( -3.315923205871632362, 9.650666666666662508, -43.24506100211545601 ) ) ;
#569=AXIS2_PLACEMENT_3D ( 'NONE', #10282, #10214, #3101 ) ;
#570=DIRECTION ( 'NONE',  ( -0.000000000000000000, -1.000000000000000000, -0.000000000000000000 ) ) ;
#574=CARTESIAN_POINT ( 'NONE',  ( -5.899062623765880531, 10.00000000000000178, -109.4162288830486887 ) ) ;
#590=APPLICATION_CONTEXT ( 'configuration controlled 3d designs of mechanical parts and assemblies' ) ;
#591=CARTESIAN_POINT ( 'NONE',  ( -7.079750767422662960, 14.09909992734707807, -104.2797251405894912 ) ) ;
#594=CIRCLE ( 'NONE', #14916, 5.000000000000001776 ) ;
#596=CIRCLE ( 'NONE', #7496, 3.000000000000002665 ) ;
#597=B_SPLINE_CURVE_WITH_KNOTS ( 'NONE', 3,
 ( #4870, #5, #5800, #3637, #10670, #8499, #9511, #10745, #13150, #1321, #14236, #8339, #14163, #11896, #231, #13064, #10520, #15255 ),
 .UNSPECIFIED., .F., .F.,
 ( 4, 2, 2, 2, 2, 2, 2, 2, 4 ),
 ( 7.806255641895631925E-18, 0.0007604115106050202957, 0.001520823021210032785, 0.002281234531815045166, 0.003041646042420057764, 0.003802057553025070362, 0.004562469063630082526, 0.005322880574235095558, 0.006083292084840107722 ),
 .UNSPECIFIED. ) ;
#598=DIRECTION ( 'NONE',  ( -0.9961255586397056438, 0.000000000000000000, 0.08794243244722428632 ) ) ;
#599=EDGE_LOOP ( 'NONE', ( #3826, #9848, #1789, #6970, #3305, #177 ) ) ;
#602=VERTEX_POINT ( 'NONE', #2107 ) ;
#608=CARTESIAN_POINT ( 'NONE',  ( 7.251665800977816545, 3.308594936348907112, -24.41847810565704080 ) ) ;
#609=CARTESIAN_POINT ( 'NONE',  ( 0.4577222846077236285, 2.652767234986340927, 5.184628782367975752 ) ) ;
#613=CIRCLE ( 'NONE', #14450, 7.000000000000016875 ) ;
#620=LINE ( 'NONE', #2862, #3306 ) ;
#625=EDGE_CURVE ( 'NONE', #10703, #14402, #14164, .T. ) ;
#629=CARTESIAN_POINT ( 'NONE',  ( 4.394544305604815015, 15.00077533664657636, -1.522866948741665727 ) ) ;
#635=CARTESIAN_POINT ( 'NONE',  ( -39.10933222484039362, 15.00000000000000000, -151.7704989434176923 ) ) ;
#655=FACE_OUTER_BOUND ( 'NONE', #9245, .T. ) ;
#662=ORIENTED_EDGE ( 'NONE', *, *, #10644, .T. ) ;
#666=CARTESIAN_POINT ( 'NONE',  ( -6.438219714322270804, 14.38465807372143956, -104.2571274176714553 ) ) ;
#678=ORIENTED_EDGE ( 'NONE', *, *, #14167, .T. ) ;
#681=CARTESIAN_POINT ( 'NONE',  ( 7.773533131393477902, 4.718920071733073485, -20.62283890789821683 ) ) ;
#682=CARTESIAN_POINT ( 'NONE',  ( 3.230086961373112242, 5.000000000003343992, 5.208283729180106292 ) ) ;
#683=CIRCLE ( 'NONE', #6090, 1.000000000000000888 ) ;
#692=CARTESIAN_POINT ( 'NONE',  ( -17.32624372123753886, 2.500000000000000444, -131.8796757791585037 ) ) ;
#699=CARTESIAN_POINT ( 'NONE',  ( -3.805953545085057677, 10.68988111647421846, -43.62564591857165652 ) ) ;
#703=DIRECTION ( 'NONE',  ( -0.9961255586397056438, 0.000000000000000000, 0.08794243244722428632 ) ) ;
#707=CARTESIAN_POINT ( 'NONE',  ( -52.06782037834351939, 15.00000000000000000, -159.8510668928024359 ) ) ;
#711=CARTESIAN_POINT ( 'NONE',  ( -14.68073284315481253, 7.499999999999991118, -92.37694453701993780 ) ) ;
#712=CARTESIAN_POINT ( 'NONE',  ( -25.68053481550299111, -5.000000000000000888, -142.4798935003980773 ) ) ;
#713=DIRECTION ( 'NONE',  ( -1.861571024194515387E-16, -1.000000000000000000, -2.108604941688510506E-15 ) ) ;
#718=CARTESIAN_POINT ( 'NONE',  ( -14.68073284315481253, 7.499999999999991118, -92.37694453701993780 ) ) ;
#735=ORIENTED_EDGE ( 'NONE', *, *, #14546, .F. ) ;
#738=CARTESIAN_POINT ( 'NONE',  ( -6.293558381461702211, 14.52912145056953719, -103.7844163225382772 ) ) ;
#743=FACE_OUTER_BOUND ( 'NONE', #171, .T. ) ;
#745=VERTEX_POINT ( 'NONE', #1553 ) ;
#757=CARTESIAN_POINT ( 'NONE',  ( 0.03998412334521193878, 2.500000000000000888, 0.4529009045602684913 ) ) ;
#762=DIRECTION ( 'NONE',  ( 0.000000000000000000, 0.000000000000000000, -1.000000000000000000 ) ) ;
#763=TOROIDAL_SURFACE ( 'NONE', #9394, 8.000000000000000000, 5.000000000000000000 ) ;
#766=CARTESIAN_POINT ( 'NONE',  ( -68.96619529829705186, 10.00000000000000000, -201.1288088042396112 ) ) ;
#770=CARTESIAN_POINT ( 'NONE',  ( -9.302736714298539766, 4.336808689942017736E-16, -123.7731201990410597 ) ) ;
#776=CARTESIAN_POINT ( 'NONE',  ( 3.890350893699055401, 0.000000000000000000, -1.782295516753907849 ) ) ;
#785=DIRECTION ( 'NONE',  ( 0.08794243244722392550, 0.000000000000000000, 0.9961255586397055328 ) ) ;
#786=CARTESIAN_POINT ( 'NONE',  ( -50.98844033420547106, 15.00000000000000000, -158.7499874894748757 ) ) ;
#791=CYLINDRICAL_SURFACE ( 'NONE', #2074, 2.326940983401415419 ) ;
#792=CARTESIAN_POINT ( 'NONE',  ( -49.26721305452312549, 5.000000000000000000, -156.1716796081737186 ) ) ;
#795=AXIS2_PLACEMENT_3D ( 'NONE', #13365, #1374, #6076 ) ;
#799=CARTESIAN_POINT ( 'NONE',  ( -67.56077635250289859, 9.999999999999998224, -204.5805788406221097 ) ) ;
#800=CARTESIAN_POINT ( 'NONE',  ( -8.141169791565570080, 12.70346812208739529, -105.1150889670498287 ) ) ;
#804=CARTESIAN_POINT ( 'NONE',  ( -25.97807323962435078, -0.3396484172265533674, -142.5647913107548277 ) ) ;
#806=CARTESIAN_POINT ( 'NONE',  ( 2.655454743645370375, 0.03267829224664529214, 0.8826354733248792384 ) ) ;
#807=DIRECTION ( 'NONE',  ( 0.000000000000000000, -1.000000000000000000, 0.000000000000000000 ) ) ;
#809=ORIENTED_EDGE ( 'NONE', *, *, #4890, .F. ) ;
#817=DIRECTION ( 'NONE',  ( 0.000000000000000000, -1.000000000000000000, 0.000000000000000000 ) ) ;
#818=ADVANCED_FACE ( 'NONE', ( #233 ), #2402, .T. ) ;
#834=EDGE_CURVE ( 'NONE', #5223, #6652, #7605, .T. ) ;
#835=CARTESIAN_POINT ( 'NONE',  ( 0.2399920231728725206, 3.887405386441892485, 2.718394084632874463 ) ) ;
#840=DIRECTION ( 'NONE',  ( 0.7575874476598363216, 0.000000000000000000, 0.6527336816407245390 ) ) ;
#854=DIRECTION ( 'NONE',  ( 0.000000000000000000, -0.000000000000000000, -1.000000000000000000 ) ) ;
#858=ORIENTED_EDGE ( 'NONE', *, *, #6268, .T. ) ;
#861=CARTESIAN_POINT ( 'NONE',  ( -37.87309319206281089, 15.00000000000000000, -156.6288150090828424 ) ) ;
#864=CARTESIAN_POINT ( 'NONE',  ( -8.661991262811081782, 15.00000000000000000, -130.6821289911104600 ) ) ;
#875=CARTESIAN_POINT ( 'NONE',  ( -3.520407287333057855, 7.379999999999995453, -45.56125597433126018 ) ) ;
#878=CARTESIAN_POINT ( 'NONE',  ( 3.031377627837373634, 1.223715101037531339, 3.507052158993249069 ) ) ;
#882=VERTEX_POINT ( 'NONE', #6343 ) ;
#891=CARTESIAN_POINT ( 'NONE',  ( -8.398494254132010894, 12.74145370061613036, -104.4010416228292399 ) ) ;
#906=EDGE_CURVE ( 'NONE', #10778, #119, #6635, .T. ) ;
#916=EDGE_CURVE ( 'NONE', #9927, #7124, #9915, .T. ) ;
#921=CARTESIAN_POINT ( 'NONE',  ( -66.05397366910187884, 15.01442789161885472, -199.5963413483335955 ) ) ;
#927=CARTESIAN_POINT ( 'NONE',  ( -29.69515346086422980, 5.000000000000000000, -156.7390981038715836 ) ) ;
#931=CARTESIAN_POINT ( 'NONE',  ( -7.237223302401282865, 0.05734158322681513070, -104.4616748367153320 ) ) ;
#935=EDGE_CURVE ( 'NONE', #7022, #7777, #15292, .T. ) ;
#936=CARTESIAN_POINT ( 'NONE',  ( -3.942526376314868131, 15.00000000000000178, -136.1336533158788029 ) ) ;
#940=CARTESIAN_POINT ( 'NONE',  ( -25.82983890416511841, 9.999999999999998224, -142.4527639562402328 ) ) ;
#942=CARTESIAN_POINT ( 'NONE',  ( 0.5065669489466559927, 9.999999999999998224, 5.737893198614714585 ) ) ;
#947=CARTESIAN_POINT ( 'NONE',  ( -1.437999228988334544, 5.000000000000000888, -140.6782968106692522 ) ) ;
#973=VERTEX_POINT ( 'NONE', #13693 ) ;
#974=CARTESIAN_POINT ( 'NONE',  ( 1.893911505664648054, 5.000000000000000888, -1.663006917529762152 ) ) ;
#979=EDGE_CURVE ( 'NONE', #2743, #333, #11479, .T. ) ;
#984=ORIENTED_EDGE ( 'NONE', *, *, #4488, .T. ) ;
#991=CARTESIAN_POINT ( 'NONE',  ( -14.85661770804926007, 7.499999999999991118, -94.36919565429934664 ) ) ;
#994=CARTESIAN_POINT ( 'NONE',  ( -2.958380929922356906, 4.336808689942018722E-16, -110.3652039456601983 ) ) ;
#997=EDGE_CURVE ( 'NONE', #7124, #9927, #12825, .T. ) ;
#999=ORIENTED_EDGE ( 'NONE', *, *, #11506, .T. ) ;
#1000=DIRECTION ( 'NONE',  ( 0.7575874476598360996, -0.000000000000000000, 0.6527336816407247611 ) ) ;
#1002=CARTESIAN_POINT ( 'NONE',  ( -56.34877470247857900, 15.00000000000000000, -165.2605511895863799 ) ) ;
#1005=ORIENTED_EDGE ( 'NONE', *, *, #13682, .T. ) ;
#1009=AXIS2_PLACEMENT_3D ( 'NONE', #1918, #12811, #762 ) ;
#1016=FACE_OUTER_BOUND ( 'NONE', #12058, .T. ) ;
#1017=AXIS2_PLACEMENT_3D ( 'NONE', #10308, #11372, #6808 ) ;
#1020=EDGE_CURVE ( 'NONE', #2289, #4876, #7951, .T. ) ;
#1021=CARTESIAN_POINT ( 'NONE',  ( -7.773700879994175139, 9.999999999999998224, -121.5245725921722908 ) ) ;
#1022=EDGE_CURVE ( 'NONE', #9480, #7043, #3333, .T. ) ;
#1032=FACE_OUTER_BOUND ( 'NONE', #11557, .T. ) ;
#1037=DIRECTION ( 'NONE',  ( 0.9982196940171963462, 0.000000000000000000, -0.05964429961207440289 ) ) ;
#1043=VERTEX_POINT ( 'NONE', #927 ) ;
#1044=CARTESIAN_POINT ( 'NONE',  ( -3.231884997086563516, 15.00000000000000178, -104.1825805049879108 ) ) ;
#1059=DIRECTION ( 'NONE',  ( 0.000000000000000000, 0.000000000000000000, -1.000000000000000000 ) ) ;
#1060=AXIS2_PLACEMENT_3D ( 'NONE', #711, #5115, #2802 ) ;
#1062=LINE ( 'NONE', #4616, #7254 ) ;
#1070=CARTESIAN_POINT ( 'NONE',  ( -67.52238797519952129, 13.85924130086240602, -199.4941995012791267 ) ) ;
#1071=CARTESIAN_POINT ( 'NONE',  ( -1.655958715138094783, 0.9295642660359961784, -137.9252659957873561 ) ) ;
#1074=CARTESIAN_POINT ( 'NONE',  ( 5.844703153020811115, 9.999999999999998224, -103.2023327213425432 ) ) ;
#1078=AXIS2_PLACEMENT_3D ( 'NONE', #10444, #9206, #15103 ) ;
#1079=VERTEX_POINT ( 'NONE', #5708 ) ;
#1082=CARTESIAN_POINT ( 'NONE',  ( -61.70104298252753949, 14.99999999999465849, -192.5140885290328185 ) ) ;
#1084=ORIENTED_EDGE ( 'NONE', *, *, #2239, .T. ) ;
#1096=CARTESIAN_POINT ( 'NONE',  ( -5.795830733078562780, 9.999999999999998224, -117.2993747367960253 ) ) ;
#1100=DIRECTION ( 'NONE',  ( 0.000000000000000000, 0.000000000000000000, -1.000000000000000000 ) ) ;
#1103=B_SPLINE_CURVE_WITH_KNOTS ( 'NONE', 3,
 ( #3789, #14551, #10897, #9819, #470, #7410, #6410, #14391, #11129, #13230, #2869, #3947, #7568, #8572, #5183, #9578 ),
 .UNSPECIFIED., .F., .F.,
 ( 4, 2, 2, 2, 2, 2, 2, 4 ),
 ( 0.000000000000000000, 0.0004969249972743298906, 0.0009938499945486597813, 0.001490774991822989672, 0.001987699989097319563, 0.002981549983645979344, 0.003478474980920309018, 0.003975399978194639125 ),
 .UNSPECIFIED. ) ;
#1104=ORIENTED_EDGE ( 'NONE', *, *, #2330, .T. ) ;
#1108=CARTESIAN_POINT ( 'NONE',  ( 5.079523875978591896, 15.00000000000802558, -108.2552591983019994 ) ) ;
#1128=ORIENTED_EDGE ( 'NONE', *, *, #2993, .F. ) ;
#1135=DIRECTION ( 'NONE',  ( 0.000000000000000000, 0.000000000000000000, -1.000000000000000000 ) ) ;
#1139=ORIENTED_EDGE ( 'NONE', *, *, #7503, .F. ) ;
#1144=CARTESIAN_POINT ( 'NONE',  ( -65.74075837058826721, 15.17285174006052273, -202.4370987171274408 ) ) ;
#1151=EDGE_LOOP ( 'NONE', ( #10949, #5671, #3319 ) ) ;
#1154=CARTESIAN_POINT ( 'NONE',  ( -6.683304552674629306, 4.336808689942017736E-16, -104.1296019027812321 ) ) ;
#1156=ORIENTED_EDGE ( 'NONE', *, *, #11118, .T. ) ;
#1157=CARTESIAN_POINT ( 'NONE',  ( -5.229219651426930682, 15.00000000000000000, -111.7283649856961318 ) ) ;
#1164=CARTESIAN_POINT ( 'NONE',  ( 0.2625675448779583032, 9.999999999999998224, 2.974107436473179877 ) ) ;
#1167=CARTESIAN_POINT ( 'NONE',  ( -12.27209645382210823, 9.999999999999998224, -127.2227734861304782 ) ) ;
#1169=DIRECTION ( 'NONE',  ( 0.000000000000000000, 1.000000000000000000, 0.000000000000000000 ) ) ;
#1171=CARTESIAN_POINT ( 'NONE',  ( 4.856804767890293029, 14.90536770052035109, -1.840041787218291036 ) ) ;
#1172=CARTESIAN_POINT ( 'NONE',  ( 5.079523875935373134, 5.000000000000000888, -108.2552591983082806 ) ) ;
#1174=ORIENTED_EDGE ( 'NONE', *, *, #1793, .T. ) ;
#1175=CARTESIAN_POINT ( 'NONE',  ( -5.131649475197874288, -6.588576144931190669E-14, -112.7947322869705289 ) ) ;
#1179=CARTESIAN_POINT ( 'NONE',  ( -7.534724830571902565, 2.770061804015413626E-12, -106.8248685501869062 ) ) ;
#1189=EDGE_CURVE ( 'NONE', #5809, #1079, #10489, .T. ) ;
#1190=CARTESIAN_POINT ( 'NONE',  ( -0.4126978180549508712, 14.99999999999999822, -116.4224499489989881 ) ) ;
#1200=CARTESIAN_POINT ( 'NONE',  ( -12.27209645382210823, 2.500000000000000444, -127.2227734861304782 ) ) ;
#1205=EDGE_CURVE ( 'NONE', #12491, #8603, #12753, .T. ) ;
#1209=CARTESIAN_POINT ( 'NONE',  ( -65.95160144704729532, 15.05880728265431578, -200.7665161391323352 ) ) ;
#1210=CARTESIAN_POINT ( 'NONE',  ( -4.924771681124648026, 0.000000000000000000, -137.0932397189673111 ) ) ;
#1215=FACE_OUTER_BOUND ( 'NONE', #8276, .T. ) ;
#1216=DIRECTION ( 'NONE',  ( 0.000000000000000000, -1.000000000000000000, 0.000000000000000000 ) ) ;
#1217=VECTOR ( 'NONE', #7703, 1000.000000000000000 ) ;
#1222=CARTESIAN_POINT ( 'NONE',  ( -65.40294475132493801, 15.00000000000000000, -186.2934539482498337 ) ) ;
#1225=CARTESIAN_POINT ( 'NONE',  ( -5.447453277355505108, 9.999999999999998224, -116.0587048211077814 ) ) ;
#1233=AXIS2_PLACEMENT_3D ( 'NONE', #6432, #2733, #7667 ) ;
#1241=CARTESIAN_POINT ( 'NONE',  ( 4.261909775985413873, 13.80603281949575845, 3.020287175281327841 ) ) ;
#1245=CARTESIAN_POINT ( 'NONE',  ( -8.512178793150408040, 12.56551871291872580, -104.4358902311836914 ) ) ;
#1246=CARTESIAN_POINT ( 'NONE',  ( 4.586790536111674754, 8.673617379884035472E-16, -116.5616331785999762 ) ) ;
#1250=CARTESIAN_POINT ( 'NONE',  ( -2.641315011715085426, 4.336808689942017736E-16, -114.1979735927311879 ) ) ;
#1261=CARTESIAN_POINT ( 'NONE',  ( -47.98141941977416280, 15.00000000000000000, -149.0590141369269759 ) ) ;
#1267=ORIENTED_EDGE ( 'NONE', *, *, #557, .F. ) ;
#1268=CARTESIAN_POINT ( 'NONE',  ( -3.194662295375430894, 15.00000000000000178, -123.6199554999345764 ) ) ;
#1276=EDGE_LOOP ( 'NONE', ( #12705, #2489, #6368, #3902, #4448 ) ) ;
#1280=EDGE_CURVE ( 'NONE', #12491, #602, #5926, .T. ) ;
#1281=AXIS2_PLACEMENT_3D ( 'NONE', #1438, #6144, #1517 ) ;
#1282=CARTESIAN_POINT ( 'NONE',  ( -8.698259420408664511, 0.9528231151539969801, -104.5458497525427077 ) ) ;
#1294=EDGE_CURVE ( 'NONE', #4481, #15113, #12104, .T. ) ;
#1295=CARTESIAN_POINT ( 'NONE',  ( -64.28343470285902583, 14.09174185945640190, -209.5512319406730342 ) ) ;
#1306=CARTESIAN_POINT ( 'NONE',  ( -8.643796269099508933, 1.337050190792271387, -105.3552258418637706 ) ) ;
#1309=CARTESIAN_POINT ( 'NONE',  ( -6.422940335516989840, 9.999999999999998224, -108.3014594335602112 ) ) ;
#1310=CARTESIAN_POINT ( 'NONE',  ( 3.787708185468225519, 14.86616054401451414, -0.8541222820799866389 ) ) ;
#1311=CARTESIAN_POINT ( 'NONE',  ( -10.50399746308849913, 15.00000000000000000, -142.5005062768871653 ) ) ;
#1319=CARTESIAN_POINT ( 'NONE',  ( 2.198198389973041955, 14.05584352655475122, 1.458542947118257604 ) ) ;
#1321=CARTESIAN_POINT ( 'NONE',  ( -3.836704105290339228, 11.25565849803658125, -45.28046668454305035 ) ) ;
#1323=CARTESIAN_POINT ( 'NONE',  ( -8.886921396801742645, 2.500000000000000444, -105.5168766094550676 ) ) ;
#1326=CARTESIAN_POINT ( 'NONE',  ( -7.434246213560691707, 13.81406867328371746, -104.1118743468900050 ) ) ;
#1327=FACE_OUTER_BOUND ( 'NONE', #9612, .T. ) ;
#1331=CARTESIAN_POINT ( 'NONE',  ( -6.399074641068315472, 7.806255641895631925E-15, -108.4234853096273099 ) ) ;
#1336=VECTOR ( 'NONE', #1872, 1000.000000000000000 ) ;
#1340=CARTESIAN_POINT ( 'NONE',  ( -59.94788933440509737, 15.00000000000000000, -157.3141654283494120 ) ) ;
#1344=VECTOR ( 'NONE', #9791, 1000.000000000000227 ) ;
#1361=CARTESIAN_POINT ( 'NONE',  ( -40.67260926563410806, 10.00000000000000178, -157.6318504523734703 ) ) ;
#1362=CARTESIAN_POINT ( 'NONE',  ( -67.58382170693636226, 10.00000000000000000, -204.5178482451963191 ) ) ;
#1373=CARTESIAN_POINT ( 'NONE',  ( -63.21422129964969372, 10.11977001910463869, -203.6040552221171254 ) ) ;
#1374=DIRECTION ( 'NONE',  ( -0.000000000000000000, 1.000000000000000000, -0.000000000000000000 ) ) ;
#1378=B_SPLINE_CURVE_WITH_KNOTS ( 'NONE', 3,
 ( #1954, #13943, #12543, #14014, #15034, #6747 ),
 .UNSPECIFIED., .F., .F.,
 ( 4, 2, 4 ),
 ( 1.551583845779545699E-17, 0.006357786140926138634, 0.01271557228185226165 ),
 .UNSPECIFIED. ) ;
#1385=CARTESIAN_POINT ( 'NONE',  ( -9.094070923552267871, 1.650112951200696232, -104.6311941295649177 ) ) ;
#1388=CARTESIAN_POINT ( 'NONE',  ( -0.7574197398874851217, 14.99999999999999822, -108.9338761800286051 ) ) ;
#1389=CARTESIAN_POINT ( 'NONE',  ( 1.638000757872857260, 13.54559192810887680, 1.952774218784175231 ) ) ;
#1390=CARTESIAN_POINT ( 'NONE',  ( 1.818681402053747842, 9.999999999999998224, -137.3269588978967590 ) ) ;
#1394=CARTESIAN_POINT ( 'NONE',  ( -4.210400098449615491, 10.37725045066806295, -47.82562292290668893 ) ) ;
#1396=CARTESIAN_POINT ( 'NONE',  ( 0.8058036530323656743, 11.95234907359183296, 5.394660120521390212 ) ) ;
#1398=CARTESIAN_POINT ( 'NONE',  ( -47.48189921986827500, 5.000000000000000000, -141.5723758807981483 ) ) ;
#1402=CARTESIAN_POINT ( 'NONE',  ( -63.84637985160913587, 14.99926611874769478, -181.3101853188241535 ) ) ;
#1403=CIRCLE ( 'NONE', #15249, 14.80000000000025651 ) ;
#1407=ORIENTED_EDGE ( 'NONE', *, *, #4989, .F. ) ;
#1408=CARTESIAN_POINT ( 'NONE',  ( -4.554948446345685298, 4.336808689942017736E-16, -106.6475783469824847 ) ) ;
#1412=CARTESIAN_POINT ( 'NONE',  ( -18.07331279040889882, 2.111503226455494708, -129.3631649207090675 ) ) ;
#1413=VERTEX_POINT ( 'NONE', #5853 ) ;
#1417=CARTESIAN_POINT ( 'NONE',  ( -69.36122292246929533, 15.00000000000000000, -183.5207230678662143 ) ) ;
#1426=DIRECTION ( 'NONE',  ( 0.08794243244722413366, 0.000000000000000000, 0.9961255586397056438 ) ) ;
#1429=VERTEX_POINT ( 'NONE', #13048 ) ;
#1434=ORIENTED_EDGE ( 'NONE', *, *, #9620, .T. ) ;
#1438=CARTESIAN_POINT ( 'NONE',  ( -4.018470066652908734, 7.379999999999995453, -45.51728475810764962 ) ) ;
#1444=FACE_OUTER_BOUND ( 'NONE', #13418, .T. ) ;
#1446=EDGE_CURVE ( 'NONE', #12487, #2721, #6437, .T. ) ;
#1447=CARTESIAN_POINT ( 'NONE',  ( -67.58603348964146562, 10.40788280224345463, -204.4791092025774901 ) ) ;
#1452=CARTESIAN_POINT ( 'NONE',  ( -67.62826500021935772, 13.12245405995659375, -201.7210169101921906 ) ) ;
#1454=ORIENTED_EDGE ( 'NONE', *, *, #7611, .F. ) ;
#1457=CARTESIAN_POINT ( 'NONE',  ( -8.404493273108490925, 0.9205354583497085130, -105.1983221212521897 ) ) ;
#1460=CARTESIAN_POINT ( 'NONE',  ( -5.611193301459971750, 9.999999999999998224, -110.1737759617912786 ) ) ;
#1467=CARTESIAN_POINT ( 'NONE',  ( 2.538077654277008488, 14.29157444423261758, 1.114435963501728022 ) ) ;
#1471=CARTESIAN_POINT ( 'NONE',  ( -24.86990227130816322, 5.000000000000000888, -145.8847246090277281 ) ) ;
#1472=CARTESIAN_POINT ( 'NONE',  ( 0.7552767017137608230, 8.673617379884034486E-16, -110.7727649483667847 ) ) ;
#1479=CARTESIAN_POINT ( 'NONE',  ( -3.431082444819314681, 4.336808689942017736E-16, -108.8148713286762046 ) ) ;
#1483=VECTOR ( 'NONE', #11234, 1000.000000000000227 ) ;
#1490=CARTESIAN_POINT ( 'NONE',  ( -68.53010506246435796, 15.00000000000343370, -179.3208756447880035 ) ) ;
#1501=LINE ( 'NONE', #1808, #1483 ) ;
#1512=CIRCLE ( 'NONE', #14350, 5.000000000000002665 ) ;
#1516=CARTESIAN_POINT ( 'NONE',  ( -9.240119717576693148, 2.330807083298499727, -104.6630069175297706 ) ) ;
#1517=DIRECTION ( 'NONE',  ( -0.08794243244722436958, 0.000000000000000000, -0.9961255586397055328 ) ) ;
#1518=CARTESIAN_POINT ( 'NONE',  ( -56.40225323527551637, 14.99999999999999645, -165.3314606177903272 ) ) ;
#1528=CARTESIAN_POINT ( 'NONE',  ( -67.60597199914535338, 11.34385781021491368, -204.0782660919513773 ) ) ;
#1533=CARTESIAN_POINT ( 'NONE',  ( -67.58382170693636226, 10.00000000000000000, -204.5178482451963191 ) ) ;
#1534=VERTEX_POINT ( 'NONE', #15310 ) ;
#1538=CARTESIAN_POINT ( 'NONE',  ( -70.08363909706210393, 10.00000000000000178, -190.3084480996344894 ) ) ;
#1541=DIRECTION ( 'NONE',  ( 0.000000000000000000, -1.000000000000000000, -0.000000000000000000 ) ) ;
#1542=CARTESIAN_POINT ( 'NONE',  ( 0.02975126090548325941, 2.500000000000000444, 0.3369930824702306316 ) ) ;
#1548=CARTESIAN_POINT ( 'NONE',  ( -3.822630838043659995, 11.22863355747944070, -45.03847635001736904 ) ) ;
#1550=CARTESIAN_POINT ( 'NONE',  ( 3.873902325247619238, 13.05645226711805584, 3.961767634410926497 ) ) ;
#1552=AXIS2_PLACEMENT_3D ( 'NONE', #7228, #9333, #4841 ) ;
#1553=CARTESIAN_POINT ( 'NONE',  ( -8.469744009338400659, 7.499999999999991118, -95.93694702384601669 ) ) ;
#1557=ORIENTED_EDGE ( 'NONE', *, *, #4888, .T. ) ;
#1558=EDGE_CURVE ( 'NONE', #13993, #3117, #2467, .T. ) ;
#1566=EDGE_LOOP ( 'NONE', ( #14097, #9470, #2283, #12579 ) ) ;
#1568=AXIS2_PLACEMENT_3D ( 'NONE', #4173, #11049, #8877 ) ;
#1571=CARTESIAN_POINT ( 'NONE',  ( -68.53010506257494683, 9.999999999999998224, -179.3208756447420171 ) ) ;
#1572=CARTESIAN_POINT ( 'NONE',  ( 2.850044070969222521, 9.999999999999998224, -103.0233998225063345 ) ) ;
#1580=LINE ( 'NONE', #424, #5918 ) ;
#1583=EDGE_LOOP ( 'NONE', ( #14859, #10275 ) ) ;
#1586=DIRECTION ( 'NONE',  ( 0.08794243244723003172, 0.000000000000000000, 0.9961255586397049777 ) ) ;
#1592=CARTESIAN_POINT ( 'NONE',  ( -63.21422130130007133, 5.000000000000000000, -203.6040552426024703 ) ) ;
#1594=AXIS2_PLACEMENT_3D ( 'NONE', #11291, #713, #5417 ) ;
#1596=CARTESIAN_POINT ( 'NONE',  ( -54.80198710092766134, 10.00000000000000000, -172.3578233953475376 ) ) ;
#1599=CARTESIAN_POINT ( 'NONE',  ( 0.4711736884522539359, 15.00000000000000000, 5.336993082470237404 ) ) ;
#1608=CARTESIAN_POINT ( 'NONE',  ( -65.16270098009177048, 15.39946212108827162, -205.5516834495680598 ) ) ;
#1612=CARTESIAN_POINT ( 'NONE',  ( -67.59204273365905635, 13.51751734435156393, -200.6893734332653310 ) ) ;
#1617=CARTESIAN_POINT ( 'NONE',  ( -52.57969357448924796, 9.999999999999998224, -146.7268407086697550 ) ) ;
#1622=CARTESIAN_POINT ( 'NONE',  ( -25.68053481550299111, 15.00000000000000000, -142.4798935003980773 ) ) ;
#1626=CARTESIAN_POINT ( 'NONE',  ( -3.911481695397140079, 10.31382935203035700, -44.10643064657414669 ) ) ;
#1629=DIRECTION ( 'NONE',  ( -1.000000000000000000, -0.000000000000000000, -0.000000000000000000 ) ) ;
#1635=ORIENTED_EDGE ( 'NONE', *, *, #14289, .F. ) ;
#1641=ORIENTED_EDGE ( 'NONE', *, *, #6101, .F. ) ;
#1646=CARTESIAN_POINT ( 'NONE',  ( -70.10710660171159248, 9.999999999999998224, -192.1972859456682272 ) ) ;
#1650=CARTESIAN_POINT ( 'NONE',  ( -1.724164254788412842, 5.321094445766560987, -19.52964039877223712 ) ) ;
#1662=CLOSED_SHELL ( 'NONE', ( #7737, #15014, #7787, #3243, #13011, #13938, #9045, #14931, #2350, #1864, #9390, #10283, #3651, #15291, #11753, #4537, #13090, #449, #10997, #58, #13744, #5453, #13226, #15012, #3092, #6226, #1730, #3438, #8060, #8777, #2977, #13473, #11933, #4422, #6588, #3630, #13410, #5924, #9781, #9302, #9383, #13206, #3954, #2049, #9694, #8178, #4869, #4115, #3265, #7713, #8567, #13066, #11586, #3270, #4200, #818, #9047, #13191, #6344, #3477, #14846, #7870, #13411, #9664, #8565, #1943, #13205, #252, #6858, #4238, #10365, #14316, #8728, #6312, #5991, #7625, #6166, #12049, #12321 ) ) ;
#1674=VERTEX_POINT ( 'NONE', #6247 ) ;
#1679=CARTESIAN_POINT ( 'NONE',  ( 0.4757783475439041343, 3.128924928913413339, 5.389150141154763318 ) ) ;
#1684=CARTESIAN_POINT ( 'NONE',  ( -67.61802425151131501, 11.74280943683806377, -203.7724845797763464 ) ) ;
#1688=CARTESIAN_POINT ( 'NONE',  ( -32.47904071408094495, 15.00000000000000000, -151.1158311594353734 ) ) ;
#1691=CARTESIAN_POINT ( 'NONE',  ( 2.752881441477225355, 9.999999999999998224, 2.754251355355159081 ) ) ;
#1692=CARTESIAN_POINT ( 'NONE',  ( -12.27209645382209757, 2.500000000000000444, -127.2227734861304782 ) ) ;
#1697=CARTESIAN_POINT ( 'NONE',  ( -4.222591397270751834, 9.819471330552410393, -47.66802519420133422 ) ) ;
#1703=CARTESIAN_POINT ( 'NONE',  ( 6.049910241306248437, 0.000000000000000000, -118.3734240199295300 ) ) ;
#1708=CARTESIAN_POINT ( 'NONE',  ( 4.373577830794676657, 12.45268385026016666, -1.811168651986067468 ) ) ;
#1709=DIRECTION ( 'NONE',  ( -0.9961255586397055328, 0.000000000000000000, 0.08794243244722428632 ) ) ;
#1716=CARTESIAN_POINT ( 'NONE',  ( 1.893911505664648054, 0.000000000000000000, -1.663006917529762152 ) ) ;
#1720=CARTESIAN_POINT ( 'NONE',  ( -6.226828414324827143, 9.999999999999996447, -108.7107943239692673 ) ) ;
#1730=ADVANCED_FACE ( 'NONE', ( #9878, #7478 ), #12275, .F. ) ;
#1731=CARTESIAN_POINT ( 'NONE',  ( -1.330285697047033366, 7.379999999999995453, -43.49585833228641008 ) ) ;
#1736=EDGE_LOOP ( 'NONE', ( #13514, #5414, #2878, #5216 ) ) ;
#1742=CARTESIAN_POINT ( 'NONE',  ( -4.743345422599378303, 15.00000000000000000, -103.3611366015581154 ) ) ;
#1746=DIRECTION ( 'NONE',  ( 0.000000000000000000, -1.000000000000000000, 0.000000000000000000 ) ) ;
#1752=TOROIDAL_SURFACE ( 'NONE', #1009, 9.800000000000245848, 5.000000000000000000 ) ;
#1755=CARTESIAN_POINT ( 'NONE',  ( 3.230086961373112242, 15.00000000000000000, 5.208283729180106292 ) ) ;
#1759=CARTESIAN_POINT ( 'NONE',  ( 2.928550336651898789, 0.6497958086621815621, 2.702460884016614440 ) ) ;
#1766=CARTESIAN_POINT ( 'NONE',  ( -69.76017711480231753, 9.999999999999998224, -197.5794603834288239 ) ) ;
#1773=CARTESIAN_POINT ( 'NONE',  ( -63.21422130130007133, 15.00000000000000000, -203.6040552426024703 ) ) ;
#1777=CARTESIAN_POINT ( 'NONE',  ( -17.32624372123753886, 2.500000000000000444, -122.3796757791585321 ) ) ;
#1778=CARTESIAN_POINT ( 'NONE',  ( -3.329332828452641113, 9.806810919949601413, -43.39695214296718717 ) ) ;
#1787=CARTESIAN_POINT ( 'NONE',  ( -36.05823818790233304, 15.00000000000000000, -151.2682901559026334 ) ) ;
#1789=ORIENTED_EDGE ( 'NONE', *, *, #9515, .F. ) ;
#1793=EDGE_CURVE ( 'NONE', #4876, #14091, #11126, .T. ) ;
#1799=DIRECTION ( 'NONE',  ( 0.000000000000000000, 0.000000000000000000, -1.000000000000000000 ) ) ;
#1802=CARTESIAN_POINT ( 'NONE',  ( -67.29661116483784156, 9.999999999999998224, -205.0278900928575183 ) ) ;
#1807=DIRECTION ( 'NONE',  ( -0.000000000000000000, -1.000000000000000000, -0.000000000000000000 ) ) ;
#1808=CARTESIAN_POINT ( 'NONE',  ( 0.4711736884522539359, 9.999999999999998224, 5.336993082470237404 ) ) ;
#1809=CARTESIAN_POINT ( 'NONE',  ( 2.011321487292375032, 9.999999999999998224, -137.8771695030452520 ) ) ;
#1815=CIRCLE ( 'NONE', #11424, 2.500000000000000000 ) ;
#1818=ORIENTED_EDGE ( 'NONE', *, *, #14993, .F. ) ;
#1829=( BOUNDED_SURFACE ( )  B_SPLINE_SURFACE ( 3, 2, ( 
 ( #11691, #7042, #10380 ),
 ( #2042, #6974, #12704 ),
 ( #7984, #1108, #14096 ),
 ( #11759, #15119, #4510 ),
 ( #14020, #10601, #3417 ),
 ( #3346, #10533, #14177 ) ),
 .UNSPECIFIED., .F., .F., .T. ) 
 B_SPLINE_SURFACE_WITH_KNOTS ( ( 4, 2, 4 ),
 ( 3, 3 ),
 ( 0.000000000000000000, 0.006940540637791398938, 0.01388108127558279788 ),
 ( 0.000000000000000000, 1.000000000000000000 ),
 .UNSPECIFIED. ) 
 GEOMETRIC_REPRESENTATION_ITEM ( )  RATIONAL_B_SPLINE_SURFACE ( (
 ( 1.000000000000000000, 0.7071067811865471286, 1.000000000000000000),
 ( 1.000000000000000000, 0.7071067811865471286, 1.000000000000000000),
 ( 1.000000000000000000, 0.7071067811865475727, 1.000000000000000000),
 ( 1.000000000000000000, 0.7071067811865475727, 1.000000000000000000),
 ( 1.000000000000000000, 0.7071067811865469066, 1.000000000000000000),
 ( 1.000000000000000000, 0.7071067811865469066, 1.000000000000000000) ) ) 
 REPRESENTATION_ITEM ( '' )  SURFACE ( )  );
#1830=ORIENTED_EDGE ( 'NONE', *, *, #6589, .F. ) ;
#1834=ORIENTED_EDGE ( 'NONE', *, *, #320, .F. ) ;
#1839=CARTESIAN_POINT ( 'NONE',  ( 7.641599596749856005, 4.009295114047140451, -21.18645330027491269 ) ) ;
#1840=CARTESIAN_POINT ( 'NONE',  ( 0.4810967732360011406, 3.291314837355760137, 5.449392047321778065 ) ) ;
#1841=EDGE_CURVE ( 'NONE', #6670, #6553, #10134, .T. ) ;
#1846=CIRCLE ( 'NONE', #11944, 7.000000000000016875 ) ;
#1852=CARTESIAN_POINT ( 'NONE',  ( -7.737061903549631303, 15.00000000000000888, -106.6108512366692480 ) ) ;
#1864=ADVANCED_FACE ( 'NONE', ( #13749 ), #1752, .T. ) ;
#1866=EDGE_LOOP ( 'NONE', ( #5293, #14647, #10401, #9553 ) ) ;
#1869=CARTESIAN_POINT ( 'NONE',  ( -48.65881315193669110, 15.00000000000000000, -156.6898889965183628 ) ) ;
#1872=DIRECTION ( 'NONE',  ( -0.000000000000000000, -1.000000000000000000, -0.000000000000000000 ) ) ;
#1880=CARTESIAN_POINT ( 'NONE',  ( -67.78894976056668042, 9.999999999999998224, -204.1377247873641068 ) ) ;
#1881=CARTESIAN_POINT ( 'NONE',  ( -18.09353981420591140, -1.734723475976807094E-15, -129.3374956033358387 ) ) ;
#1885=DIRECTION ( 'NONE',  ( -0.000000000000000000, -1.000000000000000000, -0.000000000000000000 ) ) ;
#1887=CARTESIAN_POINT ( 'NONE',  ( 3.116228908706373701, 1.920977637013419947, 4.205425761845583033 ) ) ;
#1894=ORIENTED_EDGE ( 'NONE', *, *, #4195, .T. ) ;
#1897=CARTESIAN_POINT ( 'NONE',  ( 2.159942170319879562, 9.999999999999998224, -121.5147849362692369 ) ) ;
#1904=EDGE_LOOP ( 'NONE', ( #3933, #12185, #4859, #13166 ) ) ;
#1909=EDGE_LOOP ( 'NONE', ( #149, #8122, #8707, #7208 ) ) ;
#1913=CARTESIAN_POINT ( 'NONE',  ( 7.393739102816695663, 4.119861755223847233, -25.69316058899638833 ) ) ;
#1914=CARTESIAN_POINT ( 'NONE',  ( 3.154843497088497539, 2.483716029600458786, 4.543567367663276180 ) ) ;
#1918=CARTESIAN_POINT ( 'NONE',  ( -25.82983890416511841, 9.999999999999998224, -142.4527639562402328 ) ) ;
#1919=EDGE_LOOP ( 'NONE', ( #1454, #5980, #12777, #11990, #5653, #6083, #4304, #7053, #3449, #13322, #1156, #2244 ) ) ;
#1920=CARTESIAN_POINT ( 'NONE',  ( -68.74655823203735849, 9.999999999999998224, -201.8315121478229912 ) ) ;
#1923=CARTESIAN_POINT ( 'NONE',  ( -6.591932536214704541, 4.336808689942017736E-16, -124.2971136505211831 ) ) ;
#1929=DIRECTION ( 'NONE',  ( -0.9961255586397049777, -0.000000000000000000, 0.08794243244723004560 ) ) ;
#1931=CARTESIAN_POINT ( 'NONE',  ( 4.284495748330572340, 14.99196994537862260, -0.3632064617744598656 ) ) ;
#1937=CARTESIAN_POINT ( 'NONE',  ( -35.54172072644912106, 15.00000000000000000, -156.2450653136882011 ) ) ;
#1940=CARTESIAN_POINT ( 'NONE',  ( -14.61394712176886834, 5.000000000000000888, -133.7291658263849854 ) ) ;
#1943=ADVANCED_FACE ( 'NONE', ( #11498 ), #11566, .F. ) ;
#1948=CARTESIAN_POINT ( 'NONE',  ( -68.19209817244900762, 9.999999999999998224, -203.2686135453940608 ) ) ;
#1953=CARTESIAN_POINT ( 'NONE',  ( 2.597361546216158334, 7.589415207398532024E-16, 0.5567601655735897603 ) ) ;
#1954=CARTESIAN_POINT ( 'NONE',  ( 3.136841903360915396, 5.000000000000000888, -104.4936450199714955 ) ) ;
#1969=LINE ( 'NONE', #2192, #15083 ) ;
#1974=CARTESIAN_POINT ( 'NONE',  ( 2.539506111722884096, 15.00000000000000000, -24.39141914772463693 ) ) ;
#1987=CARTESIAN_POINT ( 'NONE',  ( 3.030111226435038052, 1.214660924608283343, 3.496784441768035379 ) ) ;
#2004=ORIENTED_EDGE ( 'NONE', *, *, #8855, .T. ) ;
#2008=CARTESIAN_POINT ( 'NONE',  ( -7.400090585548307232, 4.336808689942017736E-16, -125.4022374643889464 ) ) ;
#2016=CARTESIAN_POINT ( 'NONE',  ( -29.69515346086419427, 15.00000000000000000, -156.7390981038714699 ) ) ;
#2018=ORIENTED_EDGE ( 'NONE', *, *, #3173, .F. ) ;
#2020=FACE_OUTER_BOUND ( 'NONE', #5308, .T. ) ;
#2021=DIRECTION ( 'NONE',  ( -0.08794243244722427244, 0.000000000000000000, -0.9961255586397055328 ) ) ;
#2032=CARTESIAN_POINT ( 'NONE',  ( 4.439041005648131311, 14.09689541346372543, 2.512619722007936041 ) ) ;
#2034=CARTESIAN_POINT ( 'NONE',  ( -3.042169416580296826, 8.673617379884035472E-16, -135.1880271770022546 ) ) ;
#2038=ORIENTED_EDGE ( 'NONE', *, *, #9298, .T. ) ;
#2042=CARTESIAN_POINT ( 'NONE',  ( 4.047901358979359543, 9.999999999999998224, -106.4041221358673113 ) ) ;
#2046=CARTESIAN_POINT ( 'NONE',  ( -7.344214697115496904, 13.90884050551771622, -104.3832092088654804 ) ) ;
#2047=DIRECTION ( 'NONE',  ( 0.000000000000000000, 0.000000000000000000, -1.000000000000000000 ) ) ;
#2049=ADVANCED_FACE ( 'NONE', ( #8333 ), #9392, .T. ) ;
#2062=DIRECTION ( 'NONE',  ( -0.9961255586397049777, -0.000000000000000000, 0.08794243244723004560 ) ) ;
#2066=AXIS2_PLACEMENT_3D ( 'NONE', #9354, #3562, #8192 ) ;
#2073=ORIENTED_EDGE ( 'NONE', *, *, #7235, .F. ) ;
#2074=AXIS2_PLACEMENT_3D ( 'NONE', #4044, #4270, #8750 ) ;
#2077=DIRECTION ( 'NONE',  ( 0.000000000000000000, 0.000000000000000000, -1.000000000000000000 ) ) ;
#2080=CARTESIAN_POINT ( 'NONE',  ( -67.21428272770161527, 14.43681881222333629, -196.2604947070364574 ) ) ;
#2081=CARTESIAN_POINT ( 'NONE',  ( -3.862572585540200443, 9.963559498897122779, -43.53919170703361630 ) ) ;
#2089=DIRECTION ( 'NONE',  ( 0.000000000000000000, -1.000000000000000000, 0.000000000000000000 ) ) ;
#2090=CARTESIAN_POINT ( 'NONE',  ( -59.62538729158823969, 9.999999999999998224, -184.0486941882289784 ) ) ;
#2095=( BOUNDED_SURFACE ( )  B_SPLINE_SURFACE ( 3, 1, ( 
 ( #10450, #3116 ),
 ( #9212, #7829 ),
 ( #8121, #11534 ),
 ( #15112, #9065 ) ),
 .UNSPECIFIED., .F., .F., .F. ) 
 B_SPLINE_SURFACE_WITH_KNOTS ( ( 4, 4 ),
 ( 2, 2 ),
 ( 0.000000000000000000, 1.000000000000000000 ),
 ( 0.000000000000000000, 1.000000000000000000 ),
 .UNSPECIFIED. ) 
 GEOMETRIC_REPRESENTATION_ITEM ( )  RATIONAL_B_SPLINE_SURFACE ( (
 ( 1.000000000000000000, 1.000000000000000000),
 ( 0.9206647990551181104, 0.9206647990551181104),
 ( 0.9206647990551181104, 0.9206647990551181104),
 ( 1.000000000000000000, 1.000000000000000000) ) ) 
 REPRESENTATION_ITEM ( '' )  SURFACE ( )  );
#2097=AXIS2_PLACEMENT_3D ( 'NONE', #10330, #12740, #7859 ) ;
#2101=CARTESIAN_POINT ( 'NONE',  ( -13.05415704217878670, 0.000000000000000000, -133.9853474364657870 ) ) ;
#2105=CARTESIAN_POINT ( 'NONE',  ( -8.725755766768878985, 11.34072931828999309, -105.4285433685658546 ) ) ;
#2107=CARTESIAN_POINT ( 'NONE',  ( -2.141054399116761875, 15.00000000000000000, -102.7251783244459631 ) ) ;
#2110=CARTESIAN_POINT ( 'NONE',  ( 3.230086961373113130, 4.669421605118766472, 5.208283729180105404 ) ) ;
#2139=FACE_OUTER_BOUND ( 'NONE', #4677, .T. ) ;
#2146=CARTESIAN_POINT ( 'NONE',  ( 10.01939027896081313, 9.999999999999998224, -127.6977514918621637 ) ) ;
#2150=ORIENTED_EDGE ( 'NONE', *, *, #12494, .T. ) ;
#2157=CARTESIAN_POINT ( 'NONE',  ( -32.49979969806456381, 5.000000000000000000, -156.1716796081737186 ) ) ;
#2159=CARTESIAN_POINT ( 'NONE',  ( -65.38695984819520390, 14.99496204924664333, -188.1638777877195707 ) ) ;
#2162=CARTESIAN_POINT ( 'NONE',  ( -12.27209645382210823, 9.999999999999998224, -127.2227734861304782 ) ) ;
#2164=DIRECTION ( 'NONE',  ( -0.000000000000000000, -1.000000000000000000, -0.000000000000000000 ) ) ;
#2168=CARTESIAN_POINT ( 'NONE',  ( -53.33476332432898914, 9.999999999999998224, -169.8150382216356320 ) ) ;
#2171=CARTESIAN_POINT ( 'NONE',  ( 9.939878312292620421, 5.000000000000000888, -115.2320631035898373 ) ) ;
#2182=CARTESIAN_POINT ( 'NONE',  ( 3.555703521826507174, 14.99969716236488182, -12.86313601129666750 ) ) ;
#2184=EDGE_LOOP ( 'NONE', ( #13158, #1128, #13339, #9772 ) ) ;
#2189=DIRECTION ( 'NONE',  ( 0.000000000000000000, -1.000000000000000000, -0.000000000000000000 ) ) ;
#2192=CARTESIAN_POINT ( 'NONE',  ( -67.58382170693636226, 15.00000000000000000, -204.5178482451963191 ) ) ;
#2202=ORIENTED_EDGE ( 'NONE', *, *, #1189, .T. ) ;
#2212=CARTESIAN_POINT ( 'NONE',  ( -7.160896140961710898, 10.00000000000000000, -146.2205208844301580 ) ) ;
#2214=CARTESIAN_POINT ( 'NONE',  ( -63.21837158064308682, 15.00000000000000000, -178.6113122644988209 ) ) ;
#2215=EDGE_CURVE ( 'NONE', #1043, #8933, #6187, .T. ) ;
#2218=ORIENTED_EDGE ( 'NONE', *, *, #10940, .F. ) ;
#2227=CARTESIAN_POINT ( 'NONE',  ( -65.07427810169019722, 14.43681881204452111, -196.3032221514726530 ) ) ;
#2232=VECTOR ( 'NONE', #6285, 1000.000000000000000 ) ;
#2234=DIRECTION ( 'NONE',  ( 0.000000000000000000, 0.6972771395097921987, 0.7168016397282039875 ) ) ;
#2239=EDGE_CURVE ( 'NONE', #6631, #9693, #10763, .T. ) ;
#2240=CARTESIAN_POINT ( 'NONE',  ( -63.02554947701982968, 9.999999999999998224, -201.1265914030773843 ) ) ;
#2241=EDGE_CURVE ( 'NONE', #6383, #12545, #3461, .T. ) ;
#2242=AXIS2_PLACEMENT_3D ( 'NONE', #2744, #4063, #12164 ) ;
#2244=ORIENTED_EDGE ( 'NONE', *, *, #6102, .T. ) ;
#2264=EDGE_LOOP ( 'NONE', ( #2985, #423, #13054, #6040 ) ) ;
#2271=AXIS2_PLACEMENT_3D ( 'NONE', #8010, #10629, #8234 ) ;
#2273=CARTESIAN_POINT ( 'NONE',  ( -49.70557948942859383, 14.99999999999999467, -143.6055563704040026 ) ) ;
#2275=( LENGTH_UNIT ( ) NAMED_UNIT ( * ) SI_UNIT ( .MILLI., .METRE. ) );
#2281=CARTESIAN_POINT ( 'NONE',  ( -1.509598306946452917, 15.00000000000000000, -120.1442827665486135 ) ) ;
#2283=ORIENTED_EDGE ( 'NONE', *, *, #9491, .F. ) ;
#2284=ORIENTED_EDGE ( 'NONE', *, *, #10998, .F. ) ;
#2289=VERTEX_POINT ( 'NONE', #6186 ) ;
#2299=DIRECTION ( 'NONE',  ( 0.9961255586397054218, -0.000000000000000000, -0.08794243244722428632 ) ) ;
#2307=EDGE_CURVE ( 'NONE', #14034, #6631, #2734, .T. ) ;
#2308=CARTESIAN_POINT ( 'NONE',  ( -66.14601255874971741, 14.98129325284761215, -196.3414374098033193 ) ) ;
#2309=CARTESIAN_POINT ( 'NONE',  ( -0.5658740575277120266, 1.810181481809467696, -138.1533701416837800 ) ) ;
#2321=CARTESIAN_POINT ( 'NONE',  ( -55.02646020061353482, 15.00000000000000000, -163.3737094562771972 ) ) ;
#2324=CARTESIAN_POINT ( 'NONE',  ( -1.406912714274181297, 15.00000000000000000, -119.8620791452180185 ) ) ;
#2330=EDGE_CURVE ( 'NONE', #3581, #4145, #11123, .T. ) ;
#2333=DIRECTION ( 'NONE',  ( -0.000000000000000000, -1.000000000000000000, -0.000000000000000000 ) ) ;
#2334=CARTESIAN_POINT ( 'NONE',  ( 9.939878312292615092, 5.000000000000000888, -115.2320631035898373 ) ) ;
#2335=DIRECTION ( 'NONE',  ( -0.08794243244722420305, -1.868163743359636407E-15, -0.9961255586397055328 ) ) ;
#2336=CARTESIAN_POINT ( 'NONE',  ( 3.390724094347318029, 11.60484605096695532, 4.922330974931754533 ) ) ;
#2339=CARTESIAN_POINT ( 'NONE',  ( 1.855481649321460091, 15.00000000000000000, -35.83830032691798095 ) ) ;
#2340=CARTESIAN_POINT ( 'NONE',  ( 6.049910241306251990, 8.673617379884035472E-16, -118.3734240199295300 ) ) ;
#2350=ADVANCED_FACE ( 'NONE', ( #12520 ), #2484, .T. ) ;
#2357=CARTESIAN_POINT ( 'NONE',  ( -17.32624372123753886, 0.000000000000000000, -122.3796757791585321 ) ) ;
#2364=EDGE_LOOP ( 'NONE', ( #11780, #14151, #12930, #13139 ) ) ;
#2369=CARTESIAN_POINT ( 'NONE',  ( 6.025425613339945308, 10.00000000000000355, -132.6130656762864248 ) ) ;
#2372=CARTESIAN_POINT ( 'NONE',  ( -46.71028124165312079, 15.00000000000000000, -147.6754287972959503 ) ) ;
#2374=LINE ( 'NONE', #8165, #2794 ) ;
#2377=CARTESIAN_POINT ( 'NONE',  ( -65.21504661764039668, 14.99629524799717650, -187.1630048673123383 ) ) ;
#2383=CARTESIAN_POINT ( 'NONE',  ( 2.863878713867060277, 15.00000000000000000, -24.41542356333742703 ) ) ;
#2388=CARTESIAN_POINT ( 'NONE',  ( -53.69697306016067273, 14.99999999999731948, -170.4167521506885237 ) ) ;
#2390=ORIENTED_EDGE ( 'NONE', *, *, #13032, .T. ) ;
#2391=CARTESIAN_POINT ( 'NONE',  ( -7.119867912801005616, 9.999999999999998224, -107.3464651432735195 ) ) ;
#2400=CARTESIAN_POINT ( 'NONE',  ( -16.94138229547581531, 5.000000000000000000, -154.2864167784019571 ) ) ;
#2401=DIRECTION ( 'NONE',  ( -0.2611699024796619306, 0.000000000000000000, -0.9652928478129131351 ) ) ;
#2402=CYLINDRICAL_SURFACE ( 'NONE', #11085, 5.000000000000000000 ) ;
#2406=CARTESIAN_POINT ( 'NONE',  ( -65.03433155014064937, 14.91485314970007003, -188.6938424094274751 ) ) ;
#2408=EDGE_CURVE ( 'NONE', #15312, #411, #14086, .T. ) ;
#2410=CARTESIAN_POINT ( 'NONE',  ( -2.902626628659604968, 4.336808689942017736E-16, -110.5536484212200463 ) ) ;
#2414=CARTESIAN_POINT ( 'NONE',  ( -16.94138229547582242, 9.999999999999998224, -154.2864167784019003 ) ) ;
#2415=ORIENTED_EDGE ( 'NONE', *, *, #3077, .F. ) ;
#2424=CARTESIAN_POINT ( 'NONE',  ( -44.21823081166466096, 15.00000000000000000, -145.3603131190973272 ) ) ;
#2425=ORIENTED_EDGE ( 'NONE', *, *, #11774, .T. ) ;
#2430=ORIENTED_EDGE ( 'NONE', *, *, #10165, .T. ) ;
#2433=EDGE_CURVE ( 'NONE', #12487, #12545, #11214, .T. ) ;
#2435=ORIENTED_EDGE ( 'NONE', *, *, #14894, .T. ) ;
#2437=DIRECTION ( 'NONE',  ( 0.000000000000000000, 0.000000000000000000, -1.000000000000000000 ) ) ;
#2440=CARTESIAN_POINT ( 'NONE',  ( -6.224392388573470214, 2.500000000000000000, -108.7152457258569314 ) ) ;
#2445=B_SPLINE_CURVE_WITH_KNOTS ( 'NONE', 3,
 ( #7854, #681, #2851, #11034, #1839, #11103, #5387, #14838, #4162, #4237, #7551, #14687, #14764, #6320, #13670, #608, #3069, #5239, #7783, #5160, #8864, #12496, #1913, #5466, #14918, #12269 ),
 .UNSPECIFIED., .F., .F.,
 ( 4, 2, 2, 2, 2, 2, 2, 2, 2, 2, 2, 2, 4 ),
 ( 0.000000000000000000, 0.0009121890263906905130, 0.001368283539586035444, 0.001824378052781380592, 0.002280472565976725523, 0.002736567079172070888, 0.003648756105562761184, 0.004560945131953451914, 0.005017039645148801616, 0.005473134158344152185, 0.005929228671539501887, 0.006385323184734852456, 0.007297512211125546655 ),
 .UNSPECIFIED. ) ;
#2448=APPLICATION_CONTEXT ( 'configuration controlled 3d designs of mechanical parts and assemblies' ) ;
#2452=CARTESIAN_POINT ( 'NONE',  ( -63.36957375107780877, 11.34385781002516858, -203.2580046453681177 ) ) ;
#2459=CARTESIAN_POINT ( 'NONE',  ( -16.85248002973657577, 0.2716729216455838203, -130.7235999261775419 ) ) ;
#2460=AXIS2_PLACEMENT_3D ( 'NONE', #4582, #9289, #3411 ) ;
#2464=CARTESIAN_POINT ( 'NONE',  ( -9.172836789864245333, 1.744788764959713134, -105.1340277003996846 ) ) ;
#2467=B_SPLINE_CURVE_WITH_KNOTS ( 'NONE', 3,
 ( #5927, #8322, #10652, #13214, #2459, #67, #9493, #10799 ),
 .UNSPECIFIED., .F., .F.,
 ( 4, 2, 2, 4 ),
 ( 3.497257266061400950E-18, 0.001156836261567012903, 0.001735254392350513934, 0.002313672523134014964 ),
 .UNSPECIFIED. ) ;
#2468=CARTESIAN_POINT ( 'NONE',  ( -5.365035937071200856, 15.00000000000000000, -111.0566899280935473 ) ) ;
#2471=CARTESIAN_POINT ( 'NONE',  ( 6.020998550614976352, 9.999999999999998224, -132.6181299100964281 ) ) ;
#2478=CARTESIAN_POINT ( 'NONE',  ( 3.821717871283383250, 14.91756675554889888, 1.043977372916836233 ) ) ;
#2481=AXIS2_PLACEMENT_3D ( 'NONE', #13179, #12468, #14810 ) ;
#2484=TOROIDAL_SURFACE ( 'NONE', #11617, 11.99999999999994138, 5.000000000000000000 ) ;
#2486=CARTESIAN_POINT ( 'NONE',  ( -64.96257786778912191, 14.30082101381936788, -197.2009545595533382 ) ) ;
#2488=ORIENTED_EDGE ( 'NONE', *, *, #8197, .F. ) ;
#2489=ORIENTED_EDGE ( 'NONE', *, *, #1558, .F. ) ;
#2490=CARTESIAN_POINT ( 'NONE',  ( -6.947321920531724260, 4.336808689942017736E-16, -120.0269581757037969 ) ) ;
#2498=AXIS2_PLACEMENT_3D ( 'NONE', #13285, #3852, #7312 ) ;
#2499=( BOUNDED_SURFACE ( )  B_SPLINE_SURFACE ( 3, 2, ( 
 ( #11526, #942, #1164 ),
 ( #5645, #4723, #10363 ),
 ( #12213, #13232, #3636 ),
 ( #13387, #10814, #8498 ),
 ( #11895, #1396, #9748 ),
 ( #2634, #86, #10669 ),
 ( #6099, #13307, #5030 ),
 ( #2792, #13149, #10980 ),
 ( #3792, #8416, #6180 ),
 ( #8574, #230, #159 ),
 ( #7336, #12134, #14307 ),
 ( #12047, #2559, #7261 ),
 ( #1550, #397, #10899 ),
 ( #11976, #4797, #14553 ),
 ( #14476, #2709, #8653 ),
 ( #7495, #4946, #9510 ),
 ( #14393, #5945, #1319 ),
 ( #7412, #6023, #1467 ),
 ( #9661, #315, #3873 ),
 ( #14234, #6264, #8338 ),
 ( #13063, #2478, #7174 ),
 ( #3949, #10744, #4868 ),
 ( #9580, #5106, #3708 ),
 ( #9821, #1931, #10048 ),
 ( #7869, #5334, #14632 ),
 ( #547, #12289, #14784 ),
 ( #5485, #629, #14710 ),
 ( #4110, #8811, #11208 ) ),
 .UNSPECIFIED., .F., .F., .F. ) 
 B_SPLINE_SURFACE_WITH_KNOTS ( ( 4, 2, 2, 2, 2, 2, 2, 2, 2, 2, 2, 2, 2, 4 ),
 ( 3, 3 ),
 ( 0.000000000000000000, 0.0003810285474897536721, 0.0007620570949795073441, 0.001143085642469261016, 0.001333599916214137961, 0.001524114189959014688, 0.001905142737448768360, 0.002286171284938522032, 0.003048228379918029377, 0.003429256927407782832, 0.003810285474897536721, 0.004572342569877044065, 0.005334399664856551843, 0.006096456759836058753 ),
 ( 0.000000000000000000, 1.000000000000000000 ),
 .UNSPECIFIED. ) 
 GEOMETRIC_REPRESENTATION_ITEM ( )  RATIONAL_B_SPLINE_SURFACE ( (
 ( 1.000000000000000000, 0.6693962893781428836, 1.000000000000000000),
 ( 1.000000000000000000, 0.6693969518177473876, 1.000000000000000000),
 ( 1.000000000000000000, 0.6717808526532893509, 1.000000000000000000),
 ( 1.000000000000000000, 0.6807237459914237121, 1.000000000000000000),
 ( 1.000000000000000000, 0.6873971151302553650, 1.000000000000000000),
 ( 1.000000000000000000, 0.7036635658348195932, 1.000000000000000000),
 ( 1.000000000000000000, 0.7132100160774622610, 1.000000000000000000),
 ( 1.000000000000000000, 0.7289110705425655423, 1.000000000000000000),
 ( 1.000000000000000000, 0.7344009482827760227, 1.000000000000000000),
 ( 1.000000000000000000, 0.7455531118719149752, 1.000000000000000000),
 ( 1.000000000000000000, 0.7512296405307345992, 1.000000000000000000),
 ( 1.000000000000000000, 0.7684203367994919542, 1.000000000000000000),
 ( 1.000000000000000000, 0.7800900503501072558, 1.000000000000000000),
 ( 1.000000000000000000, 0.8032919924401181744, 1.000000000000000000),
 ( 1.000000000000000000, 0.8148697721608513245, 1.000000000000000000),
 ( 1.000000000000000000, 0.8479710425742933433, 1.000000000000000000),
 ( 1.000000000000000000, 0.8681360573711495165, 1.000000000000000000),
 ( 1.000000000000000000, 0.8947228763049550615, 1.000000000000000000),
 ( 1.000000000000000000, 0.9030109035537770001, 1.000000000000000000),
 ( 1.000000000000000000, 0.9180946610702154231, 1.000000000000000000),
 ( 1.000000000000000000, 0.9249162233022707458, 1.000000000000000000),
 ( 1.000000000000000000, 0.9433494181431361092, 1.000000000000000000),
 ( 1.000000000000000000, 0.9529202612203482303, 1.000000000000000000),
 ( 1.000000000000000000, 0.9675496472389664149, 1.000000000000000000),
 ( 1.000000000000000000, 0.9726176721090025179, 1.000000000000000000),
 ( 1.000000000000000000, 0.9792068586059596846, 1.000000000000000000),
 ( 1.000000000000000000, 0.9807988706699215520, 1.000000000000000000),
 ( 1.000000000000000000, 0.9810773865977512331, 1.000000000000000000) ) ) 
 REPRESENTATION_ITEM ( '' )  SURFACE ( )  );
#2500=CARTESIAN_POINT ( 'NONE',  ( -63.69159315069311589, 15.00000000000000711, -164.7787203862777119 ) ) ;
#2504=CARTESIAN_POINT ( 'NONE',  ( -17.32624372123753886, 15.00000000000000000, -134.3796757791585037 ) ) ;
#2509=CARTESIAN_POINT ( 'NONE',  ( -0.8180164960865539125, 15.00000000000000355, -108.7420331879183806 ) ) ;
#2512=ORIENTED_EDGE ( 'NONE', *, *, #11115, .T. ) ;
#2524=CARTESIAN_POINT ( 'NONE',  ( -48.29558554489104694, 10.00000000000000000, -163.1462384615805661 ) ) ;
#2526=SHAPE_DEFINITION_REPRESENTATION ( #15114, #12380 ) ;
#2534=CARTESIAN_POINT ( 'NONE',  ( -63.21788648181868098, 10.23658426860817450, -203.5961373993322070 ) ) ;
#2546=CARTESIAN_POINT ( 'NONE',  ( -69.52160476852847637, 9.999999999999998224, -184.5417721423968658 ) ) ;
#2549=EDGE_LOOP ( 'NONE', ( #8450, #13961, #14833, #1818 ) ) ;
#2550=CARTESIAN_POINT ( 'NONE',  ( -5.893421222750781396, 15.00000000000000000, -117.5694263798266235 ) ) ;
#2551=CARTESIAN_POINT ( 'NONE',  ( 3.602241438175835864, 14.80771583330521501, -0.3334354230429009136 ) ) ;
#2552=CARTESIAN_POINT ( 'NONE',  ( 2.222606327615985311, 15.00000000000000000, -129.3650357597884977 ) ) ;
#2556=CARTESIAN_POINT ( 'NONE',  ( -4.098362961180376907, 10.53209361196889660, -46.33236032746155075 ) ) ;
#2559=CARTESIAN_POINT ( 'NONE',  ( 1.983632224063564431, 13.89821908686047180, 3.968066076948724596 ) ) ;
#2560=CIRCLE ( 'NONE', #12671, 9.800000000000252953 ) ;
#2566=CARTESIAN_POINT ( 'NONE',  ( -64.07033394082162658, 14.99612073371410226, -182.3557358624200333 ) ) ;
#2567=ORIENTED_EDGE ( 'NONE', *, *, #10264, .F. ) ;
#2569=ORIENTED_EDGE ( 'NONE', *, *, #1020, .F. ) ;
#2570=CARTESIAN_POINT ( 'NONE',  ( -5.948205887597929120, 4.336808689942017736E-16, -109.2829347068713588 ) ) ;
#2579=CARTESIAN_POINT ( 'NONE',  ( -70.08092325099204345, 15.00000000000000000, -193.7014402726163098 ) ) ;
#2588=ORIENTED_EDGE ( 'NONE', *, *, #9905, .F. ) ;
#2597=( BOUNDED_CURVE ( )  B_SPLINE_CURVE ( 3, ( #5527, #13802, #1974, #13960 ),
 .UNSPECIFIED., .F., .F. ) 
 B_SPLINE_CURVE_WITH_KNOTS ( ( 4, 4 ),
 ( 1.375929886000936797, 1.570796326794898112 ),
 .UNSPECIFIED. ) 
 CURVE ( )  GEOMETRIC_REPRESENTATION_ITEM ( )  RATIONAL_B_SPLINE_CURVE ( ( 1.000000000000000000, 0.9968380917696022525, 0.9968380917696022525, 1.000000000000000000 ) ) 
 REPRESENTATION_ITEM ( '' )  );
#2599=CARTESIAN_POINT ( 'NONE',  ( -9.552951302357074681, 2.499999999999999556, -124.0972072810879041 ) ) ;
#2600=CARTESIAN_POINT ( 'NONE',  ( -61.91367734689292490, 10.00000000000000355, -193.6436493912471803 ) ) ;
#2601=CARTESIAN_POINT ( 'NONE',  ( -66.44604053271804389, 10.00000000000000000, -157.9117883361228394 ) ) ;
#2610=CARTESIAN_POINT ( 'NONE',  ( -64.14881251011775021, 13.49284722309304030, -210.1482316909753365 ) ) ;
#2615=CARTESIAN_POINT ( 'NONE',  ( -26.78870578381917866, 15.00000000000000000, -139.1599602021251769 ) ) ;
#2617=ORIENTED_EDGE ( 'NONE', *, *, #6065, .F. ) ;
#2620=CARTESIAN_POINT ( 'NONE',  ( -8.243994158936985173, 15.00000000000000000, -104.7509493499769917 ) ) ;
#2622=EDGE_CURVE ( 'NONE', #7022, #7777, #3594, .T. ) ;
#2624=CARTESIAN_POINT ( 'NONE',  ( -5.365035937023899137, 9.999999999999998224, -111.0566899280839834 ) ) ;
#2625=EDGE_CURVE ( 'NONE', #6350, #9880, #14611, .T. ) ;
#2629=DIRECTION ( 'NONE',  ( 0.000000000000000000, -1.000000000000000000, 0.000000000000000000 ) ) ;
#2632=CARTESIAN_POINT ( 'NONE',  ( -4.222954148114340889, 9.650666666666662508, -47.83347973032346090 ) ) ;
#2634=CARTESIAN_POINT ( 'NONE',  ( 3.422362696586258579, 11.71486000144306416, 4.863683519685648271 ) ) ;
#2636=CARTESIAN_POINT ( 'NONE',  ( -7.260202548253541721, 0.06312176567927152426, -104.4756693458776482 ) ) ;
#2641=AXIS2_PLACEMENT_3D ( 'NONE', #5355, #13492, #5210 ) ;
#2642=ORIENTED_EDGE ( 'NONE', *, *, #14826, .F. ) ;
#2646=CARTESIAN_POINT ( 'NONE',  ( -5.462587733769669107, 2.500000000000000444, -110.6302725851820128 ) ) ;
#2650=CARTESIAN_POINT ( 'NONE',  ( -18.09353981420494151, 2.500000000000000444, -129.3374956033359240 ) ) ;
#2651=VERTEX_POINT ( 'NONE', #13641 ) ;
#2656=CIRCLE ( 'NONE', #13277, 8.000000000000007105 ) ;
#2657=CARTESIAN_POINT ( 'NONE',  ( -64.42669704464265124, 15.00000000000000000, -184.3342360300873679 ) ) ;
#2664=CARTESIAN_POINT ( 'NONE',  ( -3.647146582612662336, 14.99999999999999645, -103.6739734567058662 ) ) ;
#2675=CARTESIAN_POINT ( 'NONE',  ( -6.848205146710602875, 0.003927834388024460492, -104.1625534234818673 ) ) ;
#2676=CARTESIAN_POINT ( 'NONE',  ( -42.38382697495404017, 9.999999999999996447, -158.4544082798614397 ) ) ;
#2678=CARTESIAN_POINT ( 'NONE',  ( -58.06539719015423628, 14.99999999999999822, -167.9715705546709614 ) ) ;
#2687=CARTESIAN_POINT ( 'NONE',  ( -63.68606942785788760, 12.31334483161724336, -202.4826902647699001 ) ) ;
#2693=CARTESIAN_POINT ( 'NONE',  ( 6.089666224640344794, 0.000000000000000000, -124.6062682140657074 ) ) ;
#2694=DIRECTION ( 'NONE',  ( -0.9961255586397056438, -0.000000000000000000, 0.08794243244722427244 ) ) ;
#2695=VERTEX_POINT ( 'NONE', #14811 ) ;
#2698=CARTESIAN_POINT ( 'NONE',  ( -69.01969303127702915, 10.00000000000000000, -181.6796560542968848 ) ) ;
#2701=CARTESIAN_POINT ( 'NONE',  ( -4.773065440008094740, 15.00000000000000000, -102.4756705383327073 ) ) ;
#2702=DIRECTION ( 'NONE',  ( -1.000000000000000000, -0.000000000000000000, -0.000000000000000000 ) ) ;
#2707=CARTESIAN_POINT ( 'NONE',  ( -3.837140252011802311, 11.25564743829991343, -45.28537430115928686 ) ) ;
#2709=CARTESIAN_POINT ( 'NONE',  ( 2.569439577807433928, 14.37659876732869257, 3.184003491651386408 ) ) ;
#2711=EDGE_CURVE ( 'NONE', #2289, #5560, #9403, .T. ) ;
#2712=EDGE_CURVE ( 'NONE', #15113, #5809, #26, .T. ) ;
#2715=LINE ( 'NONE', #3877, #9488 ) ;
#2721=VERTEX_POINT ( 'NONE', #12311 ) ;
#2722=CARTESIAN_POINT ( 'NONE',  ( -5.145745206871998434, 2.500000000000000444, -112.5500021907323713 ) ) ;
#2731=CARTESIAN_POINT ( 'NONE',  ( -63.65634297892059124, 15.00000000000000000, -180.4413320423983293 ) ) ;
#2733=DIRECTION ( 'NONE',  ( -0.9961255586397049777, -0.000000000000000000, 0.08794243244723005948 ) ) ;
#2734=CIRCLE ( 'NONE', #2986, 5.000000000000004441 ) ;
#2743=VERTEX_POINT ( 'NONE', #6522 ) ;
#2744=CARTESIAN_POINT ( 'NONE',  ( 6.089666224640341241, 9.999999999999998224, -124.6062682140657074 ) ) ;
#2745=CARTESIAN_POINT ( 'NONE',  ( -17.32624372123753886, 2.500000000000000444, -129.3796757791584753 ) ) ;
#2747=ORIENTED_EDGE ( 'NONE', *, *, #15104, .F. ) ;
#2759=CARTESIAN_POINT ( 'NONE',  ( -49.14320000630262086, 10.00000000000000178, -164.0715453079124870 ) ) ;
#2760=CARTESIAN_POINT ( 'NONE',  ( -59.60145741454977752, 14.99999999999999645, -170.6931484237352379 ) ) ;
#2762=CIRCLE ( 'NONE', #2498, 1.000000000000000888 ) ;
#2766=DIRECTION ( 'NONE',  ( 0.000000000000000000, 0.000000000000000000, -1.000000000000000000 ) ) ;
#2769=CARTESIAN_POINT ( 'NONE',  ( -63.24804750230908468, 10.63074368444023676, -203.5304119779587211 ) ) ;
#2773=CARTESIAN_POINT ( 'NONE',  ( -67.63291399244498336, 12.29434701114028705, -203.1533042379604979 ) ) ;
#2779=CARTESIAN_POINT ( 'NONE',  ( -9.240119717576689595, 2.500000000000000444, -104.6630069175297564 ) ) ;
#2783=DIRECTION ( 'NONE',  ( -0.08794243244722428632, -0.000000000000000000, -0.9961255586397056438 ) ) ;
#2790=CARTESIAN_POINT ( 'NONE',  ( -3.330734844456505694, 10.45935787353785074, -44.51265823977242775 ) ) ;
#2792=CARTESIAN_POINT ( 'NONE',  ( 3.568580374889821272, 12.24296972320970944, 4.586805082927478239 ) ) ;
#2794=VECTOR ( 'NONE', #57, 1000.000000000000227 ) ;
#2796=CARTESIAN_POINT ( 'NONE',  ( -76.20282042307043469, 5.000000000000000000, -188.4633497277648928 ) ) ;
#2801=VERTEX_POINT ( 'NONE', #12244 ) ;
#2802=DIRECTION ( 'NONE',  ( -0.08794243244722413366, 0.000000000000000000, -0.9961255586397056438 ) ) ;
#2807=VERTEX_POINT ( 'NONE', #13421 ) ;
#2814=CARTESIAN_POINT ( 'NONE',  ( -70.02757949906018098, 9.999999999999998224, -189.2441461653057218 ) ) ;
#2815=CARTESIAN_POINT ( 'NONE',  ( -3.806220192786536671, 7.379999999999995453, -48.79866403991030666 ) ) ;
#2834=DIRECTION ( 'NONE',  ( 0.6527336816407247611, 0.000000000000000000, -0.7575874476598360996 ) ) ;
#2840=DIRECTION ( 'NONE',  ( 0.9961255586397056438, 0.000000000000000000, -0.08794243244722427244 ) ) ;
#2849=DIRECTION ( 'NONE',  ( -0.000000000000000000, -1.000000000000000000, -0.000000000000000000 ) ) ;
#2851=CARTESIAN_POINT ( 'NONE',  ( 7.740440778602579286, 4.463770477647834412, -20.78498225277660083 ) ) ;
#2855=CARTESIAN_POINT ( 'NONE',  ( -67.60484011711940866, 11.30829572562506335, -204.1139660933697257 ) ) ;
#2862=CARTESIAN_POINT ( 'NONE',  ( -2.573490212646732278, 7.321094445766561876, -29.14997122992682321 ) ) ;
#2864=CARTESIAN_POINT ( 'NONE',  ( -10.46704385831657902, 4.336808689942017736E-16, -128.9524512386204549 ) ) ;
#2869=CARTESIAN_POINT ( 'NONE',  ( 0.2343396196498212236, 3.734791725217455394, 2.654369205397980380 ) ) ;
#2871=CARTESIAN_POINT ( 'NONE',  ( -6.683304552674626642, 0.000000000000000000, -104.1296019027811894 ) ) ;
#2878=ORIENTED_EDGE ( 'NONE', *, *, #13294, .F. ) ;
#2896=VERTEX_POINT ( 'NONE', #2745 ) ;
#2898=DIRECTION ( 'NONE',  ( 0.9026204165532970558, 0.000000000000000000, 0.4304374328763155289 ) ) ;
#2905=CARTESIAN_POINT ( 'NONE',  ( -6.530393906344411192, 14.42323828349428361, -104.0689525186695477 ) ) ;
#2910=DIRECTION ( 'NONE',  ( 0.08794243244722392550, 0.000000000000000000, 0.9961255586397055328 ) ) ;
#2913=EDGE_CURVE ( 'NONE', #2651, #5826, #4357, .T. ) ;
#2920=CARTESIAN_POINT ( 'NONE',  ( -25.68053481550299111, 5.000000000000000888, -142.4798935003980773 ) ) ;
#2921=CARTESIAN_POINT ( 'NONE',  ( 3.087044391538636745, 1.679853004339140421, 3.965071156515985518 ) ) ;
#2924=CARTESIAN_POINT ( 'NONE',  ( -67.56452796570999908, 13.67829370444025372, -200.1615161516820365 ) ) ;
#2932=CARTESIAN_POINT ( 'NONE',  ( -3.816819072638210297, 15.00000000000000000, -103.4918378357580053 ) ) ;
#2933=DIRECTION ( 'NONE',  ( -0.000000000000000000, -1.000000000000000000, -0.000000000000000000 ) ) ;
#2942=DIRECTION ( 'NONE',  ( 0.08794243244723000397, 0.000000000000000000, 0.9961255586397049777 ) ) ;
#2946=CARTESIAN_POINT ( 'NONE',  ( -44.50300032310534704, 15.00000000000000000, -159.8141794072773223 ) ) ;
#2952=DIRECTION ( 'NONE',  ( 0.000000000000000000, 1.000000000000000000, 0.000000000000000000 ) ) ;
#2963=AXIS2_PLACEMENT_3D ( 'NONE', #7976, #807, #5508 ) ;
#2964=CARTESIAN_POINT ( 'NONE',  ( -16.94138229547579400, 5.000000000000000888, -154.2864167784019287 ) ) ;
#2977=ADVANCED_FACE ( 'NONE', ( #3185 ), #2095, .F. ) ;
#2985=ORIENTED_EDGE ( 'NONE', *, *, #1841, .T. ) ;
#2986=AXIS2_PLACEMENT_3D ( 'NONE', #7808, #2089, #5490 ) ;
#2993=EDGE_CURVE ( 'NONE', #6034, #4876, #1378, .T. ) ;
#2996=B_SPLINE_CURVE_WITH_KNOTS ( 'NONE', 3,
 ( #13858, #3110, #7968, #6740, #10224, #5726, #11453, #11376, #4277, #9284, #7821, #800, #5576, #3256, #14008, #5502, #2105, #3406, #8116, #5947 ),
 .UNSPECIFIED., .F., .F.,
 ( 4, 2, 2, 2, 2, 2, 2, 2, 2, 4 ),
 ( -1.586050209718467129E-05, 0.001006126488465763913, 0.002028113479028712755, 0.003050100469591661596, 0.004072087460154610004, 0.005094074450717559280, 0.005605067945999035219, 0.006116061441280511157, 0.007138048431843450892, 0.008160035422406390626 ),
 .UNSPECIFIED. ) ;
#2998=CARTESIAN_POINT ( 'NONE',  ( 7.190027994173562753, 5.321094445766561876, -30.38850508759179192 ) ) ;
#2999=CARTESIAN_POINT ( 'NONE',  ( 0.1841197429283822073, 0.1140767794773729221, 2.085527733063581746 ) ) ;
#3003=CARTESIAN_POINT ( 'NONE',  ( -1.078957824791472619, 8.673617379884037444E-16, -133.0846919315902142 ) ) ;
#3006=CARTESIAN_POINT ( 'NONE',  ( -67.58382170693636226, 10.00000000000000000, -204.5178482451963191 ) ) ;
#3011=DIRECTION ( 'NONE',  ( 0.9982196940171963462, 0.000000000000000000, -0.05964429961207242531 ) ) ;
#3021=DIRECTION ( 'NONE',  ( 0.9961255586397049777, 0.000000000000000000, -0.08794243244723005948 ) ) ;
#3025=CARTESIAN_POINT ( 'NONE',  ( -31.41915002255961298, 15.00000000000000000, -151.2642837462047964 ) ) ;
#3027=ORIENTED_EDGE ( 'NONE', *, *, #916, .T. ) ;
#3028=CYLINDRICAL_SURFACE ( 'NONE', #1060, 3.000000000000010214 ) ;
#3030=CARTESIAN_POINT ( 'NONE',  ( -3.517695908037311803, 10.45879132743789341, -46.62865316603851085 ) ) ;
#3036=CARTESIAN_POINT ( 'NONE',  ( -62.99132485747528420, 15.00000000000000000, -202.4853500613857307 ) ) ;
#3042=CARTESIAN_POINT ( 'NONE',  ( 6.363274845736492935, 5.000000000000000888, -132.2089327231056473 ) ) ;
#3048=AXIS2_PLACEMENT_3D ( 'NONE', #6073, #14206, #3453 ) ;
#3066=ORIENTED_EDGE ( 'NONE', *, *, #13094, .F. ) ;
#3069=CARTESIAN_POINT ( 'NONE',  ( 7.262177415846634787, 3.361685231369096805, -24.56097010744011300 ) ) ;
#3070=CARTESIAN_POINT ( 'NONE',  ( 0.06817676530921484845, -0.03742728397158888443, 0.7722394814505989524 ) ) ;
#3074=AXIS2_PLACEMENT_3D ( 'NONE', #12181, #1746, #14521 ) ;
#3077=EDGE_CURVE ( 'NONE', #10989, #11588, #8048, .T. ) ;
#3078=CARTESIAN_POINT ( 'NONE',  ( -30.41959608467592702, 15.00000000000000355, -151.3633174574383418 ) ) ;
#3081=DIRECTION ( 'NONE',  ( 0.000000000000000000, 0.000000000000000000, -1.000000000000000000 ) ) ;
#3092=ADVANCED_FACE ( 'NONE', ( #12776 ), #12621, .T. ) ;
#3094=DIRECTION ( 'NONE',  ( -0.9961255586397050887, 0.000000000000000000, 0.08794243244723005948 ) ) ;
#3096=FACE_OUTER_BOUND ( 'NONE', #9098, .T. ) ;
#3099=ORIENTED_EDGE ( 'NONE', *, *, #12258, .T. ) ;
#3100=CARTESIAN_POINT ( 'NONE',  ( -11.40820045174505992, 9.999999999999998224, -126.3212311505415784 ) ) ;
#3101=DIRECTION ( 'NONE',  ( 0.000000000000000000, 0.000000000000000000, -1.000000000000000000 ) ) ;
#3109=CARTESIAN_POINT ( 'NONE',  ( -68.68211634358988249, 15.00000000000000000, -201.9941738958162603 ) ) ;
#3110=CARTESIAN_POINT ( 'NONE',  ( -4.403991534456141999, 15.00000000000000178, -103.3272078610332301 ) ) ;
#3115=CARTESIAN_POINT ( 'NONE',  ( 3.201254193339545751, 3.381110835560071859, 4.950899197493613180 ) ) ;
#3116=CARTESIAN_POINT ( 'NONE',  ( -12.27209645382209402, 2.500000000000000444, -127.2227734861304782 ) ) ;
#3117=VERTEX_POINT ( 'NONE', #15188 ) ;
#3118=CYLINDRICAL_SURFACE ( 'NONE', #9552, 2.326940983401415419 ) ;
#3127=CARTESIAN_POINT ( 'NONE',  ( -9.055672782877035587, 11.36792136377893492, -104.6047652700399198 ) ) ;
#3149=CARTESIAN_POINT ( 'NONE',  ( -8.645680077725348411, 2.500000000000000444, -122.8677831016847790 ) ) ;
#3152=EDGE_CURVE ( 'NONE', #9480, #333, #248, .T. ) ;
#3160=ORIENTED_EDGE ( 'NONE', *, *, #12337, .F. ) ;
#3163=CARTESIAN_POINT ( 'NONE',  ( -54.08656694241062013, 15.00000000000000000, -162.1624640010098517 ) ) ;
#3166=CARTESIAN_POINT ( 'NONE',  ( 9.939878312292620421, 9.999999999999998224, -115.2320631035898373 ) ) ;
#3168=( BOUNDED_SURFACE ( )  B_SPLINE_SURFACE ( 3, 1, ( 
 ( #9018, #10027 ),
 ( #6466, #9873 ),
 ( #6547, #8942 ),
 ( #6626, #4009 ) ),
 .UNSPECIFIED., .F., .F., .T. ) 
 B_SPLINE_SURFACE_WITH_KNOTS ( ( 4, 4 ),
 ( 2, 2 ),
 ( 0.000000000000000000, 1.000000000000000000 ),
 ( 0.000000000000000000, 1.000000000000000000 ),
 .UNSPECIFIED. ) 
 GEOMETRIC_REPRESENTATION_ITEM ( )  RATIONAL_B_SPLINE_SURFACE ( (
 ( 1.000000000000000000, 1.000000000000000000),
 ( 0.8388501503673406745, 0.8388501503673406745),
 ( 0.8388501503673406745, 0.8388501503673406745),
 ( 1.000000000000000000, 1.000000000000000000) ) ) 
 REPRESENTATION_ITEM ( '' )  SURFACE ( )  );
#3169=CARTESIAN_POINT ( 'NONE',  ( -1.843872751574030300, 15.00000000000000000, -133.9216539038831399 ) ) ;
#3173=EDGE_CURVE ( 'NONE', #2695, #9540, #5777, .T. ) ;
#3177=CARTESIAN_POINT ( 'NONE',  ( -69.06832266532519782, 9.999999999999998224, -200.7467498273179274 ) ) ;
#3181=CARTESIAN_POINT ( 'NONE',  ( -8.105036670657762343, 10.00000000000000178, -106.2142721819313920 ) ) ;
#3182=CARTESIAN_POINT ( 'NONE',  ( 4.548248957081511001, 14.25778345964358529, 2.149752393844249543 ) ) ;
#3184=CARTESIAN_POINT ( 'NONE',  ( 10.01939027896081313, 5.000000000000000888, -127.6977514918621637 ) ) ;
#3185=FACE_OUTER_BOUND ( 'NONE', #6854, .T. ) ;
#3187=ORIENTED_EDGE ( 'NONE', *, *, #979, .T. ) ;
#3192=ORIENTED_EDGE ( 'NONE', *, *, #9515, .T. ) ;
#3197=CARTESIAN_POINT ( 'NONE',  ( -9.240119717576694924, 9.999999999999998224, -104.6630069175297564 ) ) ;
#3199=CIRCLE ( 'NONE', #5186, 3.500000000000003109 ) ;
#3206=ORIENTED_EDGE ( 'NONE', *, *, #1022, .T. ) ;
#3223=AXIS2_PLACEMENT_3D ( 'NONE', #8482, #11878, #9563 ) ;
#3226=DIRECTION ( 'NONE',  ( 0.000000000000000000, -1.000000000000000000, 0.000000000000000000 ) ) ;
#3227=VECTOR ( 'NONE', #10584, 1000.000000000000000 ) ;
#3228=VECTOR ( 'NONE', #266, 1000.000000000000227 ) ;
#3235=CARTESIAN_POINT ( 'NONE',  ( -4.125453648579471277, 4.336808689942017736E-16, -107.3641501471127526 ) ) ;
#3237=DIRECTION ( 'NONE',  ( 0.05964429961207245307, 0.000000000000000000, 0.9982196940171964572 ) ) ;
#3239=ORIENTED_EDGE ( 'NONE', *, *, #4488, .F. ) ;
#3242=CARTESIAN_POINT ( 'NONE',  ( -43.80089141906720585, 15.00000000000000000, -153.5888841403339597 ) ) ;
#3243=ADVANCED_FACE ( 'NONE', ( #1327 ), #10359, .F. ) ;
#3246=CARTESIAN_POINT ( 'NONE',  ( -12.27209645382210113, 9.999999999999998224, -127.2227734861304782 ) ) ;
#3247=DIRECTION ( 'NONE',  ( 0.003262051938530752433, 0.000000000000000000, 0.9999946794944213346 ) ) ;
#3256=CARTESIAN_POINT ( 'NONE',  ( -8.375425654315606039, 12.27215496146240703, -105.2394517302402619 ) ) ;
#3261=CARTESIAN_POINT ( 'NONE',  ( 3.000122744334918767, 1.017992234156722242, 3.255451705640021842 ) ) ;
#3265=ADVANCED_FACE ( 'NONE', ( #6030 ), #13157, .T. ) ;
#3270=ADVANCED_FACE ( 'NONE', ( #3492 ), #12055, .T. ) ;
#3272=ORIENTED_EDGE ( 'NONE', *, *, #916, .F. ) ;
#3275=CARTESIAN_POINT ( 'NONE',  ( -9.201659748534703809, 10.69856349024409425, -104.6507959483510604 ) ) ;
#3289=DIRECTION ( 'NONE',  ( 0.000000000000000000, -1.000000000000000000, 0.000000000000000000 ) ) ;
#3296=CARTESIAN_POINT ( 'NONE',  ( -1.528156170053301510, 7.379999999999995453, -45.73714083922575213 ) ) ;
#3305=ORIENTED_EDGE ( 'NONE', *, *, #4143, .T. ) ;
#3306=VECTOR ( 'NONE', #13533, 1000.000000000000227 ) ;
#3313=CARTESIAN_POINT ( 'NONE',  ( -4.238957102262124188, -1.739993903204167602E-15, -137.2930163777632799 ) ) ;
#3316=CARTESIAN_POINT ( 'NONE',  ( -2.613481103162547114, 4.336808689942018722E-16, -113.0003292951173535 ) ) ;
#3318=DIRECTION ( 'NONE',  ( -0.06144244613645849507, 0.7154473348115049092, -0.6959597236362767836 ) ) ;
#3319=ORIENTED_EDGE ( 'NONE', *, *, #3760, .F. ) ;
#3322=CARTESIAN_POINT ( 'NONE',  ( -57.59976990480181058, 15.00000000000000000, -167.2044102620146759 ) ) ;
#3324=EDGE_LOOP ( 'NONE', ( #11552, #2018, #14248, #8449 ) ) ;
#3326=VECTOR ( 'NONE', #9516, 1000.000000000000000 ) ;
#3333=CIRCLE ( 'NONE', #125, 5.000000000000001776 ) ;
#3336=CARTESIAN_POINT ( 'NONE',  ( -6.351131181362492661, 10.00000000000000533, -118.7647174387982290 ) ) ;
#3339=DIRECTION ( 'NONE',  ( 0.000000000000000000, 0.000000000000000000, -1.000000000000000000 ) ) ;
#3346=CARTESIAN_POINT ( 'NONE',  ( 9.939878312292623974, 9.999999999999998224, -115.2320631035898373 ) ) ;
#3350=CARTESIAN_POINT ( 'NONE',  ( -57.71664061942946233, 15.00000000000000000, -153.6990377947844593 ) ) ;
#3351=CARTESIAN_POINT ( 'NONE',  ( -14.50484797826036321, 7.499999999999991118, -90.38469341974051474 ) ) ;
#3355=FACE_OUTER_BOUND ( 'NONE', #14290, .T. ) ;
#3357=ORIENTED_EDGE ( 'NONE', *, *, #7611, .T. ) ;
#3366=ORIENTED_EDGE ( 'NONE', *, *, #4696, .F. ) ;
#3375=CARTESIAN_POINT ( 'NONE',  ( -44.21823081166466096, 15.00000000000000000, -145.3603131190973272 ) ) ;
#3377=ORIENTED_EDGE ( 'NONE', *, *, #7503, .T. ) ;
#3382=CARTESIAN_POINT ( 'NONE',  ( -29.69515346086422980, 5.000000000000000000, -156.7390981038715836 ) ) ;
#3383=CARTESIAN_POINT ( 'NONE',  ( -65.55349497823009131, 14.94604455468336468, -187.0977264243838647 ) ) ;
#3386=CARTESIAN_POINT ( 'NONE',  ( -4.090890948359609425, 15.00000000000000000, -103.1929727064838289 ) ) ;
#3387=EDGE_CURVE ( 'NONE', #3600, #882, #2597, .T. ) ;
#3395=CARTESIAN_POINT ( 'NONE',  ( -66.60702730184040377, 15.00000000000000000, -191.5456185926130956 ) ) ;
#3398=CARTESIAN_POINT ( 'NONE',  ( 4.011956498685772310, 5.000000000000001776, -134.9775950754472831 ) ) ;
#3399=CARTESIAN_POINT ( 'NONE',  ( 2.850044070969222521, 5.000000000000000888, -103.0233998225063345 ) ) ;
#3406=CARTESIAN_POINT ( 'NONE',  ( -8.853589897535512065, 10.68297945906494029, -105.4984887282087982 ) ) ;
#3407=DIRECTION ( 'NONE',  ( 0.000000000000000000, 0.000000000000000000, -1.000000000000000000 ) ) ;
#3408=CARTESIAN_POINT ( 'NONE',  ( -2.238468823239509131, 7.379999999999995453, -42.41179034119947744 ) ) ;
#3410=CARTESIAN_POINT ( 'NONE',  ( -6.619426566176021431, 14.36547257068670724, -103.8764596943030654 ) ) ;
#3411=DIRECTION ( 'NONE',  ( 0.000000000000000000, 0.000000000000000000, -1.000000000000000000 ) ) ;
#3412=ORIENTED_EDGE ( 'NONE', *, *, #10907, .F. ) ;
#3417=CARTESIAN_POINT ( 'NONE',  ( 4.586790536108142469, 15.00000000000000000, -116.5616331786029036 ) ) ;
#3420=CARTESIAN_POINT ( 'NONE',  ( -52.65879960150161310, 15.00000000000000000, -146.8206079635090191 ) ) ;
#3426=DIRECTION ( 'NONE',  ( 0.000000000000000000, 0.000000000000000000, -1.000000000000000000 ) ) ;
#3428=CARTESIAN_POINT ( 'NONE',  ( -4.567589802617025185, 14.99999999999999822, -125.7656343796584082 ) ) ;
#3437=ORIENTED_EDGE ( 'NONE', *, *, #1294, .F. ) ;
#3438=ADVANCED_FACE ( 'NONE', ( #743 ), #6904, .F. ) ;
#3443=CARTESIAN_POINT ( 'NONE',  ( -17.32624372123753886, 15.00000000000000000, -122.3796757791585321 ) ) ;
#3449=ORIENTED_EDGE ( 'NONE', *, *, #6759, .T. ) ;
#3450=VECTOR ( 'NONE', #10927, 1000.000000000000000 ) ;
#3452=EDGE_CURVE ( 'NONE', #14745, #5270, #12839, .T. ) ;
#3453=DIRECTION ( 'NONE',  ( 0.08794243244723005948, 0.000000000000000000, 0.9961255586397049777 ) ) ;
#3458=CARTESIAN_POINT ( 'NONE',  ( -65.84020878422680312, 15.11604966749248646, -201.7286952349428475 ) ) ;
#3461=CIRCLE ( 'NONE', #14854, 3.500000000000013323 ) ;
#3462=PLANE ( 'NONE',  #10696 ) ;
#3470=CARTESIAN_POINT ( 'NONE',  ( -53.33476332437127354, 15.00000000000000000, -169.8150382216088587 ) ) ;
#3471=CIRCLE ( 'NONE', #2481, 3.000000000000010214 ) ;
#3474=CARTESIAN_POINT ( 'NONE',  ( -5.808150136414201192, 9.999999999999998224, -117.3161822536842607 ) ) ;
#3475=AXIS2_PLACEMENT_3D ( 'NONE', #4863, #2629, #7331 ) ;
#3477=ADVANCED_FACE ( 'NONE', ( #6765 ), #7995, .T. ) ;
#3484=AXIS2_PLACEMENT_3D ( 'NONE', #14211, #12898, #4699 ) ;
#3486=( BOUNDED_CURVE ( )  B_SPLINE_CURVE ( 3, ( #141, #2383, #10571, #7080 ),
 .UNSPECIFIED., .F., .T. ) 
 B_SPLINE_CURVE_WITH_KNOTS ( ( 4, 4 ),
 ( 4.712388980384687898, 4.907255421178649435 ),
 .UNSPECIFIED. ) 
 CURVE ( )  GEOMETRIC_REPRESENTATION_ITEM ( )  RATIONAL_B_SPLINE_CURVE ( ( 1.000000000000000000, 0.9968380917696022525, 0.9968380917696022525, 1.000000000000000000 ) ) 
 REPRESENTATION_ITEM ( '' )  );
#3487=DIRECTION ( 'NONE',  ( 0.000000000000000000, -1.000000000000000000, 0.000000000000000000 ) ) ;
#3488=CARTESIAN_POINT ( 'NONE',  ( 4.010609318860100636, 13.34515119446107612, 3.652314080085856229 ) ) ;
#3491=CARTESIAN_POINT ( 'NONE',  ( -9.203293576667494591, 10.68436263327555835, -104.6513152614200237 ) ) ;
#3492=FACE_OUTER_BOUND ( 'NONE', #2184, .T. ) ;
#3493=VERTEX_POINT ( 'NONE', #2424 ) ;
#3494=( BOUNDED_CURVE ( )  B_SPLINE_CURVE ( 3, ( #11308, #13719, #8915, #13566 ),
 .UNSPECIFIED., .F., .F. ) 
 B_SPLINE_CURVE_WITH_KNOTS ( ( 4, 4 ),
 ( 5.855884514716120925, 5.964107263055466568 ),
 .UNSPECIFIED. ) 
 CURVE ( )  GEOMETRIC_REPRESENTATION_ITEM ( )  RATIONAL_B_SPLINE_CURVE ( ( 1.000000000000000000, 0.9990242245225531281, 0.9990242245225531281, 1.000000000000000000 ) ) 
 REPRESENTATION_ITEM ( '' )  );
#3503=CARTESIAN_POINT ( 'NONE',  ( -56.93825309396395085, 15.00000000000456346, -152.5131710536675200 ) ) ;
#3509=PLANE ( 'NONE',  #6775 ) ;
#3511=VERTEX_POINT ( 'NONE', #7052 ) ;
#3516=CARTESIAN_POINT ( 'NONE',  ( -8.060080686208022982, 9.999999999999998224, -91.29668298688132211 ) ) ;
#3524=CIRCLE ( 'NONE', #4033, 3.000000000000002665 ) ;
#3529=ORIENTED_EDGE ( 'NONE', *, *, #6781, .T. ) ;
#3533=TOROIDAL_SURFACE ( 'NONE', #11192, 9.800000000000245848, 5.000000000000000000 ) ;
#3536=CARTESIAN_POINT ( 'NONE',  ( -64.63541926112564795, 14.99927084828137858, -184.1902271030175484 ) ) ;
#3537=CARTESIAN_POINT ( 'NONE',  ( -2.580341218501653433, 0.4558749503568839123, -137.7136442480489222 ) ) ;
#3539=CARTESIAN_POINT ( 'NONE',  ( -2.986019729822490643, 4.336808689942016750E-16, -116.5136792814622879 ) ) ;
#3541=EDGE_CURVE ( 'NONE', #7777, #114, #1501, .T. ) ;
#3542=CARTESIAN_POINT ( 'NONE',  ( 3.235167919141236137, 15.00000000000000000, -114.6791120453068373 ) ) ;
#3543=AXIS2_PLACEMENT_3D ( 'NONE', #8260, #2702, #7401 ) ;
#3544=CARTESIAN_POINT ( 'NONE',  ( -3.520407287333057855, 7.379999999999995453, -45.56125597433126018 ) ) ;
#3549=CARTESIAN_POINT ( 'NONE',  ( -7.316781067255146098, 0.05734158317339200367, -104.2569854988662570 ) ) ;
#3551=ORIENTED_EDGE ( 'NONE', *, *, #6202, .T. ) ;
#3552=CARTESIAN_POINT ( 'NONE',  ( -1.457387361610950727, 15.00000000000000000, -106.9488561393970940 ) ) ;
#3553=DIRECTION ( 'NONE',  ( -0.9961255586397056438, 0.000000000000000000, 0.08794243244722428632 ) ) ;
#3556=AXIS2_PLACEMENT_3D ( 'NONE', #4001, #598, #2910 ) ;
#3562=DIRECTION ( 'NONE',  ( -0.9961255586397055328, 0.000000000000000000, 0.08794243244722428632 ) ) ;
#3564=EDGE_CURVE ( 'NONE', #2807, #14091, #6212, .T. ) ;
#3565=EDGE_CURVE ( 'NONE', #14271, #8293, #9771, .T. ) ;
#3571=CARTESIAN_POINT ( 'NONE',  ( -4.421378549306751893, 14.99999999999999822, -103.2781497068736059 ) ) ;
#3572=CARTESIAN_POINT ( 'NONE',  ( -65.02458175624013847, 14.37806382103629588, -196.6750733491710719 ) ) ;
#3575=CARTESIAN_POINT ( 'NONE',  ( -5.763540231036513362, 2.500000000000000444, -109.7236846929843210 ) ) ;
#3581=VERTEX_POINT ( 'NONE', #991 ) ;
#3584=( BOUNDED_SURFACE ( )  B_SPLINE_SURFACE ( 3, 2, ( 
 ( #5884, #6896, #4817 ),
 ( #13015, #10386, #5816 ),
 ( #27, #2273, #7113 ),
 ( #1261, #10686, #15199 ),
 ( #11694, #3420, #4663 ),
 ( #9299, #8132, #104 ),
 ( #9530, #4517, #9369 ),
 ( #14101, #3503, #9224 ),
 ( #13953, #3350, #12786 ),
 ( #12234, #1340, #14328 ),
 ( #3894, #8593, #3732 ),
 ( #12154, #2500, #8355 ),
 ( #6044, #14570, #7436 ),
 ( #7515, #5204, #13328 ),
 ( #13083, #14496, #8438 ),
 ( #2731, #1490, #1571 ),
 ( #6205, #7195, #11915 ),
 ( #2657, #1417, #10762 ),
 ( #6122, #13252, #415 ),
 ( #10835, #3654, #6284 ),
 ( #12070, #9601, #2814 ),
 ( #9838, #11993, #10920 ),
 ( #11000, #13169, #1646 ),
 ( #489, #2579, #5123 ),
 ( #11072, #6360, #9918 ),
 ( #3970, #7279, #7357 ),
 ( #337, #8676, #5051 ),
 ( #9766, #13409, #179 ),
 ( #4889, #254, #4969 ),
 ( #9684, #14416, #3814 ),
 ( #8518, #7665, #3177 ),
 ( #11150, #4052, #10141 ),
 ( #13710, #3109, #12462 ),
 ( #12303, #12381, #13634 ),
 ( #7820, #8904, #1948 ),
 ( #6661, #14651, #1880 ),
 ( #11374, #12534, #799 ),
 ( #3036, #5501, #1802 ) ),
 .UNSPECIFIED., .F., .F., .F. ) 
 B_SPLINE_SURFACE_WITH_KNOTS ( ( 4, 2, 2, 2, 2, 2, 2, 2, 2, 2, 2, 2, 2, 2, 2, 2, 2, 2, 4 ),
 ( 3, 3 ),
 ( 0.08381559250741665856, 0.08776888376050354101, 0.09172217501359040959, 0.09567546626667727816, 0.09962875751976416061, 0.1075353400259379255, 0.1154419225321116765, 0.1233485050382854276, 0.1273017962913723100, 0.1312550875444591925, 0.1352083787975460749, 0.1371850244240895300, 0.1391616700506329574, 0.1411383156771763847, 0.1431149613037198121, 0.1441032841169915257, 0.1450916069302632394, 0.1460799297435349531, 0.1470682525568066945 ),
 ( 0.000000000000000000, 1.000000000000000000 ),
 .UNSPECIFIED. ) 
 GEOMETRIC_REPRESENTATION_ITEM ( )  RATIONAL_B_SPLINE_SURFACE ( (
 ( 1.000000000000000000, 0.7071067811865475727, 1.000000000000000000),
 ( 1.000000000000000000, 0.7071067811865475727, 1.000000000000000000),
 ( 1.000000000000000000, 0.7071067811865477948, 1.000000000000000000),
 ( 1.000000000000000000, 0.7071067811865477948, 1.000000000000000000),
 ( 1.000000000000000000, 0.7071067811865475727, 1.000000000000000000),
 ( 1.000000000000000000, 0.7071067811865475727, 1.000000000000000000),
 ( 1.000000000000000000, 0.7071067811865475727, 1.000000000000000000),
 ( 1.000000000000000000, 0.7071067811865475727, 1.000000000000000000),
 ( 1.000000000000000000, 0.7071067811865475727, 1.000000000000000000),
 ( 1.000000000000000000, 0.7071067811865475727, 1.000000000000000000),
 ( 1.000000000000000000, 0.7071067811865471286, 1.000000000000000000),
 ( 1.000000000000000000, 0.7071067811865471286, 1.000000000000000000),
 ( 1.000000000000000000, 0.7071067811865475727, 1.000000000000000000),
 ( 1.000000000000000000, 0.7071067811865475727, 1.000000000000000000),
 ( 1.000000000000000000, 0.7071067811865471286, 1.000000000000000000),
 ( 1.000000000000000000, 0.7071067811865471286, 1.000000000000000000),
 ( 1.000000000000000000, 0.7071067811865475727, 1.000000000000000000),
 ( 1.000000000000000000, 0.7071067811865475727, 1.000000000000000000),
 ( 1.000000000000000000, 0.7071067811865477948, 1.000000000000000000),
 ( 1.000000000000000000, 0.7071067811865477948, 1.000000000000000000),
 ( 1.000000000000000000, 0.7071067811865475727, 1.000000000000000000),
 ( 1.000000000000000000, 0.7071067811865475727, 1.000000000000000000),
 ( 1.000000000000000000, 0.7071067811865475727, 1.000000000000000000),
 ( 1.000000000000000000, 0.7071067811865475727, 1.000000000000000000),
 ( 1.000000000000000000, 0.7071067811865475727, 1.000000000000000000),
 ( 1.000000000000000000, 0.7071067811865475727, 1.000000000000000000),
 ( 1.000000000000000000, 0.7071067811865475727, 1.000000000000000000),
 ( 1.000000000000000000, 0.7071067811865475727, 1.000000000000000000),
 ( 1.000000000000000000, 0.7071067811865475727, 1.000000000000000000),
 ( 1.000000000000000000, 0.7071067811865475727, 1.000000000000000000),
 ( 1.000000000000000000, 0.7071067811865475727, 1.000000000000000000),
 ( 1.000000000000000000, 0.7071067811865475727, 1.000000000000000000),
 ( 1.000000000000000000, 0.7071067811865475727, 1.000000000000000000),
 ( 1.000000000000000000, 0.7071067811865475727, 1.000000000000000000),
 ( 1.000000000000000000, 0.7071067811865466846, 1.000000000000000000),
 ( 1.000000000000000000, 0.7071067811865466846, 1.000000000000000000),
 ( 1.000000000000000000, 0.7071067811865465735, 1.000000000000000000),
 ( 1.000000000000000000, 0.7071067811865465735, 1.000000000000000000) ) ) 
 REPRESENTATION_ITEM ( '' )  SURFACE ( )  );
#3590=DIRECTION ( 'NONE',  ( 0.000000000000000000, -0.000000000000000000, -1.000000000000000000 ) ) ;
#3592=ORIENTED_EDGE ( 'NONE', *, *, #2913, .F. ) ;
#3594=LINE ( 'NONE', #7122, #3228 ) ;
#3595=ORIENTED_EDGE ( 'NONE', *, *, #3850, .F. ) ;
#3600=VERTEX_POINT ( 'NONE', #15000 ) ;
#3603=CARTESIAN_POINT ( 'NONE',  ( -5.111334017457858536, 2.499999999999999556, -113.2220991196416549 ) ) ;
#3604=CARTESIAN_POINT ( 'NONE',  ( -34.54324019596916173, 9.999999999999998224, -156.1716796081745429 ) ) ;
#3612=CARTESIAN_POINT ( 'NONE',  ( -63.28143670021790967, 10.89016550017335128, -203.4568824459457232 ) ) ;
#3613=CARTESIAN_POINT ( 'NONE',  ( 0.07898452467418404233, 2.651103404268615460, -138.2779449578589208 ) ) ;
#3618=CARTESIAN_POINT ( 'NONE',  ( -9.240119717576689595, 15.00000000000000000, -104.6630069175297564 ) ) ;
#3623=CARTESIAN_POINT ( 'NONE',  ( -62.68280523391339898, 9.999999999999998224, -198.2448752127049261 ) ) ;
#3625=ORIENTED_EDGE ( 'NONE', *, *, #12319, .T. ) ;
#3626=CARTESIAN_POINT ( 'NONE',  ( -5.229219651521534118, 9.999999999999998224, -111.7283649857152739 ) ) ;
#3629=FACE_OUTER_BOUND ( 'NONE', #2549, .T. ) ;
#3630=ADVANCED_FACE ( 'NONE', ( #13986 ), #6243, .T. ) ;
#3636=CARTESIAN_POINT ( 'NONE',  ( 0.2814260646950919043, 10.51133653148715652, 2.961392013598888706 ) ) ;
#3637=CARTESIAN_POINT ( 'NONE',  ( -4.144693943509170531, 10.67450019962763186, -47.43930023633046744 ) ) ;
#3638=CARTESIAN_POINT ( 'NONE',  ( -8.030143518455577833, 0.4858890952578076017, -104.9565718900056055 ) ) ;
#3641=DIRECTION ( 'NONE',  ( 0.000000000000000000, -1.000000000000000000, 0.000000000000000000 ) ) ;
#3642=CARTESIAN_POINT ( 'NONE',  ( -64.92429726018247038, 14.93831521102260496, -187.6311702733107154 ) ) ;
#3645=CARTESIAN_POINT ( 'NONE',  ( -5.948205887739289821, 2.500000000000000444, -109.2829347069437915 ) ) ;
#3649=CARTESIAN_POINT ( 'NONE',  ( -18.09353981420590785, 2.305072418039671334, -129.3374956033358671 ) ) ;
#3651=ADVANCED_FACE ( 'NONE', ( #10182 ), #3168, .F. ) ;
#3654=CARTESIAN_POINT ( 'NONE',  ( -69.91247589369663729, 14.99999999999771383, -187.7969989154929351 ) ) ;
#3670=ORIENTED_EDGE ( 'NONE', *, *, #3936, .T. ) ;
#3674=CARTESIAN_POINT ( 'NONE',  ( -6.336334816315998708, 2.500000000000000000, -118.7797536126130353 ) ) ;
#3677=CARTESIAN_POINT ( 'NONE',  ( -58.04430385666621817, 15.00000000000000355, -164.4058708478957271 ) ) ;
#3682=CARTESIAN_POINT ( 'NONE',  ( -67.59410015116293380, 10.89016549995086969, -204.3299372489977088 ) ) ;
#3688=CARTESIAN_POINT ( 'NONE',  ( -32.49979969806455671, 10.00000000000000178, -156.1716796081737186 ) ) ;
#3694=CARTESIAN_POINT ( 'NONE',  ( -57.72850238822916680, 10.00000000000000355, -153.7160801922878193 ) ) ;
#3697=ORIENTED_EDGE ( 'NONE', *, *, #13475, .T. ) ;
#3698=CARTESIAN_POINT ( 'NONE',  ( -0.1929122761615916781, 15.00000000000000000, -111.6573691072870957 ) ) ;
#3699=CARTESIAN_POINT ( 'NONE',  ( 0.3014166804839332192, 10.73715447649216514, 2.948015770753482645 ) ) ;
#3706=CARTESIAN_POINT ( 'NONE',  ( -4.141308399130902984, 10.68732985402159841, -47.42052949952586260 ) ) ;
#3708=CARTESIAN_POINT ( 'NONE',  ( 3.398729321283757709, 14.73417332778925015, 0.02313801857711561549 ) ) ;
#3718=CARTESIAN_POINT ( 'NONE',  ( -2.524281728693006599, 7.379999999999995453, -45.64919840677852392 ) ) ;
#3720=EDGE_LOOP ( 'NONE', ( #15, #12904, #2430, #11906 ) ) ;
#3722=EDGE_LOOP ( 'NONE', ( #7811, #3697, #1894, #7038 ) ) ;
#3723=CARTESIAN_POINT ( 'NONE',  ( -2.774786199743468629, 4.336808689942017736E-16, -115.4094725772310710 ) ) ;
#3731=VECTOR ( 'NONE', #7643, 1000.000000000000227 ) ;
#3732=CARTESIAN_POINT ( 'NONE',  ( -61.28061730020114339, 9.999999999999998224, -159.7704501038838885 ) ) ;
#3737=EDGE_CURVE ( 'NONE', #2801, #6678, #2445, .T. ) ;
#3742=CARTESIAN_POINT ( 'NONE',  ( -2.474470739939843789, 15.00000000000000355, -105.2423196785570525 ) ) ;
#3746=EDGE_LOOP ( 'NONE', ( #13506, #3800, #2390, #8883, #662, #6296 ) ) ;
#3755=CARTESIAN_POINT ( 'NONE',  ( -5.609104562801103810, 2.500000000000000444, -110.1436424206518296 ) ) ;
#3758=EDGE_CURVE ( 'NONE', #15277, #11355, #12338, .T. ) ;
#3760=EDGE_CURVE ( 'NONE', #2721, #11588, #3199, .T. ) ;
#3768=VECTOR ( 'NONE', #5810, 1000.000000000000000 ) ;
#3769=CARTESIAN_POINT ( 'NONE',  ( -67.62154853663403742, 11.85838142823737407, -203.6530897608368775 ) ) ;
#3780=CARTESIAN_POINT ( 'NONE',  ( -8.808752097635895950, 1.812406719312052994, -105.4646567900641259 ) ) ;
#3784=CARTESIAN_POINT ( 'NONE',  ( -5.170287126225677987, 9.999999999999998224, -112.1835598689908693 ) ) ;
#3789=CARTESIAN_POINT ( 'NONE',  ( 0.03998412334521189021, 2.500000000000000444, 0.4529009045602680472 ) ) ;
#3791=AXIS2_PLACEMENT_3D ( 'NONE', #7488, #5326, #7795 ) ;
#3792=CARTESIAN_POINT ( 'NONE',  ( 3.600783729107427611, 12.34370855950721868, 4.524114163355855034 ) ) ;
#3795=DIRECTION ( 'NONE',  ( 0.9982196940171965682, 0.000000000000000000, -0.05964429961207162734 ) ) ;
#3799=CARTESIAN_POINT ( 'NONE',  ( -64.80993498075393688, 14.11280149795716987, -198.2430571597587630 ) ) ;
#3800=ORIENTED_EDGE ( 'NONE', *, *, #11404, .T. ) ;
#3803=CARTESIAN_POINT ( 'NONE',  ( -3.700120845809676595, 0.000000000000000000, -118.9498343876333308 ) ) ;
#3810=EDGE_LOOP ( 'NONE', ( #13889, #14129, #7978, #9234 ) ) ;
#3814=CARTESIAN_POINT ( 'NONE',  ( -69.17701954046839319, 9.999999999999998224, -200.3386666626966246 ) ) ;
#3815=DIRECTION ( 'NONE',  ( -0.9961255586397050887, 0.000000000000000000, 0.08794243244723005948 ) ) ;
#3826=ORIENTED_EDGE ( 'NONE', *, *, #3737, .F. ) ;
#3828=CARTESIAN_POINT ( 'NONE',  ( 7.427446726622314976, 7.321094445766561876, -26.41501464507892294 ) ) ;
#3838=CARTESIAN_POINT ( 'NONE',  ( -55.37984062407457486, 9.999999999999998224, -173.4719643169354413 ) ) ;
#3850=EDGE_CURVE ( 'NONE', #5223, #11706, #11482, .T. ) ;
#3851=CARTESIAN_POINT ( 'NONE',  ( -67.63542228451777305, 12.84083462875344317, -202.2854057673654324 ) ) ;
#3852=DIRECTION ( 'NONE',  ( 0.000000000000000000, -1.000000000000000000, 0.000000000000000000 ) ) ;
#3861=CARTESIAN_POINT ( 'NONE',  ( -56.93003040406973270, 9.999999999999998224, -152.4998193340993282 ) ) ;
#3864=DIRECTION ( 'NONE',  ( 0.000000000000000000, 0.000000000000000000, 1.000000000000000000 ) ) ;
#3865=CARTESIAN_POINT ( 'NONE',  ( 2.786934050261072215, 14.45009198851748522, 0.8495871595598972759 ) ) ;
#3871=CARTESIAN_POINT ( 'NONE',  ( -4.100181976537629502, 10.82147003695433796, -47.20166826208706823 ) ) ;
#3873=CARTESIAN_POINT ( 'NONE',  ( 2.648785598488645476, 14.36106363934144703, 0.9962225538062225993 ) ) ;
#3877=CARTESIAN_POINT ( 'NONE',  ( 28.48375933933716198, 5.321094445766561876, -22.19653139158566901 ) ) ;
#3885=CARTESIAN_POINT ( 'NONE',  ( -5.689254932628163175, -1.854186021507445874E-12, -117.0567294046643099 ) ) ;
#3894=CARTESIAN_POINT ( 'NONE',  ( -56.84718378481262135, 15.00000000000000000, -162.0882091452447185 ) ) ;
#3898=DIRECTION ( 'NONE',  ( 1.076984184057326235E-17, 1.000000000000000000, 1.219901976936983860E-16 ) ) ;
#3901=DIRECTION ( 'NONE',  ( -0.7575874476598363216, 0.000000000000000000, -0.6527336816407245390 ) ) ;
#3902=ORIENTED_EDGE ( 'NONE', *, *, #9597, .T. ) ;
#3906=B_SPLINE_CURVE_WITH_KNOTS ( 'NONE', 3,
 ( #36, #9308, #14110, #8219, #3428, #1268, #11771, #12869, #2281, #5973, #6987, #112, #1190, #5892, #4747, #9538, #14264, #8364, #13095, #2509, #11626, #188, #4898, #14339, #3742, #1044, #2664, #9846 ),
 .UNSPECIFIED., .F., .F.,
 ( 4, 2, 2, 2, 2, 2, 2, 2, 2, 2, 2, 2, 2, 4 ),
 ( 1.734723475976807094E-18, 0.003819759381942296628, 0.007639518763884591522, 0.01145927814582688685, 0.01336915783679803495, 0.01527903752776918131, 0.01718891721874032941, 0.01909879690971147403, 0.02291855629165377023, 0.02387349613713933560, 0.02482843598262490098, 0.02673831567359602479, 0.02864819536456715554, 0.03055807505553827935 ),
 .UNSPECIFIED. ) ;
#3908=DIRECTION ( 'NONE',  ( 0.9961255586397050887, -0.000000000000000000, -0.08794243244723005948 ) ) ;
#3909=( BOUNDED_SURFACE ( )  B_SPLINE_SURFACE ( 3, 2, ( 
 ( #7167, #6092, #12989 ),
 ( #8332, #5862, #11970 ),
 ( #2471, #223, #2552 ),
 ( #1390, #152, #9741 ),
 ( #11888, #14228, #7330 ),
 ( #14301, #5023, #10662 ),
 ( #10808, #11811, #1311 ),
 ( #8410, #10581, #9573 ),
 ( #3957, #7252, #4790 ),
 ( #5939, #4939, #7090 ) ),
 .UNSPECIFIED., .F., .F., .T. ) 
 B_SPLINE_SURFACE_WITH_KNOTS ( ( 4, 2, 2, 2, 4 ),
 ( 3, 3 ),
 ( -2.081668171172168513E-17, 0.009142429936519532591, 0.01828485987303908600, 0.02742728980955863941, 0.03656971974607819281 ),
 ( 0.000000000000000000, 1.000000000000000000 ),
 .UNSPECIFIED. ) 
 GEOMETRIC_REPRESENTATION_ITEM ( )  RATIONAL_B_SPLINE_SURFACE ( (
 ( 1.000000000000000000, 0.7071067811865475727, 1.000000000000000000),
 ( 1.000000000000000000, 0.7071067811865475727, 1.000000000000000000),
 ( 1.000000000000000000, 0.7071067811865475727, 1.000000000000000000),
 ( 1.000000000000000000, 0.7071067811865475727, 1.000000000000000000),
 ( 1.000000000000000000, 0.7071067811865475727, 1.000000000000000000),
 ( 1.000000000000000000, 0.7071067811865475727, 1.000000000000000000),
 ( 1.000000000000000000, 0.7071067811865475727, 1.000000000000000000),
 ( 1.000000000000000000, 0.7071067811865475727, 1.000000000000000000),
 ( 1.000000000000000000, 0.7071067811865475727, 1.000000000000000000),
 ( 1.000000000000000000, 0.7071067811865475727, 1.000000000000000000) ) ) 
 REPRESENTATION_ITEM ( '' )  SURFACE ( )  );
#3913=ORIENTED_EDGE ( 'NONE', *, *, #9574, .T. ) ;
#3918=CARTESIAN_POINT ( 'NONE',  ( -62.18589641907635013, 15.00000000000000178, -176.3558874768298210 ) ) ;
#3920=CARTESIAN_POINT ( 'NONE',  ( -9.240119717576689595, 2.500000000000000444, -104.6630069175297564 ) ) ;
#3921=ORIENTED_EDGE ( 'NONE', *, *, #2993, .T. ) ;
#3927=CARTESIAN_POINT ( 'NONE',  ( -63.33207902479660589, 11.17285071206491409, -203.3434558358833328 ) ) ;
#3933=ORIENTED_EDGE ( 'NONE', *, *, #4138, .T. ) ;
#3936=EDGE_CURVE ( 'NONE', #8666, #6652, #5224, .T. ) ;
#3937=CARTESIAN_POINT ( 'NONE',  ( -8.512683829985039807, 0.7114776304792922446, -104.8579508657064849 ) ) ;
#3940=CARTESIAN_POINT ( 'NONE',  ( -3.850191409010146781, 7.379999999999995453, -49.29672681923015887 ) ) ;
#3947=CARTESIAN_POINT ( 'NONE',  ( 0.2510614944550047523, 4.187370637758943026, 2.843778190552137985 ) ) ;
#3949=CARTESIAN_POINT ( 'NONE',  ( 4.831928030476276170, 14.67058913578727264, 0.7643627623969961871 ) ) ;
#3954=ADVANCED_FACE ( 'NONE', ( #4219 ), #5914, .T. ) ;
#3957=CARTESIAN_POINT ( 'NONE',  ( -14.37903708472870790, 9.999999999999998224, -152.3617959901736754 ) ) ;
#3961=VECTOR ( 'NONE', #570, 1000.000000000000000 ) ;
#3970=CARTESIAN_POINT ( 'NONE',  ( -64.95288741863723203, 15.00000000000000000, -195.5112306306130563 ) ) ;
#3975=AXIS2_PLACEMENT_3D ( 'NONE', #1777, #7642, #13757 ) ;
#3983=EDGE_LOOP ( 'NONE', ( #7268, #12003, #3377, #1267 ) ) ;
#3990=AXIS2_PLACEMENT_3D ( 'NONE', #14239, #3641, #3339 ) ;
#3991=CARTESIAN_POINT ( 'NONE',  ( -67.58382170693634805, 5.000000000000000000, -204.5178482451963191 ) ) ;
#3994=VECTOR ( 'NONE', #8269, 1000.000000000000000 ) ;
#3998=CARTESIAN_POINT ( 'NONE',  ( -52.62960184830343735, 14.99999999999999822, -160.4142894912321822 ) ) ;
#4001=CARTESIAN_POINT ( 'NONE',  ( -14.68073284315481253, 7.499999999999991118, -92.37694453701993780 ) ) ;
#4009=CARTESIAN_POINT ( 'NONE',  ( -63.21422130130007133, 5.000000000000000888, -203.6040552426024988 ) ) ;
#4010=DIRECTION ( 'NONE',  ( 0.000000000000000000, -1.000000000000000000, 0.000000000000000000 ) ) ;
#4013=CARTESIAN_POINT ( 'NONE',  ( -67.63558047453210520, 12.45480787954772062, -202.9260935043153324 ) ) ;
#4016=ORIENTED_EDGE ( 'NONE', *, *, #2625, .T. ) ;
#4018=CARTESIAN_POINT ( 'NONE',  ( -8.763338091613618985, 1.650112951118430704, -105.4343884788352455 ) ) ;
#4029=CARTESIAN_POINT ( 'NONE',  ( -3.482786547411536038, 10.52217399014809729, -46.42572704807074047 ) ) ;
#4031=CARTESIAN_POINT ( 'NONE',  ( 9.939878312292615092, 9.999999999999998224, -115.2320631035898373 ) ) ;
#4033=AXIS2_PLACEMENT_3D ( 'NONE', #14761, #10954, #2766 ) ;
#4044=CARTESIAN_POINT ( 'NONE',  ( -65.53364736412717662, 15.00000000000000000, -203.4171941195418754 ) ) ;
#4045=ORIENTED_EDGE ( 'NONE', *, *, #13279, .T. ) ;
#4052=CARTESIAN_POINT ( 'NONE',  ( -68.82095148151569219, 14.99999999999884359, -201.5743162692542398 ) ) ;
#4055=CARTESIAN_POINT ( 'NONE',  ( -18.09353981420591140, 5.000000000000000888, -129.3374956033358387 ) ) ;
#4058=FACE_OUTER_BOUND ( 'NONE', #6748, .T. ) ;
#4063=DIRECTION ( 'NONE',  ( 0.6182966555592911417, -2.145147447033295961E-16, 0.7859448108640934016 ) ) ;
#4064=CIRCLE ( 'NONE', #14685, 2.500000000000002220 ) ;
#4077=CARTESIAN_POINT ( 'NONE',  ( -5.349394595078559966, 14.88875107336558479, -103.6307550927674157 ) ) ;
#4089=CARTESIAN_POINT ( 'NONE',  ( 0.3875314106824880311, 1.514549583805837152, 4.389575455384494340 ) ) ;
#4093=CARTESIAN_POINT ( 'NONE',  ( -67.45671875792822902, 14.09005178254165891, -198.5593552603520493 ) ) ;
#4094=DIRECTION ( 'NONE',  ( 0.6918711009959939151, -0.000000000000000000, 0.7220210382022059781 ) ) ;
#4097=CARTESIAN_POINT ( 'NONE',  ( -36.65864523137356201, 15.00000000000000355, -151.3474242096951343 ) ) ;
#4100=B_SPLINE_CURVE_WITH_KNOTS ( 'NONE', 3,
 ( #12978, #7969, #7156, #3542, #12692, #5852 ),
 .UNSPECIFIED., .F., .F.,
 ( 4, 2, 4 ),
 ( 1.301042606982605321E-18, 0.006940540637791391132, 0.01388108127558278053 ),
 .UNSPECIFIED. ) ;
#4103=CARTESIAN_POINT ( 'NONE',  ( -63.60348060676458459, 15.00000000000000000, -180.2685449772604045 ) ) ;
#4110=CARTESIAN_POINT ( 'NONE',  ( 4.856804767888951879, 14.90536770052154303, -1.840041787218201108 ) ) ;
#4115=ADVANCED_FACE ( 'NONE', ( #13433 ), #7823, .T. ) ;
#4116=CARTESIAN_POINT ( 'NONE',  ( -36.12930860108175324, 15.00000000000000000, -156.3173234978368953 ) ) ;
#4119=VERTEX_POINT ( 'NONE', #14974 ) ;
#4124=CARTESIAN_POINT ( 'NONE',  ( -3.686330242103970978, 9.945035726838405310, -47.56170239355795104 ) ) ;
#4129=CARTESIAN_POINT ( 'NONE',  ( -14.59253236707263213, 5.000000000000000000, -133.7561938577802891 ) ) ;
#4133=DIRECTION ( 'NONE',  ( -0.000000000000000000, -1.000000000000000000, -0.000000000000000000 ) ) ;
#4137=ORIENTED_EDGE ( 'NONE', *, *, #11859, .F. ) ;
#4138=EDGE_CURVE ( 'NONE', #4565, #9696, #4458, .T. ) ;
#4143=EDGE_CURVE ( 'NONE', #10703, #8603, #14845, .T. ) ;
#4145=VERTEX_POINT ( 'NONE', #3351 ) ;
#4149=CARTESIAN_POINT ( 'NONE',  ( -4.090890948359604984, 15.00000000000000000, -103.1929727064838147 ) ) ;
#4150=DIRECTION ( 'NONE',  ( 0.000000000000000000, 0.000000000000000000, -1.000000000000000000 ) ) ;
#4154=EDGE_LOOP ( 'NONE', ( #12727, #7985, #10683, #5749, #3412, #10129 ) ) ;
#4158=EDGE_CURVE ( 'NONE', #14745, #3581, #5443, .T. ) ;
#4159=ORIENTED_EDGE ( 'NONE', *, *, #6501, .T. ) ;
#4162=CARTESIAN_POINT ( 'NONE',  ( 7.460881341449208115, 3.483300008960984240, -21.91331374262868437 ) ) ;
#4163=CARTESIAN_POINT ( 'NONE',  ( 0.5034979235748735515, 4.307496502786065662, 5.703130291473766711 ) ) ;
#4167=DIRECTION ( 'NONE',  ( 0.05964429961207245307, 0.000000000000000000, 0.9982196940171964572 ) ) ;
#4173=CARTESIAN_POINT ( 'NONE',  ( -13.68460728451510455, 7.499999999999991118, -92.46488696946715891 ) ) ;
#4187=CARTESIAN_POINT ( 'NONE',  ( -45.49174724913770262, 15.00000000000000000, -154.5113044852771793 ) ) ;
#4189=ORIENTED_EDGE ( 'NONE', *, *, #3758, .T. ) ;
#4190=FACE_OUTER_BOUND ( 'NONE', #3746, .T. ) ;
#4193=CARTESIAN_POINT ( 'NONE',  ( -3.330734913716225876, 10.45930188447218967, -44.51251088684002610 ) ) ;
#4195=EDGE_CURVE ( 'NONE', #4565, #9274, #1969, .T. ) ;
#4199=CARTESIAN_POINT ( 'NONE',  ( -25.82983890416511841, 15.00000000000000000, -142.4527639562402328 ) ) ;
#4200=ADVANCED_FACE ( 'NONE', ( #6684 ), #4702, .T. ) ;
#4202=CARTESIAN_POINT ( 'NONE',  ( -5.619345720332211691, 10.00000000000000355, -110.1466364959252786 ) ) ;
#4206=AXIS2_PLACEMENT_3D ( 'NONE', #11477, #10472, #3426 ) ;
#4207=CARTESIAN_POINT ( 'NONE',  ( 2.930385861258905322, 0.6578274304494683422, 2.716317821862583859 ) ) ;
#4215=ORIENTED_EDGE ( 'NONE', *, *, #4989, .T. ) ;
#4219=FACE_OUTER_BOUND ( 'NONE', #5821, .T. ) ;
#4227=ORIENTED_EDGE ( 'NONE', *, *, #14342, .T. ) ;
#4234=FACE_OUTER_BOUND ( 'NONE', #1909, .T. ) ;
#4236=TOROIDAL_SURFACE ( 'NONE', #1017, 3.750000000000003553, 0.5000000000000000000 ) ;
#4237=CARTESIAN_POINT ( 'NONE',  ( 7.402595682379108588, 3.357345713539126031, -22.18559871638025882 ) ) ;
#4238=ADVANCED_FACE ( 'NONE', ( #14181 ), #13253, .T. ) ;
#4239=CARTESIAN_POINT ( 'NONE',  ( 0.09758847591599836835, -0.03653965946317055263, 1.105386471401409443 ) ) ;
#4250=VECTOR ( 'NONE', #6535, 1000.000000000000227 ) ;
#4264=CARTESIAN_POINT ( 'NONE',  ( -17.32624372123753886, 9.999999999999998224, -122.3796757791585321 ) ) ;
#4265=CARTESIAN_POINT ( 'NONE',  ( -41.55509581774215633, 15.00000000000000000, -158.0567977604056011 ) ) ;
#4270=DIRECTION ( 'NONE',  ( -0.000000000000000000, -1.000000000000000000, -0.000000000000000000 ) ) ;
#4277=CARTESIAN_POINT ( 'NONE',  ( -7.229287782379126170, 13.81375925440817731, -104.6456827072011038 ) ) ;
#4282=FACE_OUTER_BOUND ( 'NONE', #13981, .T. ) ;
#4295=DIRECTION ( 'NONE',  ( 0.000000000000000000, -1.000000000000000000, -0.000000000000000000 ) ) ;
#4300=AXIS2_PLACEMENT_3D ( 'NONE', #9011, #3289, #13584 ) ;
#4304=ORIENTED_EDGE ( 'NONE', *, *, #10792, .T. ) ;
#4312=CARTESIAN_POINT ( 'NONE',  ( -1.726026643059569432, 7.379999999999995453, -47.97842334616509419 ) ) ;
#4314=CARTESIAN_POINT ( 'NONE',  ( -63.84839510230030868, 9.999999999999998224, -211.4757795387517945 ) ) ;
#4315=LINE ( 'NONE', #9019, #10169 ) ;
#4321=ORIENTED_EDGE ( 'NONE', *, *, #6013, .F. ) ;
#4322=DIRECTION ( 'NONE',  ( 0.000000000000000000, 0.000000000000000000, -1.000000000000000000 ) ) ;
#4326=CARTESIAN_POINT ( 'NONE',  ( -5.307246684019970573, 4.336808689942017736E-16, -122.2414390436973122 ) ) ;
#4333=CARTESIAN_POINT ( 'NONE',  ( -5.813238319161563972, 2.708338984294549324E-32, -104.9413748694892661 ) ) ;
#4338=DIRECTION ( 'NONE',  ( 0.08794243244723007336, 0.000000000000000000, 0.9961255586397049777 ) ) ;
#4339=CARTESIAN_POINT ( 'NONE',  ( -42.37771161474321957, 9.999999999999998224, -158.4861704487694567 ) ) ;
#4342=CARTESIAN_POINT ( 'NONE',  ( 7.220173501946012706, 4.999999999999999112, -111.8642345870615458 ) ) ;
#4345=CARTESIAN_POINT ( 'NONE',  ( 2.222606327602053788, 15.00000000000000178, -129.3650357598043001 ) ) ;
#4353=CARTESIAN_POINT ( 'NONE',  ( -8.886921396801742645, 9.999999999999998224, -105.5168766094550676 ) ) ;
#4356=CARTESIAN_POINT ( 'NONE',  ( 0.5805642473066149334, -4.817921077453451975E-12, -138.6354391049652293 ) ) ;
#4357=LINE ( 'NONE', #10231, #11830 ) ;
#4368=CARTESIAN_POINT ( 'NONE',  ( -8.651269111992894167, 12.39895203580364047, -104.9132380198166885 ) ) ;
#4374=CARTESIAN_POINT ( 'NONE',  ( 0.2625675448779695720, 5.000000000000000888, 2.974107436473219401 ) ) ;
#4385=EDGE_CURVE ( 'NONE', #13160, #7071, #4942, .T. ) ;
#4387=CARTESIAN_POINT ( 'NONE',  ( 3.226532413654821685, 4.345304807832050642, 5.176332484491082297 ) ) ;
#4402=EDGE_LOOP ( 'NONE', ( #11243, #9388, #7105, #8368, #3357, #5785 ) ) ;
#4405=CARTESIAN_POINT ( 'NONE',  ( -37.87309319203819769, 9.999999999999998224, -156.6288150092206024 ) ) ;
#4407=EDGE_LOOP ( 'NONE', ( #2425, #6421, #8484, #10315 ) ) ;
#4421=CARTESIAN_POINT ( 'NONE',  ( -8.243994158936986949, 2.500000000000000444, -104.7509493499769917 ) ) ;
#4422=ADVANCED_FACE ( 'NONE', ( #13635 ), #13155, .T. ) ;
#4423=CARTESIAN_POINT ( 'NONE',  ( -5.255910738709840935, 10.00000000000000178, -115.0300074718742991 ) ) ;
#4430=ORIENTED_EDGE ( 'NONE', *, *, #10144, .T. ) ;
#4434=CARTESIAN_POINT ( 'NONE',  ( -25.82983890416511841, 9.999999999999998224, -142.4527639562402328 ) ) ;
#4448=ORIENTED_EDGE ( 'NONE', *, *, #6781, .F. ) ;
#4458=CIRCLE ( 'NONE', #7896, 2.326940983401415419 ) ;
#4465=AXIS2_PLACEMENT_3D ( 'NONE', #508, #8697, #14208 ) ;
#4467=ORIENTED_EDGE ( 'NONE', *, *, #2625, .F. ) ;
#4474=CARTESIAN_POINT ( 'NONE',  ( -0.1182668585043939180, 2.358359890833529260, -138.2405088131075956 ) ) ;
#4476=CARTESIAN_POINT ( 'NONE',  ( -2.638275913571042519, 4.336808689942017243E-16, -112.4126634647521570 ) ) ;
#4480=CIRCLE ( 'NONE', #795, 6.999999999999950262 ) ;
#4481=VERTEX_POINT ( 'NONE', #2815 ) ;
#4484=( BOUNDED_SURFACE ( )  B_SPLINE_SURFACE ( 3, 2, ( 
 ( #8967, #2016, #13625 ),
 ( #6574, #9977, #15013 ),
 ( #12450, #14944, #3025 ),
 ( #10278, #6726, #5491 ),
 ( #13697, #6500, #5339 ),
 ( #14717, #1937, #1787 ),
 ( #7732, #4116, #11439 ),
 ( #4405, #861, #635 ),
 ( #556, #10210, #12675 ),
 ( #6649, #8819, #7809 ),
 ( #14869, #6418, #9114 ),
 ( #5563, #14792, #11215 ),
 ( #13840, #4265, #3242 ),
 ( #4339, #7955, #13546 ),
 ( #10055, #12521, #4187 ),
 ( #5412, #2946, #11138 ),
 ( #5268, #8892, #1869 ),
 ( #7653, #11358, #786 ),
 ( #9046, #11286, #707 ),
 ( #13768, #12597, #3163 ),
 ( #7875, #10657, #2321 ),
 ( #4635, #15089, #1002 ),
 ( #4485, #14068, #5712 ),
 ( #2168, #3470, #3322 ),
 ( #8032, #2388, #12757 ),
 ( #12829, #15169, #6800 ),
 ( #9194, #4563, #11664 ),
 ( #13924, #14149, #72 ),
 ( #2090, #8256, #10349 ),
 ( #7084, #5857, #1222 ),
 ( #6870, #11585, #11806 ),
 ( #4784, #5932, #9272 ),
 ( #9498, #10432, #8182 ),
 ( #13996, #1082, #3395 ),
 ( #12907, #14222, #8104 ),
 ( #3623, #5634, #10509 ),
 ( #2240, #11733, #6947 ),
 ( #4710, #5788, #15243 ) ),
 .UNSPECIFIED., .F., .F., .T. ) 
 B_SPLINE_SURFACE_WITH_KNOTS ( ( 4, 2, 2, 2, 2, 2, 2, 2, 2, 2, 2, 2, 2, 2, 2, 2, 2, 2, 4 ),
 ( 3, 3 ),
 ( 0.000000000000000000, 0.004617214637118580677, 0.006925821955677870581, 0.009234429274237161353, 0.01385164391135574116, 0.01500594757063538655, 0.01616025122991503193, 0.01846885854847432271, 0.02308607318559290078, 0.02770328782271148232, 0.03232050245983006387, 0.03462910977838935811, 0.03693771709694864541, 0.04617214637118580156, 0.05540657564542296465, 0.05771518296398225889, 0.06002379028254154619, 0.06464100491966012774, 0.07387543419389729082 ),
 ( 0.000000000000000000, 1.000000000000000000 ),
 .UNSPECIFIED. ) 
 GEOMETRIC_REPRESENTATION_ITEM ( )  RATIONAL_B_SPLINE_SURFACE ( (
 ( 1.000000000000000000, 0.7071067811865475727, 1.000000000000000000),
 ( 1.000000000000000000, 0.7071067811865475727, 1.000000000000000000),
 ( 1.000000000000000000, 0.7071067811865475727, 1.000000000000000000),
 ( 1.000000000000000000, 0.7071067811865475727, 1.000000000000000000),
 ( 1.000000000000000000, 0.7071067811865475727, 1.000000000000000000),
 ( 1.000000000000000000, 0.7071067811865475727, 1.000000000000000000),
 ( 1.000000000000000000, 0.7071067811865475727, 1.000000000000000000),
 ( 1.000000000000000000, 0.7071067811865475727, 1.000000000000000000),
 ( 1.000000000000000000, 0.7071067811865475727, 1.000000000000000000),
 ( 1.000000000000000000, 0.7071067811865475727, 1.000000000000000000),
 ( 1.000000000000000000, 0.7071067811865475727, 1.000000000000000000),
 ( 1.000000000000000000, 0.7071067811865475727, 1.000000000000000000),
 ( 1.000000000000000000, 0.7071067811865475727, 1.000000000000000000),
 ( 1.000000000000000000, 0.7071067811865475727, 1.000000000000000000),
 ( 1.000000000000000000, 0.7071067811865475727, 1.000000000000000000),
 ( 1.000000000000000000, 0.7071067811865475727, 1.000000000000000000),
 ( 1.000000000000000000, 0.7071067811865475727, 1.000000000000000000),
 ( 1.000000000000000000, 0.7071067811865475727, 1.000000000000000000),
 ( 1.000000000000000000, 0.7071067811865477948, 1.000000000000000000),
 ( 1.000000000000000000, 0.7071067811865477948, 1.000000000000000000),
 ( 1.000000000000000000, 0.7071067811865475727, 1.000000000000000000),
 ( 1.000000000000000000, 0.7071067811865475727, 1.000000000000000000),
 ( 1.000000000000000000, 0.7071067811865475727, 1.000000000000000000),
 ( 1.000000000000000000, 0.7071067811865475727, 1.000000000000000000),
 ( 1.000000000000000000, 0.7071067811865475727, 1.000000000000000000),
 ( 1.000000000000000000, 0.7071067811865475727, 1.000000000000000000),
 ( 1.000000000000000000, 0.7071067811865480168, 1.000000000000000000),
 ( 1.000000000000000000, 0.7071067811865480168, 1.000000000000000000),
 ( 1.000000000000000000, 0.7071067811865475727, 1.000000000000000000),
 ( 1.000000000000000000, 0.7071067811865475727, 1.000000000000000000),
 ( 1.000000000000000000, 0.7071067811865475727, 1.000000000000000000),
 ( 1.000000000000000000, 0.7071067811865475727, 1.000000000000000000),
 ( 1.000000000000000000, 0.7071067811865475727, 1.000000000000000000),
 ( 1.000000000000000000, 0.7071067811865475727, 1.000000000000000000),
 ( 1.000000000000000000, 0.7071067811865475727, 1.000000000000000000),
 ( 1.000000000000000000, 0.7071067811865475727, 1.000000000000000000),
 ( 1.000000000000000000, 0.7071067811865475727, 1.000000000000000000),
 ( 1.000000000000000000, 0.7071067811865475727, 1.000000000000000000) ) ) 
 REPRESENTATION_ITEM ( '' )  SURFACE ( )  );
#4485=CARTESIAN_POINT ( 'NONE',  ( -52.59034431212841554, 9.999999999999998224, -168.6389827469478178 ) ) ;
#4488=EDGE_CURVE ( 'NONE', #14756, #6134, #11001, .T. ) ;
#4499=CARTESIAN_POINT ( 'NONE',  ( 3.890350893699055845, 0.000000000000000000, -1.782295516753892972 ) ) ;
#4501=CARTESIAN_POINT ( 'NONE',  ( 4.200501518084891472, 13.70058811643232843, 3.183963981513004970 ) ) ;
#4506=ORIENTED_EDGE ( 'NONE', *, *, #1793, .F. ) ;
#4510=CARTESIAN_POINT ( 'NONE',  ( 3.235167919087375221, 15.00000000000000000, -114.6791120453254962 ) ) ;
#4517=CARTESIAN_POINT ( 'NONE',  ( -55.30796743861389331, 14.99999999999543476, -150.1894123920446305 ) ) ;
#4518=CARTESIAN_POINT ( 'NONE',  ( -9.240119717569001523, 10.34875921372550955, -104.6630069174426154 ) ) ;
#4529=ORIENTED_EDGE ( 'NONE', *, *, #10907, .T. ) ;
#4537=ADVANCED_FACE ( 'NONE', ( #8594 ), #13556, .F. ) ;
#4553=CARTESIAN_POINT ( 'NONE',  ( -67.58587069055120367, 13.53642980795543593, -200.6028043760882724 ) ) ;
#4557=CARTESIAN_POINT ( 'NONE',  ( -10.46704385831657902, 0.000000000000000000, -128.9524512386204549 ) ) ;
#4563=CARTESIAN_POINT ( 'NONE',  ( -56.64898049662669877, 15.00000000000794032, -176.0284089207902980 ) ) ;
#4565=VERTEX_POINT ( 'NONE', #12155 ) ;
#4567=CARTESIAN_POINT ( 'NONE',  ( -19.94423925787078389, 15.00000000000000000, -150.2885610952392881 ) ) ;
#4573=CYLINDRICAL_SURFACE ( 'NONE', #4778, 7.000000000000016875 ) ;
#4574=EDGE_CURVE ( 'NONE', #4119, #9480, #14334, .T. ) ;
#4577=CARTESIAN_POINT ( 'NONE',  ( -25.82983890416511841, 5.000000000000000000, -142.4527639562402328 ) ) ;
#4578=EDGE_CURVE ( 'NONE', #12491, #2651, #7747, .T. ) ;
#4581=DIRECTION ( 'NONE',  ( 0.000000000000000000, -0.000000000000000000, -1.000000000000000000 ) ) ;
#4582=CARTESIAN_POINT ( 'NONE',  ( -17.32624372123753886, 15.00000000000000000, -122.3796757791585321 ) ) ;
#4588=CARTESIAN_POINT ( 'NONE',  ( -8.602511404923770755, -2.262486257093532419E-12, -105.7492080830174359 ) ) ;
#4593=DIRECTION ( 'NONE',  ( 0.000000000000000000, 0.000000000000000000, 1.000000000000000000 ) ) ;
#4597=DIRECTION ( 'NONE',  ( 0.9961255586397056438, -0.000000000000000000, -0.08794243244722428632 ) ) ;
#4598=ORIENTED_EDGE ( 'NONE', *, *, #3387, .F. ) ;
#4605=CARTESIAN_POINT ( 'NONE',  ( -20.05675593593863582, 9.999999999999998224, -128.8251628084967706 ) ) ;
#4616=CARTESIAN_POINT ( 'NONE',  ( -14.41690554581313854, 7.499999999999991118, -89.38856786110081032 ) ) ;
#4619=EDGE_LOOP ( 'NONE', ( #11646, #3437, #4754, #7557 ) ) ;
#4623=AXIS2_PLACEMENT_3D ( 'NONE', #7199, #14499, #341 ) ;
#4625=CARTESIAN_POINT ( 'NONE',  ( -66.21231308551345762, 14.86702644051741551, -190.0915466865270673 ) ) ;
#4628=CARTESIAN_POINT ( 'NONE',  ( -3.725055588901181824, 4.336808689942017243E-16, -108.1536978458372147 ) ) ;
#4631=B_SPLINE_CURVE_WITH_KNOTS ( 'NONE', 3,
 ( #8912, #2110, #6746, #6815, #3115, #7675, #1887, #878, #3261, #4207, #7828, #15033, #12542, #806, #1953, #5581 ),
 .UNSPECIFIED., .F., .F.,
 ( 4, 2, 2, 2, 2, 2, 2, 4 ),
 ( 0.000000000000000000, 0.0009849038691403968863, 0.001969807738280793773, 0.003939615476561587545, 0.004924519345701984865, 0.005909423214842381318, 0.006894327083982777771, 0.007879230953123175091 ),
 .UNSPECIFIED. ) ;
#4633=CARTESIAN_POINT ( 'NONE',  ( -44.21823081166466096, 9.999999999999998224, -145.3603131190973272 ) ) ;
#4635=CARTESIAN_POINT ( 'NONE',  ( -52.20743557207289598, 9.999999999999998224, -168.0633964595267571 ) ) ;
#4638=CARTESIAN_POINT ( 'NONE',  ( 4.921100845785776556, 4.999999999999999112, -108.2352075023247409 ) ) ;
#4645=PLANE ( 'NONE',  #2066 ) ;
#4646=DIRECTION ( 'NONE',  ( 0.08794243244723003172, 0.000000000000000000, 0.9961255586397049777 ) ) ;
#4650=CARTESIAN_POINT ( 'NONE',  ( -7.171502477872234493, 14.01677234745007183, -104.0350480920882319 ) ) ;
#4657=DIRECTION ( 'NONE',  ( 0.000000000000000000, 0.000000000000000000, -1.000000000000000000 ) ) ;
#4662=EDGE_CURVE ( 'NONE', #602, #1534, #10625, .T. ) ;
#4663=CARTESIAN_POINT ( 'NONE',  ( -52.65879960168029328, 9.999999999999998224, -146.8206079633650063 ) ) ;
#4668=DIRECTION ( 'NONE',  ( -0.000000000000000000, -1.000000000000000000, -0.000000000000000000 ) ) ;
#4672=ORIENTED_EDGE ( 'NONE', *, *, #14788, .F. ) ;
#4677=EDGE_LOOP ( 'NONE', ( #5439, #12967, #2617, #3192 ) ) ;
#4696=EDGE_CURVE ( 'NONE', #6539, #882, #6811, .T. ) ;
#4698=CARTESIAN_POINT ( 'NONE',  ( -66.76779559092599925, 14.71819778747807206, -193.1373159669256836 ) ) ;
#4699=DIRECTION ( 'NONE',  ( 0.9982196940171965682, 0.000000000000000000, -0.05964429961207244613 ) ) ;
#4702=TOROIDAL_SURFACE ( 'NONE', #7143, 8.000000000000000000, 5.000000000000000000 ) ;
#4710=CARTESIAN_POINT ( 'NONE',  ( -63.24671589544669814, 9.999999999999998224, -204.0178512890850868 ) ) ;
#4711=AXIS2_PLACEMENT_3D ( 'NONE', #11605, #10449, #10591 ) ;
#4714=CARTESIAN_POINT ( 'NONE',  ( -5.187227155321425975, 14.99999999999878142, -114.5705604395851083 ) ) ;
#4715=AXIS2_PLACEMENT_3D ( 'NONE', #14737, #12165, #11158 ) ;
#4717=CARTESIAN_POINT ( 'NONE',  ( -8.205916711996726676, 7.499999999999991118, -92.94857034792688921 ) ) ;
#4718=CARTESIAN_POINT ( 'NONE',  ( -17.32624372123753886, 15.00000000000000000, -122.3796757791585321 ) ) ;
#4723=CARTESIAN_POINT ( 'NONE',  ( 0.5065669725921494448, 10.41780148816173579, 5.737893171667577619 ) ) ;
#4724=AXIS2_PLACEMENT_3D ( 'NONE', #9002, #6536, #2047 ) ;
#4725=CARTESIAN_POINT ( 'NONE',  ( 5.844703153020811115, 9.999999999999998224, -103.2023327213425432 ) ) ;
#4730=DIRECTION ( 'NONE',  ( -0.9961255586397050887, 0.000000000000000000, 0.08794243244723005948 ) ) ;
#4733=CARTESIAN_POINT ( 'NONE',  ( -5.191659272726472985, -2.650598460978561364E-13, -112.0623128200408303 ) ) ;
#4747=CARTESIAN_POINT ( 'NONE',  ( -0.1555714895694204625, 15.00000000000000000, -114.4873493435821246 ) ) ;
#4754=ORIENTED_EDGE ( 'NONE', *, *, #8197, .T. ) ;
#4767=AXIS2_PLACEMENT_3D ( 'NONE', #11558, #13896, #2437 ) ;
#4770=CARTESIAN_POINT ( 'NONE',  ( -63.31408601554949911, 11.08167271840351376, -203.3839820180451454 ) ) ;
#4775=CARTESIAN_POINT ( 'NONE',  ( -31.09209721305613527, 10.00000000000000178, -156.3611406121567597 ) ) ;
#4778=AXIS2_PLACEMENT_3D ( 'NONE', #8267, #9435, #12768 ) ;
#4784=CARTESIAN_POINT ( 'NONE',  ( -61.08087366678788754, 9.999999999999998224, -189.6635742862258098 ) ) ;
#4786=EDGE_LOOP ( 'NONE', ( #6295, #12878 ) ) ;
#4787=CARTESIAN_POINT ( 'NONE',  ( -5.114204838963765987, 15.00000000000000000, -113.1151338089720753 ) ) ;
#4789=CARTESIAN_POINT ( 'NONE',  ( -4.924771681124648026, 0.000000000000000000, -137.0932397189673111 ) ) ;
#4790=CARTESIAN_POINT ( 'NONE',  ( -17.48543850042227277, 15.00000000000000000, -148.4417142955295219 ) ) ;
#4797=CARTESIAN_POINT ( 'NONE',  ( 2.427959467901618318, 14.27811504255466346, 3.380083252597285703 ) ) ;
#4798=CARTESIAN_POINT ( 'NONE',  ( -20.05675593593860384, 5.000000000000000000, -128.8251628084967138 ) ) ;
#4799=CARTESIAN_POINT ( 'NONE',  ( -2.141054399116760099, 5.000000000000000888, -102.7251783244459773 ) ) ;
#4800=CARTESIAN_POINT ( 'NONE',  ( -33.91109452335874153, 15.00000000000000000, -156.1716796081737471 ) ) ;
#4803=EDGE_CURVE ( 'NONE', #6539, #1674, #2996, .T. ) ;
#4804=CARTESIAN_POINT ( 'NONE',  ( -9.062504774847164768, 11.34291795009329640, -104.6069155299892088 ) ) ;
#4805=CARTESIAN_POINT ( 'NONE',  ( 7.353370788960563509, 5.000000000000000888, -111.8370434415688663 ) ) ;
#4806=ORIENTED_EDGE ( 'NONE', *, *, #13873, .T. ) ;
#4808=CARTESIAN_POINT ( 'NONE',  ( -3.296136538559349294, 8.673617379884035472E-16, -117.8031853635174144 ) ) ;
#4815=VECTOR ( 'NONE', #3237, 1000.000000000000000 ) ;
#4817=CARTESIAN_POINT ( 'NONE',  ( -47.48189921986828921, 9.999999999999998224, -141.5723758807981483 ) ) ;
#4839=DIRECTION ( 'NONE',  ( 0.000000000000000000, 0.000000000000000000, -1.000000000000000000 ) ) ;
#4840=ORIENTED_EDGE ( 'NONE', *, *, #11678, .F. ) ;
#4841=DIRECTION ( 'NONE',  ( 0.9961255586397055328, 0.000000000000000000, -0.08794243244722442510 ) ) ;
#4846=CARTESIAN_POINT ( 'NONE',  ( -64.37630138765543109, 14.38467296841567666, -209.1382580359011456 ) ) ;
#4851=CARTESIAN_POINT ( 'NONE',  ( -33.91109452335874153, 5.000000000000000888, -156.1716796081737471 ) ) ;
#4856=CARTESIAN_POINT ( 'NONE',  ( -51.63131585254111400, 9.999999999999996447, -145.6370460379244776 ) ) ;
#4859=ORIENTED_EDGE ( 'NONE', *, *, #7993, .F. ) ;
#4860=CARTESIAN_POINT ( 'NONE',  ( -5.114204838922819185, 9.999999999999998224, -113.1151338089696452 ) ) ;
#4863=CARTESIAN_POINT ( 'NONE',  ( -17.32624372123753886, 9.999999999999998224, -122.3796757791585321 ) ) ;
#4868=CARTESIAN_POINT ( 'NONE',  ( 3.237363708849736454, 14.67058913554037680, 0.2716708463123359563 ) ) ;
#4869=ADVANCED_FACE ( 'NONE', ( #12921 ), #763, .T. ) ;
#4870=CARTESIAN_POINT ( 'NONE',  ( -4.254413237569938389, 9.999999999999998224, -48.18981741835666810 ) ) ;
#4872=CARTESIAN_POINT ( 'NONE',  ( -67.58382170693634805, 5.000000000000000000, -204.5178482451963191 ) ) ;
#4875=CARTESIAN_POINT ( 'NONE',  ( -63.30269430573372347, 11.04635765553183724, -203.4099129996182853 ) ) ;
#4876=VERTEX_POINT ( 'NONE', #2334 ) ;
#4879=CARTESIAN_POINT ( 'NONE',  ( -2.748419769261051471, 4.336808689942017736E-16, -111.4617916898408652 ) ) ;
#4888=EDGE_CURVE ( 'NONE', #13160, #1079, #597, .T. ) ;
#4889=CARTESIAN_POINT ( 'NONE',  ( -64.56669032373720540, 14.99999999999999822, -198.1238327362431448 ) ) ;
#4890=EDGE_CURVE ( 'NONE', #12332, #11957, #8647, .T. ) ;
#4897=VERTEX_POINT ( 'NONE', #4798 ) ;
#4898=CARTESIAN_POINT ( 'NONE',  ( -1.526322420895694476, 14.99999999999999822, -106.9293630793504803 ) ) ;
#4908=CARTESIAN_POINT ( 'NONE',  ( -11.55175835850915789, 2.500000000000000444, -126.4710449362810607 ) ) ;
#4910=CARTESIAN_POINT ( 'NONE',  ( -53.96941264214194689, 14.99999999999999645, -161.9875822135848296 ) ) ;
#4914=CARTESIAN_POINT ( 'NONE',  ( -45.51406255979139814, 15.00000000000000355, -146.4767954873762790 ) ) ;
#4920=CARTESIAN_POINT ( 'NONE',  ( -63.21422130130007133, 9.999999999999998224, -203.6040552426024988 ) ) ;
#4933=CARTESIAN_POINT ( 'NONE',  ( -69.71822546521497088, 9.999999999999996447, -185.9780503014303861 ) ) ;
#4936=CARTESIAN_POINT ( 'NONE',  ( -5.611193301530131627, 15.00000000000000000, -110.1737759618165171 ) ) ;
#4937=CARTESIAN_POINT ( 'NONE',  ( 3.902492714259738538, 14.90432320739552452, -1.582372767571640138 ) ) ;
#4939=CARTESIAN_POINT ( 'NONE',  ( -16.94138229547579400, 15.00000000000000000, -154.2864167784019287 ) ) ;
#4942=CIRCLE ( 'NONE', #6918, 0.5000000000000012212 ) ;
#4944=CARTESIAN_POINT ( 'NONE',  ( -3.880844424049542329, 11.25546320798563649, -45.77986880073594733 ) ) ;
#4946=CARTESIAN_POINT ( 'NONE',  ( 2.958685104891044748, 14.61614439227996520, 2.621129781322379948 ) ) ;
#4953=CARTESIAN_POINT ( 'NONE',  ( 8.595858757338769252, -1.010734139224366919E-11, -113.5677547687552646 ) ) ;
#4954=ORIENTED_EDGE ( 'NONE', *, *, #3564, .T. ) ;
#4959=CARTESIAN_POINT ( 'NONE',  ( -5.336847314811834053, 2.500000000000000444, -115.5414184962005635 ) ) ;
#4963=CARTESIAN_POINT ( 'NONE',  ( -17.32624372124044854, 0.6199615622964459449, -130.2318118670719116 ) ) ;
#4967=CIRCLE ( 'NONE', #38, 14.80000000000025651 ) ;
#4969=CARTESIAN_POINT ( 'NONE',  ( -69.46795959346728466, 9.999999999999998224, -199.1268727649999732 ) ) ;
#4977=CARTESIAN_POINT ( 'NONE',  ( -25.82983890416511841, 9.999999999999998224, -142.4527639562402328 ) ) ;
#4978=CIRCLE ( 'NONE', #7449, 3.750000000000003109 ) ;
#4979=EDGE_LOOP ( 'NONE', ( #2588, #9829, #9545 ) ) ;
#4980=EDGE_CURVE ( 'NONE', #6553, #8666, #14081, .T. ) ;
#4989=EDGE_CURVE ( 'NONE', #6272, #10654, #9641, .T. ) ;
#4994=CARTESIAN_POINT ( 'NONE',  ( -9.240119717576689595, 2.500000000000000444, -104.6630069175297564 ) ) ;
#4995=CARTESIAN_POINT ( 'NONE',  ( -50.73799765964188424, 10.00000000000000000, -166.0021564914866872 ) ) ;
#4996=CARTESIAN_POINT ( 'NONE',  ( -55.81483411153980256, 14.99999999999999822, -164.4788693041486454 ) ) ;
#5004=CARTESIAN_POINT ( 'NONE',  ( -25.82983890416511841, 5.000000000000000000, -157.2527639562405000 ) ) ;
#5006=TOROIDAL_SURFACE ( 'NONE', #569, 2.000000000000016431, 5.000000000000000000 ) ;
#5007=CARTESIAN_POINT ( 'NONE',  ( -65.24151687956603496, 15.39242333475949565, -205.1717068079038597 ) ) ;
#5012=CARTESIAN_POINT ( 'NONE',  ( -63.60348060676458459, 15.00000000000000000, -180.2685449772604045 ) ) ;
#5018=CARTESIAN_POINT ( 'NONE',  ( -7.997017844161499411, 0.4580377704404314243, -104.9354529933016380 ) ) ;
#5021=CARTESIAN_POINT ( 'NONE',  ( -7.230047174306548641, 15.00000000000000000, -120.6008656443442959 ) ) ;
#5022=CARTESIAN_POINT ( 'NONE',  ( 1.419014798623991824, 13.29791182762822288, 2.129561375652841981 ) ) ;
#5023=CARTESIAN_POINT ( 'NONE',  ( -4.827681327713614579, 15.00000000000000000, -144.0483944136883565 ) ) ;
#5027=CARTESIAN_POINT ( 'NONE',  ( -3.421776217561549149, 10.60802507245954374, -46.00634398649022927 ) ) ;
#5029=AXIS2_PLACEMENT_3D ( 'NONE', #1622, #6335, #10039 ) ;
#5030=CARTESIAN_POINT ( 'NONE',  ( 0.6250914642584898262, 11.93308722886469120, 2.723738529685005183 ) ) ;
#5037=CARTESIAN_POINT ( 'NONE',  ( -1.376260179405575323, 8.673617379884035472E-16, -106.6458321843530541 ) ) ;
#5041=CARTESIAN_POINT ( 'NONE',  ( -6.947321920292441888, 2.500000000000000444, -120.0269581758342525 ) ) ;
#5047=EDGE_LOOP ( 'NONE', ( #2569, #8456, #678, #3921 ) ) ;
#5051=CARTESIAN_POINT ( 'NONE',  ( -69.84691631900385289, 9.999999999999998224, -196.7709020262129229 ) ) ;
#5056=AXIS2_PLACEMENT_3D ( 'NONE', #804, #11456, #13561 ) ;
#5059=CARTESIAN_POINT ( 'NONE',  ( 10.01939027896081313, 15.00000000000000000, -127.6977514918621637 ) ) ;
#5060=VERTEX_POINT ( 'NONE', #5107 ) ;
#5063=EDGE_LOOP ( 'NONE', ( #8821, #10774, #4954, #10200, #9082 ) ) ;
#5072=CARTESIAN_POINT ( 'NONE',  ( -5.946715039918482937, 2.500000000000000000, -117.8159155480562958 ) ) ;
#5085=CARTESIAN_POINT ( 'NONE',  ( -67.63088312920152134, 12.20966866773095560, -203.2556435494578579 ) ) ;
#5086=CARTESIAN_POINT ( 'NONE',  ( -35.49029739244800652, 9.999999999999998224, -131.2404697308744517 ) ) ;
#5092=ORIENTED_EDGE ( 'NONE', *, *, #13294, .T. ) ;
#5095=CARTESIAN_POINT ( 'NONE',  ( -8.671996357861377902, 0.9205354582397626828, -104.5402285118089623 ) ) ;
#5098=DIRECTION ( 'NONE',  ( 0.000000000000000000, -1.000000000000000000, 0.000000000000000000 ) ) ;
#5104=CARTESIAN_POINT ( 'NONE',  ( -3.589008443032619233, 10.29141329574603958, -47.02125063507394032 ) ) ;
#5106=CARTESIAN_POINT ( 'NONE',  ( 4.127667803487161002, 14.97371045984202098, 0.2463234276174943727 ) ) ;
#5107=CARTESIAN_POINT ( 'NONE',  ( -18.09353981420494151, 2.500000000000000444, -129.3374956033359240 ) ) ;
#5114=EDGE_LOOP ( 'NONE', ( #2202, #5601, #11760, #8177 ) ) ;
#5115=DIRECTION ( 'NONE',  ( 0.9961255586397055328, -0.000000000000000000, -0.08794243244722428632 ) ) ;
#5123=CARTESIAN_POINT ( 'NONE',  ( -70.08092325134745693, 9.999999999999998224, -193.7014402726132971 ) ) ;
#5134=FACE_OUTER_BOUND ( 'NONE', #3810, .T. ) ;
#5137=EDGE_CURVE ( 'NONE', #7290, #7124, #11716, .T. ) ;
#5144=FACE_OUTER_BOUND ( 'NONE', #10011, .T. ) ;
#5146=DIRECTION ( 'NONE',  ( -0.6282721832679390994, 0.000000000000000000, 0.7779936141972743080 ) ) ;
#5148=CARTESIAN_POINT ( 'NONE',  ( -35.18331673012945515, 10.00000000000000355, -156.2104531713141000 ) ) ;
#5149=CARTESIAN_POINT ( 'NONE',  ( -37.17445053438615332, 15.00000000000000533, -151.4226814532358674 ) ) ;
#5160=CARTESIAN_POINT ( 'NONE',  ( 7.333250748047245970, 3.724583123210837066, -25.23076155689903288 ) ) ;
#5162=( BOUNDED_CURVE ( )  B_SPLINE_CURVE ( 3, ( #2400, #12996, #14007, #7096 ),
 .UNSPECIFIED., .F., .F. ) 
 B_SPLINE_CURVE_WITH_KNOTS ( ( 4, 4 ),
 ( 1.145418132354773411, 1.513845819058956765 ),
 .UNSPECIFIED. ) 
 CURVE ( )  GEOMETRIC_REPRESENTATION_ITEM ( )  RATIONAL_B_SPLINE_CURVE ( ( 1.000000000000000000, 0.9887203717716437357, 0.9887203717716437357, 1.000000000000000000 ) ) 
 REPRESENTATION_ITEM ( '' )  );
#5165=CARTESIAN_POINT ( 'NONE',  ( -2.972530561760178269, 1.218752542932547250E-31, -135.1148407643974281 ) ) ;
#5170=CARTESIAN_POINT ( 'NONE',  ( -8.953163619368993409, 1.337050190710010744, -104.6006781143766631 ) ) ;
#5174=CARTESIAN_POINT ( 'NONE',  ( -5.826275610442698927, 15.00000000000000000, -101.5594179200140132 ) ) ;
#5183=CARTESIAN_POINT ( 'NONE',  ( 0.2625675448779696275, 4.834017756466201021, 2.974107436473219845 ) ) ;
#5186=AXIS2_PLACEMENT_3D ( 'NONE', #2920, #14609, #12416 ) ;
#5194=ORIENTED_EDGE ( 'NONE', *, *, #5137, .T. ) ;
#5199=VECTOR ( 'NONE', #8829, 1000.000000000000114 ) ;
#5200=CARTESIAN_POINT ( 'NONE',  ( -3.334719860237880695, 10.18881969361360085, -43.92205146497627055 ) ) ;
#5204=CARTESIAN_POINT ( 'NONE',  ( -66.67437826163231307, 15.00000000000000000, -172.5466827975835713 ) ) ;
#5205=AXIS2_PLACEMENT_3D ( 'NONE', #6477, #14772, #5249 ) ;
#5210=DIRECTION ( 'NONE',  ( 0.000000000000000000, 0.000000000000000000, -1.000000000000000000 ) ) ;
#5216=ORIENTED_EDGE ( 'NONE', *, *, #8855, .F. ) ;
#5223=VERTEX_POINT ( 'NONE', #5838 ) ;
#5224=B_SPLINE_CURVE_WITH_KNOTS ( 'NONE', 3,
 ( #1200, #4908, #14274, #2599, #11938, #9707, #9474, #3674, #5072, #9787, #14200, #13109, #9623, #3603, #14441, #7134, #8305, #14356, #13033, #3755, #7298, #2440, #7766, #14899, #10015, #10087, #8699, #7608 ),
 .UNSPECIFIED., .F., .F.,
 ( 4, 2, 2, 2, 2, 2, 2, 2, 2, 2, 2, 2, 2, 4 ),
 ( 0.000000000000000000, 0.003096043757848191032, 0.006192087515696415023, 0.009288131273544638147, 0.01238417503139286301, 0.01393219691031695809, 0.01548021878924104797, 0.01702824066816514131, 0.01780225160762721054, 0.01857626254708927283, 0.02012428442601341128, 0.02167230630493754626, 0.02322032818386167777, 0.02476835006278580928 ),
 .UNSPECIFIED. ) ;
#5226=B_SPLINE_CURVE_WITH_KNOTS ( 'NONE', 3,
 ( #10879, #5165, #3003, #5318, #8554, #2693 ),
 .UNSPECIFIED., .F., .F.,
 ( 4, 2, 4 ),
 ( 0.000000000000000000, 0.008325297288147995647, 0.01665059457629599129 ),
 .UNSPECIFIED. ) ;
#5229=CARTESIAN_POINT ( 'NONE',  ( -4.726777819131537051, 14.99999999979950083, -103.4097970346266777 ) ) ;
#5231=CARTESIAN_POINT ( 'NONE',  ( -16.94138229547581531, 5.000000000000000000, -154.2864167784019571 ) ) ;
#5233=FACE_OUTER_BOUND ( 'NONE', #10159, .T. ) ;
#5239=CARTESIAN_POINT ( 'NONE',  ( 7.287561263328109717, 3.487951394471136446, -24.83885049245541410 ) ) ;
#5240=CARTESIAN_POINT ( 'NONE',  ( 3.172663221847307646, 2.774810772982750251, 4.699280811759631860 ) ) ;
#5244=CARTESIAN_POINT ( 'NONE',  ( -65.93966772342872673, 14.90901270607003504, -188.7849136839470248 ) ) ;
#5245=DIRECTION ( 'NONE',  ( 0.000000000000000000, 0.000000000000000000, -1.000000000000000000 ) ) ;
#5249=DIRECTION ( 'NONE',  ( 0.6527336816407252051, 0.000000000000000000, -0.7575874476598356555 ) ) ;
#5253=DIRECTION ( 'NONE',  ( 0.000000000000000000, -1.000000000000000000, 0.000000000000000000 ) ) ;
#5260=CARTESIAN_POINT ( 'NONE',  ( 7.365467492728136278, 10.00000000000000533, -111.8544754347062309 ) ) ;
#5266=CARTESIAN_POINT ( 'NONE',  ( -0.3732829694918258223, 2.850949024098341860E-47, -108.7490593617764318 ) ) ;
#5268=CARTESIAN_POINT ( 'NONE',  ( -45.52432922703760454, 9.999999999999998224, -160.5926188986135799 ) ) ;
#5270=VERTEX_POINT ( 'NONE', #6564 ) ;
#5271=DIRECTION ( 'NONE',  ( -0.9961255586397055328, 0.000000000000000000, 0.08794243244722442510 ) ) ;
#5275=CARTESIAN_POINT ( 'NONE',  ( -3.333303897718212117, 9.945529814085967146, -43.56314777000268634 ) ) ;
#5277=CIRCLE ( 'NONE', #1568, 3.000000000000010214 ) ;
#5282=CARTESIAN_POINT ( 'NONE',  ( 0.9234955565201180550, 5.000000000000000888, -138.4305453062657421 ) ) ;
#5287=LINE ( 'NONE', #9999, #11458 ) ;
#5290=DIRECTION ( 'NONE',  ( -0.9961255586397056438, 0.000000000000000000, 0.08794243244722428632 ) ) ;
#5293=ORIENTED_EDGE ( 'NONE', *, *, #834, .T. ) ;
#5295=DIRECTION ( 'NONE',  ( 3.469446951953639038E-15, 0.000000000000000000, -1.000000000000000000 ) ) ;
#5302=CARTESIAN_POINT ( 'NONE',  ( -14.94456014049648473, 7.499999999999991118, -95.36532121293905107 ) ) ;
#5303=CARTESIAN_POINT ( 'NONE',  ( -7.135297789371368715, 14.04257511099845246, -104.0245404908031759 ) ) ;
#5307=DIRECTION ( 'NONE',  ( 0.000000000000000000, -1.000000000000000000, 0.000000000000000000 ) ) ;
#5308=EDGE_LOOP ( 'NONE', ( #13248, #3625, #4137 ) ) ;
#5310=CIRCLE ( 'NONE', #5544, 9.499999999999953815 ) ;
#5315=CARTESIAN_POINT ( 'NONE',  ( 0.1381806943969094426, 2.747451044191305591, 1.565175280801531121 ) ) ;
#5318=CARTESIAN_POINT ( 'NONE',  ( 2.592859759274376064, 8.673617379884034486E-16, -128.9226664866425551 ) ) ;
#5320=ORIENTED_EDGE ( 'NONE', *, *, #6964, .T. ) ;
#5325=CARTESIAN_POINT ( 'NONE',  ( -3.148647831469975955, 15.00000000000000000, -104.3063035292612142 ) ) ;
#5326=DIRECTION ( 'NONE',  ( -0.6918711009959885860, -0.000000000000000000, -0.7220210382022110851 ) ) ;
#5327=EDGE_CURVE ( 'NONE', #5060, #2896, #8908, .T. ) ;
#5334=CARTESIAN_POINT ( 'NONE',  ( 4.337102815223837560, 14.99579250108048534, -0.6629991664209412550 ) ) ;
#5336=CARTESIAN_POINT ( 'NONE',  ( -1.528156170053301510, 7.379999999999995453, -45.73714083922575213 ) ) ;
#5339=CARTESIAN_POINT ( 'NONE',  ( -34.50207410548875941, 15.00000000000000000, -151.1654763756944817 ) ) ;
#5341=ORIENTED_EDGE ( 'NONE', *, *, #15218, .F. ) ;
#5346=B_SPLINE_CURVE_WITH_KNOTS ( 'NONE', 3,
 ( #6862, #10337, #7010, #62, #8096, #15158, #3613, #4474, #9337, #2309, #6936, #10567, #1071, #9184, #3537, #11575, #3313, #1210 ),
 .UNSPECIFIED., .F., .F.,
 ( 4, 2, 2, 2, 2, 2, 2, 2, 4 ),
 ( 2.290542279903411082E-17, 0.001058365784500584416, 0.002116731569001145848, 0.002645914461251426455, 0.003175097353501707496, 0.004233463138002267409, 0.005291828922502828624, 0.006350194707003389838, 0.008466926276004512267 ),
 .UNSPECIFIED. ) ;
#5350=CARTESIAN_POINT ( 'NONE',  ( -31.08239538787591272, 9.999999999999998224, -156.3637655406869271 ) ) ;
#5352=CARTESIAN_POINT ( 'NONE',  ( 3.136841903360915396, 5.000000000000000888, -104.4936450199714955 ) ) ;
#5355=CARTESIAN_POINT ( 'NONE',  ( -25.82983890416511841, 15.00000000000000000, -142.4527639562402328 ) ) ;
#5359=CARTESIAN_POINT ( 'NONE',  ( 8.219148137446875779, 9.765288867732527697E-12, -129.9861206049809823 ) ) ;
#5373=CARTESIAN_POINT ( 'NONE',  ( -7.195331454196918664, 13.84373920325294982, -104.6286638800799125 ) ) ;
#5387=CARTESIAN_POINT ( 'NONE',  ( 7.553398589900353066, 3.720833046399418809, -21.52982307368431236 ) ) ;
#5388=CARTESIAN_POINT ( 'NONE',  ( 3.215693626676934702, 3.859180552924430074, 5.079574387784768774 ) ) ;
#5394=CARTESIAN_POINT ( 'NONE',  ( -68.22913373597590692, 10.00000000000000000, -203.2015853754454042 ) ) ;
#5398=B_SPLINE_CURVE_WITH_KNOTS ( 'NONE', 3,
 ( #11643, #5613, #124, #8614, #2600, #6307, #6064, #13272, #9788, #14443, #13350, #3838, #1596, #7219, #11939, #13195, #5985, #14201, #4995, #2759, #2524, #7462, #9708, #7299, #12177, #10860, #2676, #1361, #11023, #13034, #13110, #10782, #440, #5148, #3604, #199 ),
 .UNSPECIFIED., .F., .F.,
 ( 4, 2, 2, 2, 2, 2, 2, 2, 2, 2, 2, 2, 2, 2, 2, 2, 2, 4 ),
 ( 2.775557561562891351E-17, 0.007532187987778461540, 0.01129828198166771443, 0.01506437597555696818, 0.02259656396333555722, 0.03012875195111415147, 0.03389484594500344339, 0.03577789294194813619, 0.03766093993889282898, 0.04142703393278219376, 0.04519312792667156548, 0.04707617492361626521, 0.04895922192056095801, 0.05272531591445035748, 0.05460836291139506415, 0.05649140990833977083, 0.05837445690528447056, 0.06025750390222917030 ),
 .UNSPECIFIED. ) ;
#5404=CARTESIAN_POINT ( 'NONE',  ( -3.797998901586684628, 10.20017658455565623, -43.02000379425279419 ) ) ;
#5410=EDGE_LOOP ( 'NONE', ( #13278, #8200, #2284, #7286 ) ) ;
#5412=CARTESIAN_POINT ( 'NONE',  ( -44.50300032302160957, 9.999999999999998224, -159.8141794074082327 ) ) ;
#5414=ORIENTED_EDGE ( 'NONE', *, *, #9298, .F. ) ;
#5415=FACE_OUTER_BOUND ( 'NONE', #12407, .T. ) ;
#5417=DIRECTION ( 'NONE',  ( 0.000000000000000000, 1.734723475976805517E-15, -1.000000000000000000 ) ) ;
#5432=DIRECTION ( 'NONE',  ( -0.000000000000000000, -1.000000000000000000, -0.000000000000000000 ) ) ;
#5439=ORIENTED_EDGE ( 'NONE', *, *, #11506, .F. ) ;
#5443=CIRCLE ( 'NONE', #6682, 1.000000000000000888 ) ;
#5445=CARTESIAN_POINT ( 'NONE',  ( -6.583754373576919505, 14.38465807378985950, -103.8663350565541492 ) ) ;
#5453=ADVANCED_FACE ( 'NONE', ( #12360 ), #7074, .F. ) ;
#5454=TOROIDAL_SURFACE ( 'NONE', #6924, 9.800000000000267164, 5.000000000000000000 ) ;
#5466=CARTESIAN_POINT ( 'NONE',  ( 7.429120998017664235, 4.464394614690160523, -25.99568145149812182 ) ) ;
#5467=CARTESIAN_POINT ( 'NONE',  ( 0.03998412334521193184, 8.673617379884035472E-16, 0.4529009045602688799 ) ) ;
#5473=DIRECTION ( 'NONE',  ( -0.000000000000000000, 1.000000000000000000, -0.000000000000000000 ) ) ;
#5475=AXIS2_PLACEMENT_3D ( 'NONE', #3443, #13903, #1059 ) ;
#5477=( BOUNDED_SURFACE ( )  B_SPLINE_SURFACE ( 3, 2, ( 
 ( #2864, #12282, #1692 ),
 ( #9963, #11121, #540 ),
 ( #13534, #14929, #13754 ),
 ( #12505, #770, #9029 ),
 ( #1923, #6636, #3149 ),
 ( #11343, #5478, #10196 ),
 ( #4326, #10826, #9591 ),
 ( #95, #2490, #5041 ),
 ( #244, #6035, #14405 ),
 ( #3803, #11755, #14319 ),
 ( #4808, #3885, #9759 ),
 ( #328, #12061, #4959 ),
 ( #3723, #11826, #10678 ),
 ( #1250, #5956, #7184 ),
 ( #13005, #9674, #8348 ),
 ( #9522, #1175, #8508 ),
 ( #5876, #13243, #2722 ),
 ( #7271, #4733, #8428 ),
 ( #4879, #10596, #14487 ),
 ( #2410, #11985, #7348 ),
 ( #14172, #13161, #2646 ),
 ( #1479, #6194, #3575 ),
 ( #14243, #2570, #3645 ),
 ( #11907, #13074, #17 ),
 ( #10910, #1331, #6113 ),
 ( #1408, #8584, #13317 ),
 ( #9444, #10755, #172 ),
 ( #8277, #7106, #13870 ),
 ( #12856, #1179, #8127 ),
 ( #6893, #12629, #5659 ),
 ( #5588, #4588, #6823 ),
 ( #9295, #5738, #5813 ) ),
 .UNSPECIFIED., .F., .F., .T. ) 
 B_SPLINE_SURFACE_WITH_KNOTS ( ( 4, 2, 2, 2, 2, 2, 2, 2, 2, 2, 2, 2, 2, 2, 2, 4 ),
 ( 3, 3 ),
 ( 0.000000000000000000, 0.003626821300828501123, 0.007253642601657002247, 0.009067053252071253025, 0.01088046390248550294, 0.01450728520331400449, 0.01632069585372825440, 0.01813410650414250605, 0.01904081182934962840, 0.01994751715455675423, 0.02176092780497100587, 0.02357433845538525752, 0.02448104378059238334, 0.02538774910579950916, 0.02720115975621376081, 0.02901457040662800899 ),
 ( 0.000000000000000000, 1.000000000000000000 ),
 .UNSPECIFIED. ) 
 GEOMETRIC_REPRESENTATION_ITEM ( )  RATIONAL_B_SPLINE_SURFACE ( (
 ( 1.000000000000000000, 0.7071067811865475727, 1.000000000000000000),
 ( 1.000000000000000000, 0.7071067811865475727, 1.000000000000000000),
 ( 1.000000000000000000, 0.7071067811865475727, 1.000000000000000000),
 ( 1.000000000000000000, 0.7071067811865475727, 1.000000000000000000),
 ( 1.000000000000000000, 0.7071067811865475727, 1.000000000000000000),
 ( 1.000000000000000000, 0.7071067811865475727, 1.000000000000000000),
 ( 1.000000000000000000, 0.7071067811865475727, 1.000000000000000000),
 ( 1.000000000000000000, 0.7071067811865475727, 1.000000000000000000),
 ( 1.000000000000000000, 0.7071067811865475727, 1.000000000000000000),
 ( 1.000000000000000000, 0.7071067811865475727, 1.000000000000000000),
 ( 1.000000000000000000, 0.7071067811865475727, 1.000000000000000000),
 ( 1.000000000000000000, 0.7071067811865475727, 1.000000000000000000),
 ( 1.000000000000000000, 0.7071067811865476838, 1.000000000000000000),
 ( 1.000000000000000000, 0.7071067811865476838, 1.000000000000000000),
 ( 1.000000000000000000, 0.7071067811865474617, 1.000000000000000000),
 ( 1.000000000000000000, 0.7071067811865474617, 1.000000000000000000),
 ( 1.000000000000000000, 0.7071067811865475727, 1.000000000000000000),
 ( 1.000000000000000000, 0.7071067811865475727, 1.000000000000000000),
 ( 1.000000000000000000, 0.7071067811865475727, 1.000000000000000000),
 ( 1.000000000000000000, 0.7071067811865475727, 1.000000000000000000),
 ( 1.000000000000000000, 0.7071067811865475727, 1.000000000000000000),
 ( 1.000000000000000000, 0.7071067811865475727, 1.000000000000000000),
 ( 1.000000000000000000, 0.7071067811865475727, 1.000000000000000000),
 ( 1.000000000000000000, 0.7071067811865475727, 1.000000000000000000),
 ( 1.000000000000000000, 0.7071067811865485719, 1.000000000000000000),
 ( 1.000000000000000000, 0.7071067811865485719, 1.000000000000000000),
 ( 1.000000000000000000, 0.7071067811865475727, 1.000000000000000000),
 ( 1.000000000000000000, 0.7071067811865475727, 1.000000000000000000),
 ( 1.000000000000000000, 0.7071067811865460184, 1.000000000000000000),
 ( 1.000000000000000000, 0.7071067811865460184, 1.000000000000000000),
 ( 1.000000000000000000, 0.7071067811865460184, 1.000000000000000000),
 ( 1.000000000000000000, 0.7071067811865460184, 1.000000000000000000) ) ) 
 REPRESENTATION_ITEM ( '' )  SURFACE ( )  );
#5478=CARTESIAN_POINT ( 'NONE',  ( -7.754603562414723150, -2.363702682127649382E-12, -121.4663199873584034 ) ) ;
#5485=CARTESIAN_POINT ( 'NONE',  ( 4.882278757662108504, 14.90393508816177714, -1.535399676672468905 ) ) ;
#5490=DIRECTION ( 'NONE',  ( 0.000000000000000000, 0.000000000000000000, -1.000000000000000000 ) ) ;
#5491=CARTESIAN_POINT ( 'NONE',  ( -33.72825374957025701, 15.00000000000000000, -151.1581928109187345 ) ) ;
#5494=CARTESIAN_POINT ( 'NONE',  ( -9.110371329266945040, 9.999999999999998224, -123.5182978443285720 ) ) ;
#5496=CARTESIAN_POINT ( 'NONE',  ( -33.91109452335874153, 5.000000000000000000, -156.1716796081737471 ) ) ;
#5501=CARTESIAN_POINT ( 'NONE',  ( -67.29661116483785577, 15.00000000000001243, -205.0278900928574615 ) ) ;
#5502=CARTESIAN_POINT ( 'NONE',  ( -8.631701571668326523, 11.65889702651062443, -105.3772359608016984 ) ) ;
#5505=CARTESIAN_POINT ( 'NONE',  ( 4.856804767890306351, 14.90536770052033866, -1.840041787218210878 ) ) ;
#5507=CARTESIAN_POINT ( 'NONE',  ( -4.994618032138967045, 8.673617379884035472E-16, -137.1639743028343048 ) ) ;
#5508=DIRECTION ( 'NONE',  ( 0.000000000000000000, -0.000000000000000000, -1.000000000000000000 ) ) ;
#5513=AXIS2_PLACEMENT_3D ( 'NONE', #9855, #14588, #2834 ) ;
#5519=DIRECTION ( 'NONE',  ( -0.08794243244722425856, -0.000000000000000000, -0.9961255586397054218 ) ) ;
#5520=DIRECTION ( 'NONE',  ( 0.000000000000000000, 0.000000000000000000, -1.000000000000000000 ) ) ;
#5523=TOROIDAL_SURFACE ( 'NONE', #10468, 3.750000000000003553, 0.5000000000000000000 ) ;
#5527=CARTESIAN_POINT ( 'NONE',  ( 3.891364641103949307, 14.90536770052033688, -1.768596708628434211 ) ) ;
#5540=CARTESIAN_POINT ( 'NONE',  ( 0.4428117151818120600, 2.348215632956504262, 5.015736486741213085 ) ) ;
#5544=AXIS2_PLACEMENT_3D ( 'NONE', #2357, #6906, #14189 ) ;
#5556=DIRECTION ( 'NONE',  ( -0.000000000000000000, 1.000000000000000000, -0.000000000000000000 ) ) ;
#5559=CARTESIAN_POINT ( 'NONE',  ( 7.190027994173562753, 7.321094445766561876, -30.38850508759179192 ) ) ;
#5560=VERTEX_POINT ( 'NONE', #14281 ) ;
#5563=CARTESIAN_POINT ( 'NONE',  ( -41.27834176923248322, 9.999999999999998224, -157.9203444102009826 ) ) ;
#5573=CARTESIAN_POINT ( 'NONE',  ( -33.91109452337774854, 10.00000000000000178, -156.1716796081737471 ) ) ;
#5575=CARTESIAN_POINT ( 'NONE',  ( -65.53364736412717662, 15.00000000000000000, -205.7441351029432894 ) ) ;
#5576=CARTESIAN_POINT ( 'NONE',  ( -8.223364455376053428, 12.56334999322341517, -105.1585554315304165 ) ) ;
#5581=CARTESIAN_POINT ( 'NONE',  ( 2.530298019944474675, 0.000000000000000000, 0.2330448234422078380 ) ) ;
#5584=ORIENTED_EDGE ( 'NONE', *, *, #4696, .T. ) ;
#5588=CARTESIAN_POINT ( 'NONE',  ( -6.941963816496072859, 4.336808689942017736E-16, -103.8778697715490011 ) ) ;
#5591=CARTESIAN_POINT ( 'NONE',  ( -3.315923205871632362, 9.650666666666662508, -43.24506100211545601 ) ) ;
#5593=CARTESIAN_POINT ( 'NONE',  ( -8.718986484435074402, 11.36792136375515483, -105.4248486380225813 ) ) ;
#5601=ORIENTED_EDGE ( 'NONE', *, *, #4888, .F. ) ;
#5604=FACE_OUTER_BOUND ( 'NONE', #12033, .T. ) ;
#5608=DIRECTION ( 'NONE',  ( 0.000000000000000000, -1.000000000000000000, 0.000000000000000000 ) ) ;
#5609=DIRECTION ( 'NONE',  ( 0.000000000000000000, 0.000000000000000000, -1.000000000000000000 ) ) ;
#5613=CARTESIAN_POINT ( 'NONE',  ( -63.01211225522952475, 9.999999999999998224, -201.0953633257875026 ) ) ;
#5622=CARTESIAN_POINT ( 'NONE',  ( -64.80788720177807249, 14.99074302883816756, -184.1356180242662788 ) ) ;
#5630=EDGE_CURVE ( 'NONE', #6631, #4876, #14603, .T. ) ;
#5634=CARTESIAN_POINT ( 'NONE',  ( -62.68280523401330129, 14.99999999999469225, -198.2448752127326088 ) ) ;
#5645=CARTESIAN_POINT ( 'NONE',  ( 3.230086971182892785, 10.25843542224570193, 5.208283727272518426 ) ) ;
#5648=CARTESIAN_POINT ( 'NONE',  ( -10.85850957030563713, 10.00000000000000178, -125.6943677036881866 ) ) ;
#5651=FACE_OUTER_BOUND ( 'NONE', #5063, .T. ) ;
#5652=DIRECTION ( 'NONE',  ( -0.000000000000000000, -1.000000000000000000, -0.000000000000000000 ) ) ;
#5653=ORIENTED_EDGE ( 'NONE', *, *, #12446, .T. ) ;
#5659=CARTESIAN_POINT ( 'NONE',  ( -8.225432057776796313, 2.500000000000000444, -106.0978137656049824 ) ) ;
#5662=FACE_OUTER_BOUND ( 'NONE', #6817, .T. ) ;
#5664=CARTESIAN_POINT ( 'NONE',  ( -8.948682078903175352, 11.69044914887355979, -104.5711183077397948 ) ) ;
#5665=AXIS2_PLACEMENT_3D ( 'NONE', #11452, #6512, #9058 ) ;
#5667=AXIS2_PLACEMENT_3D ( 'NONE', #12561, #4597, #9306 ) ;
#5671=ORIENTED_EDGE ( 'NONE', *, *, #9512, .F. ) ;
#5687=CARTESIAN_POINT ( 'NONE',  ( -11.94594212905470343, 10.00000000000000533, -150.3828439890653215 ) ) ;
#5695=ORIENTED_EDGE ( 'NONE', *, *, #3541, .F. ) ;
#5701=EDGE_CURVE ( 'NONE', #9864, #5223, #12399, .T. ) ;
#5702=CARTESIAN_POINT ( 'NONE',  ( -66.40912117502934109, 14.82863921643819261, -191.0993814215748330 ) ) ;
#5705=CARTESIAN_POINT ( 'NONE',  ( -4.273407437632543271, 4.336808689942017243E-16, -107.1048060010029417 ) ) ;
#5708=CARTESIAN_POINT ( 'NONE',  ( -3.782526895735879524, 9.999999999999998224, -42.84475209785865246 ) ) ;
#5712=CARTESIAN_POINT ( 'NONE',  ( -56.77487962284654088, 15.00000000000000000, -165.9012238629486262 ) ) ;
#5716=CARTESIAN_POINT ( 'NONE',  ( 0.7644969749118040170, 5.000000000000000000, -138.4027240657576101 ) ) ;
#5724=CARTESIAN_POINT ( 'NONE',  ( 6.089666224640344794, 15.00000000000000000, -124.6062682140657074 ) ) ;
#5726=CARTESIAN_POINT ( 'NONE',  ( -6.198501765558289911, 14.51381462227466201, -104.1424196585592057 ) ) ;
#5730=CARTESIAN_POINT ( 'NONE',  ( 1.855481649321463200, 15.00000000000000000, -35.83830032691797385 ) ) ;
#5738=CARTESIAN_POINT ( 'NONE',  ( -9.000077715877313977, -1.040834085586084099E-14, -105.4229635846035222 ) ) ;
#5744=DIRECTION ( 'NONE',  ( -0.000000000000000000, -1.000000000000000000, -0.000000000000000000 ) ) ;
#5749=ORIENTED_EDGE ( 'NONE', *, *, #3737, .T. ) ;
#5764=AXIS2_PLACEMENT_3D ( 'NONE', #9986, #2952, #7738 ) ;
#5772=AXIS2_PLACEMENT_3D ( 'NONE', #712, #9118, #3247 ) ;
#5777=B_SPLINE_CURVE_WITH_KNOTS ( 'NONE', 3,
 ( #13239, #92, #7180, #4875, #8344, #5952, #9587, #9360, #6108, #5806, #12929, #168, #10527, #9519, #3799, #2486, #3572, #10751, #13, #10821, #8504, #2406, #3642, #9441, #14169, #13002, #2566, #1402, #11903, #6968 ),
 .UNSPECIFIED., .F., .F.,
 ( 4, 2, 2, 2, 2, 2, 2, 2, 2, 2, 2, 2, 2, 2, 4 ),
 ( 1.734723475976807094E-18, 0.0008039673220171474803, 0.001607934644034293226, 0.002411901966051438646, 0.003215869288068584717, 0.004823803932102929334, 0.006431738576137275253, 0.008039673220171619436, 0.009647607864205964487, 0.01286347715227465285, 0.01607934644034334642, 0.01929521572841203653, 0.02251108501648072663, 0.02411901966051507862, 0.02572695430454942367 ),
 .UNSPECIFIED. ) ;
#5779=CARTESIAN_POINT ( 'NONE',  ( -64.23600185951367791, 13.34030093836066300, -200.8190070947437391 ) ) ;
#5785=ORIENTED_EDGE ( 'NONE', *, *, #14546, .T. ) ;
#5788=CARTESIAN_POINT ( 'NONE',  ( -63.24671589544670525, 15.00000000000000000, -204.0178512890850584 ) ) ;
#5792=CARTESIAN_POINT ( 'NONE',  ( -10.46704385831657902, 0.000000000000000000, -128.9524512386204549 ) ) ;
#5800=CARTESIAN_POINT ( 'NONE',  ( -4.212126835263352298, 10.36695148008834266, -47.83691020068690847 ) ) ;
#5804=FACE_OUTER_BOUND ( 'NONE', #3983, .T. ) ;
#5806=CARTESIAN_POINT ( 'NONE',  ( -63.97645733981619998, 12.92636406023319395, -201.6791002821226755 ) ) ;
#5808=EDGE_CURVE ( 'NONE', #14745, #745, #7839, .T. ) ;
#5809=VERTEX_POINT ( 'NONE', #5591 ) ;
#5810=DIRECTION ( 'NONE',  ( -0.000000000000000000, -1.000000000000000000, -0.000000000000000000 ) ) ;
#5813=CARTESIAN_POINT ( 'NONE',  ( -9.000077715877306872, 2.500000000000000444, -105.4229635846035222 ) ) ;
#5816=CARTESIAN_POINT ( 'NONE',  ( -48.64052432076086063, 9.999999999999998224, -142.5706416652736266 ) ) ;
#5817=CARTESIAN_POINT ( 'NONE',  ( -9.285933602755209293, 10.36776190932097386, -105.1819416493744654 ) ) ;
#5821=EDGE_LOOP ( 'NONE', ( #9041, #8238, #7353, #12397 ) ) ;
#5826=VERTEX_POINT ( 'NONE', #10306 ) ;
#5827=DIRECTION ( 'NONE',  ( 1.770125995894655399E-15, 0.000000000000000000, -1.000000000000000000 ) ) ;
#5838=CARTESIAN_POINT ( 'NONE',  ( -6.683304552674626642, 0.000000000000000000, -104.1296019027811894 ) ) ;
#5841=AXIS2_PLACEMENT_3D ( 'NONE', #875, #7970, #2335 ) ;
#5842=EDGE_LOOP ( 'NONE', ( #9955, #1557, #5341, #13453, #9405, #3366, #4045, #5695, #11013 ) ) ;
#5847=CARTESIAN_POINT ( 'NONE',  ( -67.63177441509803600, 12.98106818090269776, -202.0046632239205451 ) ) ;
#5852=CARTESIAN_POINT ( 'NONE',  ( 6.049910241306248437, 15.00000000000000000, -118.3734240199295300 ) ) ;
#5853=CARTESIAN_POINT ( 'NONE',  ( -63.21422130130007133, 5.000000000000000000, -203.6040552426024703 ) ) ;
#5857=CARTESIAN_POINT ( 'NONE',  ( -60.56192452146473215, 15.00000000000000000, -187.5450233986829289 ) ) ;
#5860=CARTESIAN_POINT ( 'NONE',  ( -5.541218901316622869, 9.999999999999998224, -110.3933575420723372 ) ) ;
#5861=CARTESIAN_POINT ( 'NONE',  ( 0.8629277978856378928, 12.44510974438689210, 2.552542045932815640 ) ) ;
#5862=CARTESIAN_POINT ( 'NONE',  ( 8.054779650680396585, 15.00000000000000000, -130.1950568140550502 ) ) ;
#5867=CARTESIAN_POINT ( 'NONE',  ( 2.850044070969222521, 5.000000000000000888, -103.0233998225063345 ) ) ;
#5868=DIRECTION ( 'NONE',  ( 0.9652928478129130241, 2.009419397152280694E-15, -0.2611699024796625968 ) ) ;
#5872=PLANE ( 'NONE',  #13608 ) ;
#5873=CARTESIAN_POINT ( 'NONE',  ( 5.079523875978591896, -9.029077709185064432E-12, -108.2552591983019994 ) ) ;
#5876=CARTESIAN_POINT ( 'NONE',  ( -2.651064740270022035, 0.000000000000000000, -112.3760762047032387 ) ) ;
#5881=ORIENTED_EDGE ( 'NONE', *, *, #532, .F. ) ;
#5884=CARTESIAN_POINT ( 'NONE',  ( -44.21823081166475333, 15.00000000000000000, -145.3603131190974125 ) ) ;
#5892=CARTESIAN_POINT ( 'NONE',  ( -0.2180828300734916347, 15.00000000000000178, -115.1409152625263346 ) ) ;
#5895=ORIENTED_EDGE ( 'NONE', *, *, #368, .T. ) ;
#5903=AXIS2_PLACEMENT_3D ( 'NONE', #3718, #4730, #14240 ) ;
#5907=CARTESIAN_POINT ( 'NONE',  ( -16.94138229547582242, 9.999999999999998224, -154.2864167784019003 ) ) ;
#5914=TOROIDAL_SURFACE ( 'NONE', #11603, 5.000000000000001776, 5.000000000000000000 ) ;
#5918=VECTOR ( 'NONE', #14736, 1000.000000000000000 ) ;
#5919=CARTESIAN_POINT ( 'NONE',  ( -67.60945598279326418, 13.34030093848967269, -201.1617207694782223 ) ) ;
#5924=ADVANCED_FACE ( 'NONE', ( #5662 ), #3584, .T. ) ;
#5926=CIRCLE ( 'NONE', #3223, 5.000000000000000000 ) ;
#5927=CARTESIAN_POINT ( 'NONE',  ( -15.73004658022870927, 0.000000000000000000, -131.7446186346720367 ) ) ;
#5932=CARTESIAN_POINT ( 'NONE',  ( -61.08087366679612984, 15.00000000000267164, -189.6635742862125085 ) ) ;
#5933=CIRCLE ( 'NONE', #15091, 3.000000000000010214 ) ;
#5936=CARTESIAN_POINT ( 'NONE',  ( -5.254015288333886424, 9.999999999999998224, -115.0648584343545764 ) ) ;
#5938=CARTESIAN_POINT ( 'NONE',  ( 3.892182721467340123, 14.89914772901184747, -1.394991539848200457 ) ) ;
#5939=CARTESIAN_POINT ( 'NONE',  ( -16.94138229547579400, 9.999999999999998224, -154.2864167784019287 ) ) ;
#5945=CARTESIAN_POINT ( 'NONE',  ( 3.189625183574164247, 14.71804858691771578, 2.256190190007254515 ) ) ;
#5947=CARTESIAN_POINT ( 'NONE',  ( -8.886921396801742645, 9.999999999999998224, -105.5168766094550676 ) ) ;
#5949=CARTESIAN_POINT ( 'NONE',  ( 3.230086961373092702, 10.41478694124928239, 5.208283729180116062 ) ) ;
#5951=CARTESIAN_POINT ( 'NONE',  ( -8.754992051701663058, 12.12271237224970477, -104.5108651954749917 ) ) ;
#5952=CARTESIAN_POINT ( 'NONE',  ( -63.47082007717695973, 11.73238145425375301, -203.0222944482916887 ) ) ;
#5953=ORIENTED_EDGE ( 'NONE', *, *, #224, .T. ) ;
#5956=CARTESIAN_POINT ( 'NONE',  ( -5.137754182365905642, -1.054997312397557146E-12, -114.0283549521487174 ) ) ;
#5962=CIRCLE ( 'NONE', #13120, 1.000000000000000888 ) ;
#5973=CARTESIAN_POINT ( 'NONE',  ( -1.065067592858583323, 15.00000000000000178, -118.9225514786646016 ) ) ;
#5980=ORIENTED_EDGE ( 'NONE', *, *, #14788, .T. ) ;
#5984=CARTESIAN_POINT ( 'NONE',  ( -9.153863602783623321, 1.835169552024503936, -104.6442049519377804 ) ) ;
#5985=CARTESIAN_POINT ( 'NONE',  ( -52.54183813970617223, 9.999999999999996447, -168.5664894671085392 ) ) ;
#5990=VERTEX_POINT ( 'NONE', #6587 ) ;
#5991=ADVANCED_FACE ( 'NONE', ( #14879 ), #11298, .T. ) ;
#5992=FACE_OUTER_BOUND ( 'NONE', #10473, .T. ) ;
#5997=CARTESIAN_POINT ( 'NONE',  ( -67.58823768853794434, 10.57596889791075867, -204.4395760673659197 ) ) ;
#6004=AXIS2_PLACEMENT_3D ( 'NONE', #14948, #1709, #6654 ) ;
#6008=CARTESIAN_POINT ( 'NONE',  ( -47.48189921986828210, 9.999999999999998224, -141.5723758807981483 ) ) ;
#6011=EDGE_LOOP ( 'NONE', ( #9590, #14430, #44, #11252 ) ) ;
#6012=CARTESIAN_POINT ( 'NONE',  ( -0.5690871621892230614, 14.99999999999999822, -109.6097011989409111 ) ) ;
#6013=EDGE_CURVE ( 'NONE', #119, #10778, #15309, .T. ) ;
#6016=CYLINDRICAL_SURFACE ( 'NONE', #12934, 6.999999999999950262 ) ;
#6018=AXIS2_PLACEMENT_3D ( 'NONE', #1599, #13352, #6382 ) ;
#6023=CARTESIAN_POINT ( 'NONE',  ( 3.489143780149524421, 14.82608718968779371, 1.723058558630278014 ) ) ;
#6028=AXIS2_PLACEMENT_3D ( 'NONE', #9438, #1169, #8 ) ;
#6029=CARTESIAN_POINT ( 'NONE',  ( -8.422539546171003977, 12.70549722942692661, -104.4083970429161639 ) ) ;
#6030=FACE_OUTER_BOUND ( 'NONE', #10084, .T. ) ;
#6034=VERTEX_POINT ( 'NONE', #5352 ) ;
#6035=CARTESIAN_POINT ( 'NONE',  ( -6.701857729235380923, -1.323436422439033798E-13, -119.5348842628491042 ) ) ;
#6040=ORIENTED_EDGE ( 'NONE', *, *, #12736, .F. ) ;
#6041=VECTOR ( 'NONE', #11729, 1000.000000000000000 ) ;
#6044=CARTESIAN_POINT ( 'NONE',  ( -60.12955526703344589, 15.00000000000000000, -169.2020697305022736 ) ) ;
#6045=DIRECTION ( 'NONE',  ( 0.06144244613646117348, 0.7154473348115029108, 0.6959597236362787820 ) ) ;
#6057=( BOUNDED_CURVE ( )  B_SPLINE_CURVE ( 3, ( #6510, #2101, #11225, #6735 ),
 .UNSPECIFIED., .F., .T. ) 
 B_SPLINE_CURVE_WITH_KNOTS ( ( 4, 4 ),
 ( 0.2828104278872010102, 0.5984188431165737843 ),
 .UNSPECIFIED. ) 
 CURVE ( )  GEOMETRIC_REPRESENTATION_ITEM ( )  RATIONAL_B_SPLINE_CURVE ( ( 1.000000000000000000, 0.9917164885600966429, 0.9917164885600966429, 1.000000000000000000 ) ) 
 REPRESENTATION_ITEM ( '' )  );
#6064=CARTESIAN_POINT ( 'NONE',  ( -61.15244389481968312, 10.00000000000000000, -189.9478847066162643 ) ) ;
#6065=EDGE_CURVE ( 'NONE', #14402, #9864, #527, .T. ) ;
#6066=CARTESIAN_POINT ( 'NONE',  ( -62.93226630389403908, 14.99999999999999822, -178.2952964610624349 ) ) ;
#6067=MECHANICAL_CONTEXT ( 'NONE', #2448, 'mechanical' ) ;
#6073=CARTESIAN_POINT ( 'NONE',  ( -2.524281728693006599, 7.379999999999995453, -45.64919840677852392 ) ) ;
#6075=CARTESIAN_POINT ( 'NONE',  ( -63.84839520601438778, 10.76401871533024313, -211.4757790814346947 ) ) ;
#6076=DIRECTION ( 'NONE',  ( 0.000000000000000000, 0.000000000000000000, -1.000000000000000000 ) ) ;
#6078=CARTESIAN_POINT ( 'NONE',  ( -8.661991262811106651, 15.00000000000000000, -130.6821289911104316 ) ) ;
#6083=ORIENTED_EDGE ( 'NONE', *, *, #7993, .T. ) ;
#6086=CARTESIAN_POINT ( 'NONE',  ( -8.630633989116716975, 0.8298274931565884360, -104.9068229896404461 ) ) ;
#6089=CARTESIAN_POINT ( 'NONE',  ( -1.056049066447270590, 15.00000000000000000, -118.8733157714634672 ) ) ;
#6090=AXIS2_PLACEMENT_3D ( 'NONE', #10924, #3898, #6209 ) ;
#6092=CARTESIAN_POINT ( 'NONE',  ( 10.01939027896081491, 15.00000000000000000, -127.6977514918621637 ) ) ;
#6097=CARTESIAN_POINT ( 'NONE',  ( -4.057877601665376588, 10.61085214779863151, -45.92595659261393592 ) ) ;
#6099=CARTESIAN_POINT ( 'NONE',  ( 3.477102512744043583, 11.93308722758116147, 4.762272240101847132 ) ) ;
#6100=DIRECTION ( 'NONE',  ( 0.000000000000000000, -1.000000000000000000, 0.000000000000000000 ) ) ;
#6101=EDGE_CURVE ( 'NONE', #9696, #447, #7746, .T. ) ;
#6102=EDGE_CURVE ( 'NONE', #13770, #3511, #5162, .T. ) ;
#6108=CARTESIAN_POINT ( 'NONE',  ( -63.75486902486332497, 12.47328257159134779, -202.3017344482634030 ) ) ;
#6113=CARTESIAN_POINT ( 'NONE',  ( -6.399074640931504021, 2.500000000000000444, -108.4234853095435369 ) ) ;
#6118=EDGE_LOOP ( 'NONE', ( #13586, #1104 ) ) ;
#6122=CARTESIAN_POINT ( 'NONE',  ( -64.62739667067044991, 15.00000000000000000, -185.6367153532767986 ) ) ;
#6127=DIRECTION ( 'NONE',  ( 0.000000000000000000, 1.000000000000000000, 0.000000000000000000 ) ) ;
#6134=VERTEX_POINT ( 'NONE', #14080 ) ;
#6144=DIRECTION ( 'NONE',  ( 0.9961255586397056438, 0.000000000000000000, -0.08794243244722427244 ) ) ;
#6145=CARTESIAN_POINT ( 'NONE',  ( -38.70827623999313971, 15.00000000000000355, -151.7039193589360764 ) ) ;
#6152=CARTESIAN_POINT ( 'NONE',  ( -64.55122089772132199, 14.81922317904516184, -208.3565710730559033 ) ) ;
#6158=DIRECTION ( 'NONE',  ( 0.000000000000000000, 0.000000000000000000, -1.000000000000000000 ) ) ;
#6160=AXIS2_PLACEMENT_3D ( 'NONE', #8274, #7267, #14089 ) ;
#6164=CARTESIAN_POINT ( 'NONE',  ( -68.56997004632950166, 9.999999999999998224, -179.5402275981996638 ) ) ;
#6166=ADVANCED_FACE ( 'NONE', ( #1016 ), #7694, .T. ) ;
#6169=CARTESIAN_POINT ( 'NONE',  ( -0.8648157786182795181, 15.00000000000000000, -108.5968152657687256 ) ) ;
#6170=CARTESIAN_POINT ( 'NONE',  ( 0.2625675448779599130, 10.37192832877892101, 2.974107436473207411 ) ) ;
#6178=CARTESIAN_POINT ( 'NONE',  ( -4.238936666282000942, 10.20023565101511842, -48.01451400917154899 ) ) ;
#6180=CARTESIAN_POINT ( 'NONE',  ( 0.8127647490234470862, 12.34370856009516793, 2.588856853449111650 ) ) ;
#6182=CARTESIAN_POINT ( 'NONE',  ( -8.772031809916272849, 1.679412279786333562, -105.4401748263509262 ) ) ;
#6184=AXIS2_PLACEMENT_3D ( 'NONE', #9958, #13530, #13455 ) ;
#6185=DIRECTION ( 'NONE',  ( 0.9961255586397049777, 0.000000000000000000, -0.08794243244723005948 ) ) ;
#6186=CARTESIAN_POINT ( 'NONE',  ( 9.939878312292615092, 9.999999999999998224, -115.2320631035898373 ) ) ;
#6187=CIRCLE ( 'NONE', #13845, 14.80000000000025651 ) ;
#6193=ORIENTED_EDGE ( 'NONE', *, *, #4574, .F. ) ;
#6194=CARTESIAN_POINT ( 'NONE',  ( -5.763540231018621007, 4.336808689942017736E-16, -109.7236846929783809 ) ) ;
#6202=EDGE_CURVE ( 'NONE', #8353, #7290, #8232, .T. ) ;
#6205=CARTESIAN_POINT ( 'NONE',  ( -63.94155209071244883, 15.00000000000000000, -181.7374336199717959 ) ) ;
#6209=DIRECTION ( 'NONE',  ( 0.000000000000000000, 0.000000000000000000, 1.000000000000000000 ) ) ;
#6212=LINE ( 'NONE', #5059, #3450 ) ;
#6216=CIRCLE ( 'NONE', #1281, 3.750000000000003109 ) ;
#6226=ADVANCED_FACE ( 'NONE', ( #9283 ), #4573, .T. ) ;
#6240=CARTESIAN_POINT ( 'NONE',  ( -65.43041955727726133, 15.34010611920397160, -204.2233706068106187 ) ) ;
#6243=( BOUNDED_SURFACE ( )  B_SPLINE_SURFACE ( 3, 2, ( 
 ( #8021, #9261, #11724 ),
 ( #12746, #9106, #15233 ),
 ( #8095, #3536, #5622 ),
 ( #7944, #2377, #3383 ),
 ( #11653, #2159, #6861 ),
 ( #10566, #14136, #4625 ),
 ( #11574, #13828, #5702 ),
 ( #12819, #7075, #4698 ),
 ( #10335, #12664, #9336 ),
 ( #2227, #2308, #2080 ),
 ( #11507, #15078, #8169 ),
 ( #12973, #15302, #8245 ),
 ( #6935, #921, #1070 ),
 ( #10421, #11795, #15157 ),
 ( #13914, #1209, #4553 ),
 ( #5779, #10500, #5919 ),
 ( #14059, #3458, #12897 ),
 ( #7009, #1144, #5847 ),
 ( #10873, #13284, #3851 ),
 ( #8316, #7473, #207 ),
 ( #10958, #8548, #377 ),
 ( #2687, #6240, #9724 ),
 ( #9636, #292, #5085 ),
 ( #13207, #5007, #14454 ),
 ( #14370, #1608, #3769 ),
 ( #7386, #12025, #8473 ),
 ( #13042, #9799, #9485 ),
 ( #12108, #14210, #61 ),
 ( #2452, #14529, #1528 ),
 ( #3927, #12190, #8625 ),
 ( #4770, #6152, #10720 ),
 ( #3612, #4846, #3682 ),
 ( #13364, #1295, #7236 ),
 ( #2769, #2610, #10645 ),
 ( #7148, #11871, #5997 ),
 ( #134, #9557, #14282 ),
 ( #8392, #13124, #1447 ),
 ( #2534, #7311, #11948 ),
 ( #1373, #6075, #10793 ),
 ( #4920, #4314, #13592 ) ),
 .UNSPECIFIED., .F., .F., .F. ) 
 B_SPLINE_SURFACE_WITH_KNOTS ( ( 4, 2, 2, 2, 2, 2, 2, 2, 2, 2, 2, 2, 2, 2, 2, 2, 2, 2, 2, 4 ),
 ( 3, 3 ),
 ( -3.279975126961391755E-05, 0.006014536522838872037, 0.009038204659893115181, 0.01206187279694735832, 0.01508554093400159973, 0.01810920907105584288, 0.01962104313958296445, 0.02037696017384652697, 0.02113287720811008602, 0.02188879424237364507, 0.02226675275950542460, 0.02264471127663720759, 0.02302266979376899059, 0.02321164905233488035, 0.02340062831090077011, 0.02358960756946665988, 0.02377858682803254964, 0.02387307645731549452, 0.02396756608659843940, 0.02415654534516432916 ),
 ( 0.000000000000000000, 1.000000000000000000 ),
 .UNSPECIFIED. ) 
 GEOMETRIC_REPRESENTATION_ITEM ( )  RATIONAL_B_SPLINE_SURFACE ( (
 ( 1.000000000000000000, 1.000000000000000000, 1.000000000000000000),
 ( 1.000000000000000000, 0.9998961004008237730, 1.000000000000000000),
 ( 1.000000000000000000, 0.9981490631740187469, 1.000000000000000000),
 ( 1.000000000000000000, 0.9892551553995345692, 1.000000000000000000),
 ( 1.000000000000000000, 0.9852355408993450636, 1.000000000000000000),
 ( 1.000000000000000000, 0.9735752570600945122, 1.000000000000000000),
 ( 1.000000000000000000, 0.9659716152100031872, 1.000000000000000000),
 ( 1.000000000000000000, 0.9442171815146421787, 1.000000000000000000),
 ( 1.000000000000000000, 0.9301391107196244068, 1.000000000000000000),
 ( 1.000000000000000000, 0.8893577403784588276, 1.000000000000000000),
 ( 1.000000000000000000, 0.8629525740881984763, 1.000000000000000000),
 ( 1.000000000000000000, 0.8031463202808644120, 1.000000000000000000),
 ( 1.000000000000000000, 0.7797588792457152973, 1.000000000000000000),
 ( 1.000000000000000000, 0.7364480129656714169, 1.000000000000000000),
 ( 1.000000000000000000, 0.7206346151360477625, 1.000000000000000000),
 ( 1.000000000000000000, 0.6854091271955076170, 1.000000000000000000),
 ( 1.000000000000000000, 0.6659717199882734251, 1.000000000000000000),
 ( 1.000000000000000000, 0.6224610072577244635, 1.000000000000000000),
 ( 1.000000000000000000, 0.5983971201618294433, 1.000000000000000000),
 ( 1.000000000000000000, 0.5574794907613763728, 1.000000000000000000),
 ( 1.000000000000000000, 0.5430094399006958339, 1.000000000000000000),
 ( 1.000000000000000000, 0.5122087497860612348, 1.000000000000000000),
 ( 1.000000000000000000, 0.4959417466219665505, 1.000000000000000000),
 ( 1.000000000000000000, 0.4614524395396406575, 1.000000000000000000),
 ( 1.000000000000000000, 0.4432189288362176072, 1.000000000000000000),
 ( 1.000000000000000000, 0.4143494501494444093, 1.000000000000000000),
 ( 1.000000000000000000, 0.4045375185897135961, 1.000000000000000000),
 ( 1.000000000000000000, 0.3847318188904718661, 1.000000000000000000),
 ( 1.000000000000000000, 0.3747241291590798773, 1.000000000000000000),
 ( 1.000000000000000000, 0.3547825414681071154, 1.000000000000000000),
 ( 1.000000000000000000, 0.3447758195551594018, 1.000000000000000000),
 ( 1.000000000000000000, 0.3258420213088968898, 1.000000000000000000),
 ( 1.000000000000000000, 0.3168993536526623078, 1.000000000000000000),
 ( 1.000000000000000000, 0.3051118154061103760, 1.000000000000000000),
 ( 1.000000000000000000, 0.3014427353064685899, 1.000000000000000000),
 ( 1.000000000000000000, 0.2949341713297093381, 1.000000000000000000),
 ( 1.000000000000000000, 0.2921166433287153419, 1.000000000000000000),
 ( 1.000000000000000000, 0.2851959977589787476, 1.000000000000000000),
 ( 1.000000000000000000, 0.2826324211101104988, 1.000000000000000000),
 ( 1.000000000000000000, 0.2826388035360150597, 1.000000000000000000) ) ) 
 REPRESENTATION_ITEM ( '' )  SURFACE ( )  );
#6244=CARTESIAN_POINT ( 'NONE',  ( -8.886921396801742645, 2.500000000000000444, -105.5168766094550676 ) ) ;
#6247=CARTESIAN_POINT ( 'NONE',  ( -8.886921396801742645, 9.999999999999998224, -105.5168766094550676 ) ) ;
#6252=CARTESIAN_POINT ( 'NONE',  ( -70.11278167081923129, 10.00000000000000355, -193.2159842960370497 ) ) ;
#6257=CARTESIAN_POINT ( 'NONE',  ( -22.00712180358226533, 15.00000000000000000, -133.4290821151669206 ) ) ;
#6261=CARTESIAN_POINT ( 'NONE',  ( -4.038573370754110492, 10.62993540156934458, -45.72135289039659511 ) ) ;
#6263=CIRCLE ( 'NONE', #11923, 3.500000000000003109 ) ;
#6264=CARTESIAN_POINT ( 'NONE',  ( 3.746804550798221278, 14.90004864566718723, 1.209732483988228191 ) ) ;
#6265=CIRCLE ( 'NONE', #6509, 5.000000000000000000 ) ;
#6268=EDGE_CURVE ( 'NONE', #5826, #2801, #11677, .T. ) ;
#6272=VERTEX_POINT ( 'NONE', #15027 ) ;
#6278=AXIS2_PLACEMENT_3D ( 'NONE', #8726, #14625, #5609 ) ;
#6280=CARTESIAN_POINT ( 'NONE',  ( 2.530298019944474675, 0.000000000000000000, 0.2330448234422078380 ) ) ;
#6284=CARTESIAN_POINT ( 'NONE',  ( -69.91247589395200634, 9.999999999999998224, -187.7969989154814812 ) ) ;
#6285=DIRECTION ( 'NONE',  ( 0.05964429961207245307, -0.000000000000000000, 0.9982196940171964572 ) ) ;
#6295=ORIENTED_EDGE ( 'NONE', *, *, #8752, .T. ) ;
#6296=ORIENTED_EDGE ( 'NONE', *, *, #5808, .F. ) ;
#6301=VERTEX_POINT ( 'NONE', #5724 ) ;
#6307=CARTESIAN_POINT ( 'NONE',  ( -61.42357225889784189, 10.00000000000000000, -191.1784762114873217 ) ) ;
#6308=CARTESIAN_POINT ( 'NONE',  ( -42.66341287047314523, 15.00000000000000355, -153.0322522593145891 ) ) ;
#6312=ADVANCED_FACE ( 'NONE', ( #15254 ), #4645, .F. ) ;
#6313=EDGE_CURVE ( 'NONE', #6350, #8933, #10586, .T. ) ;
#6320=CARTESIAN_POINT ( 'NONE',  ( 7.229479027725716378, 3.133978149981274886, -23.67143487013571956 ) ) ;
#6321=CARTESIAN_POINT ( 'NONE',  ( -2.326411255686738677, 7.379999999999995453, -43.40791589983918186 ) ) ;
#6324=CARTESIAN_POINT ( 'NONE',  ( -67.62417607549662080, 11.93961266018884260, -203.5750017624773989 ) ) ;
#6325=DIRECTION ( 'NONE',  ( -0.9982196940171964572, 0.000000000000000000, 0.05964429961207245307 ) ) ;
#6329=CARTESIAN_POINT ( 'NONE',  ( -9.285933603414314064, 2.500000000000000444, -105.1819416496436759 ) ) ;
#6332=CARTESIAN_POINT ( 'NONE',  ( -7.737061903529485640, 9.999999999999998224, -106.6108512366499923 ) ) ;
#6335=DIRECTION ( 'NONE',  ( 0.000000000000000000, 1.000000000000000000, 0.000000000000000000 ) ) ;
#6339=CARTESIAN_POINT ( 'NONE',  ( -3.803791538539230022, 10.82342741786251850, -43.84832462749526627 ) ) ;
#6343=CARTESIAN_POINT ( 'NONE',  ( 1.855481649321436777, 15.00000000000000000, -35.83830032691820122 ) ) ;
#6344=ADVANCED_FACE ( 'NONE', ( #13856 ), #2499, .T. ) ;
#6348=ORIENTED_EDGE ( 'NONE', *, *, #5808, .T. ) ;
#6350=VERTEX_POINT ( 'NONE', #13541 ) ;
#6351=CARTESIAN_POINT ( 'NONE',  ( 2.961487585051517879, 2.500000000000000444, 5.117137001352175751 ) ) ;
#6360=CARTESIAN_POINT ( 'NONE',  ( -70.04737159634794352, 14.99999999999942624, -194.4639900967369783 ) ) ;
#6366=DIRECTION ( 'NONE',  ( -0.08794243244722427244, 0.000000000000000000, -0.9961255586397055328 ) ) ;
#6368=ORIENTED_EDGE ( 'NONE', *, *, #12686, .F. ) ;
#6369=DIRECTION ( 'NONE',  ( -0.4304374328763155289, 2.729281898310473032E-15, 0.9026204165532971668 ) ) ;
#6374=VERTEX_POINT ( 'NONE', #14938 ) ;
#6380=CARTESIAN_POINT ( 'NONE',  ( -76.20282042307043469, 10.00000000000000000, -188.4633497277649496 ) ) ;
#6382=DIRECTION ( 'NONE',  ( -0.08794243244722425856, 0.000000000000000000, -0.9961255586397054218 ) ) ;
#6383=VERTEX_POINT ( 'NONE', #11131 ) ;
#6387=ORIENTED_EDGE ( 'NONE', *, *, #12736, .T. ) ;
#6388=CYLINDRICAL_SURFACE ( 'NONE', #10195, 10.00000000000000888 ) ;
#6392=CARTESIAN_POINT ( 'NONE',  ( 0.1753282536233310984, 3.004541188168042609, 1.985946371125043575 ) ) ;
#6410=CARTESIAN_POINT ( 'NONE',  ( 0.1512094758773736836, 2.824932260968233244, 1.712752529570608306 ) ) ;
#6412=CARTESIAN_POINT ( 'NONE',  ( 5.091575966645542017, 10.00000000000000000, -108.2758494551189301 ) ) ;
#6417=CARTESIAN_POINT ( 'NONE',  ( 4.586756373948227328, 1.218752542932547250E-31, -116.5615908754608085 ) ) ;
#6418=CARTESIAN_POINT ( 'NONE',  ( -40.71937926015205278, 15.00000000000067324, -157.6611590844978252 ) ) ;
#6421=ORIENTED_EDGE ( 'NONE', *, *, #6313, .T. ) ;
#6432=CARTESIAN_POINT ( 'NONE',  ( 28.21756277010331004, 6.321094445766561876, -25.21174485404201704 ) ) ;
#6437=CIRCLE ( 'NONE', #12606, 3.500000000000003109 ) ;
#6442=EDGE_LOOP ( 'NONE', ( #214, #2567, #9073 ) ) ;
#6452=CARTESIAN_POINT ( 'NONE',  ( -6.951659142864632379, 14.04257511106687240, -104.5073459644900709 ) ) ;
#6455=EDGE_CURVE ( 'NONE', #2289, #9845, #9231, .T. ) ;
#6457=ORIENTED_EDGE ( 'NONE', *, *, #13557, .T. ) ;
#6466=CARTESIAN_POINT ( 'NONE',  ( -49.26721305452313260, 10.00000000000000178, -156.1716796081737471 ) ) ;
#6467=CARTESIAN_POINT ( 'NONE',  ( 0.2625675447228704718, 4.835792971051144917, 2.974107434716409148 ) ) ;
#6477=CARTESIAN_POINT ( 'NONE',  ( -32.22662898424438538, 9.999999999999998224, -135.0284069691736306 ) ) ;
#6481=AXIS2_PLACEMENT_3D ( 'NONE', #1708, #13628, #12297 ) ;
#6482=LINE ( 'NONE', #12206, #11434 ) ;
#6489=CARTESIAN_POINT ( 'NONE',  ( 8.602948156611530450, 9.999999999999998224, -113.5765336190000738 ) ) ;
#6498=DESIGN_CONTEXT ( 'detailed design', #590, 'design' ) ;
#6500=CARTESIAN_POINT ( 'NONE',  ( -34.35934156841198472, 15.00000000000000000, -156.1669470276411289 ) ) ;
#6501=EDGE_CURVE ( 'NONE', #5223, #8123, #13497, .T. ) ;
#6507=DIRECTION ( 'NONE',  ( -1.076984184057255207E-17, 1.000000000000000000, -1.219901976936984353E-16 ) ) ;
#6509=AXIS2_PLACEMENT_3D ( 'NONE', #7452, #7368, #2898 ) ;
#6510=CARTESIAN_POINT ( 'NONE',  ( -15.73004658022870927, 0.000000000000000000, -131.7446186346720367 ) ) ;
#6512=DIRECTION ( 'NONE',  ( -0.9961255586397050887, 0.000000000000000000, 0.08794243244723005948 ) ) ;
#6516=CARTESIAN_POINT ( 'NONE',  ( -5.192805064198273257, 10.00000000000000178, -111.6595894180993582 ) ) ;
#6520=CARTESIAN_POINT ( 'NONE',  ( 2.543998210651924552, 5.000000000000000888, -136.5336064733039620 ) ) ;
#6522=CARTESIAN_POINT ( 'NONE',  ( -17.32624372123753886, 9.999999999999998224, -129.3796757791584753 ) ) ;
#6524=CARTESIAN_POINT ( 'NONE',  ( -9.240119717576689595, 9.999999999999998224, -104.6630069175297564 ) ) ;
#6535=DIRECTION ( 'NONE',  ( -0.08794243244722425856, -0.000000000000000000, -0.9961255586397054218 ) ) ;
#6536=DIRECTION ( 'NONE',  ( -0.000000000000000000, 1.000000000000000000, -0.000000000000000000 ) ) ;
#6539=VERTEX_POINT ( 'NONE', #3386 ) ;
#6547=CARTESIAN_POINT ( 'NONE',  ( -60.91137729732987793, 10.00000000000000178, -175.0198515626273661 ) ) ;
#6548=CARTESIAN_POINT ( 'NONE',  ( 0.2167269470765707806, 3.467221422101828043, 2.454870137451500067 ) ) ;
#6553=VERTEX_POINT ( 'NONE', #2162 ) ;
#6554=CARTESIAN_POINT ( 'NONE',  ( 3.230086961373112242, 9.999999999999998224, 5.208283729180105404 ) ) ;
#6557=CARTESIAN_POINT ( 'NONE',  ( -8.241439964509023497, 9.999999999999998224, -106.0832790697715495 ) ) ;
#6564=CARTESIAN_POINT ( 'NONE',  ( -13.42077998717343057, 7.499999999999991118, -89.47651029354803143 ) ) ;
#6566=CARTESIAN_POINT ( 'NONE',  ( -3.782526895735886630, 9.999999999999996447, -42.84475209785864536 ) ) ;
#6570=CARTESIAN_POINT ( 'NONE',  ( 7.427446726622314976, 7.321094445766561876, -26.41501464507892294 ) ) ;
#6574=CARTESIAN_POINT ( 'NONE',  ( -30.85915506344845483, 9.999999999999998224, -156.4241655052078954 ) ) ;
#6587=CARTESIAN_POINT ( 'NONE',  ( -18.09353981420494151, 5.000000000000000000, -129.3374956033359240 ) ) ;
#6588=ADVANCED_FACE ( 'NONE', ( #10569, #6938 ), #3462, .T. ) ;
#6589=EDGE_CURVE ( 'NONE', #9845, #12491, #596, .T. ) ;
#6590=DIRECTION ( 'NONE',  ( 0.000000000000000000, -1.000000000000000000, 0.000000000000000000 ) ) ;
#6594=LINE ( 'NONE', #11382, #9481 ) ;
#6596=CARTESIAN_POINT ( 'NONE',  ( -1.141970775756692369, 8.673617379884035472E-16, -133.1539114526842695 ) ) ;
#6612=CARTESIAN_POINT ( 'NONE',  ( 7.788671722263534214, 5.321094445766561876, -20.36947622874119546 ) ) ;
#6622=ORIENTED_EDGE ( 'NONE', *, *, #14045, .F. ) ;
#6626=CARTESIAN_POINT ( 'NONE',  ( -63.21422130130007133, 10.00000000000000178, -203.6040552426024988 ) ) ;
#6627=CARTESIAN_POINT ( 'NONE',  ( 2.998665091981967734, 1.009082376855201968, 3.243864481526151256 ) ) ;
#6631=VERTEX_POINT ( 'NONE', #14139 ) ;
#6632=CARTESIAN_POINT ( 'NONE',  ( -35.09122780324831581, 15.00000000000000178, -151.1986770539716076 ) ) ;
#6635=CIRCLE ( 'NONE', #15051, 2.250000000000005773 ) ;
#6636=CARTESIAN_POINT ( 'NONE',  ( -8.645680077366938221, 4.728706406862280561E-12, -122.8677831019022619 ) ) ;
#6641=CARTESIAN_POINT ( 'NONE',  ( 0.4711736884522539359, 9.999999999999998224, 5.336993082470237404 ) ) ;
#6649=CARTESIAN_POINT ( 'NONE',  ( -40.43640613370507708, 9.999999999999998224, -157.5381262016859125 ) ) ;
#6652=VERTEX_POINT ( 'NONE', #6244 ) ;
#6653=CARTESIAN_POINT ( 'NONE',  ( -10.59890792400177695, 9.999999999999998224, -125.3997871707501446 ) ) ;
#6654=DIRECTION ( 'NONE',  ( 0.08794243244722427244, 0.000000000000000000, 0.9961255586397054218 ) ) ;
#6661=CARTESIAN_POINT ( 'NONE',  ( -63.31459619122251326, 14.99999999999999822, -201.9013287080907162 ) ) ;
#6666=CARTESIAN_POINT ( 'NONE',  ( 4.912745175218361737, 14.82122587924934187, -0.1997555194214963581 ) ) ;
#6668=CARTESIAN_POINT ( 'NONE',  ( 6.363274845737939778, 8.673617379884035472E-16, -132.2089327231069547 ) ) ;
#6670=VERTEX_POINT ( 'NONE', #6078 ) ;
#6678=VERTEX_POINT ( 'NONE', #13524 ) ;
#6682=AXIS2_PLACEMENT_3D ( 'NONE', #8063, #12787, #4593 ) ;
#6684=FACE_OUTER_BOUND ( 'NONE', #6011, .T. ) ;
#6719=CARTESIAN_POINT ( 'NONE',  ( -3.849925124627588069, 4.336808689942017736E-16, -119.3240804248890612 ) ) ;
#6725=DIRECTION ( 'NONE',  ( -0.9961255586397056438, 0.000000000000000000, 0.08794243244722428632 ) ) ;
#6726=CARTESIAN_POINT ( 'NONE',  ( -33.77251566124539295, 15.00000000000000000, -156.1614337058108788 ) ) ;
#6729=CARTESIAN_POINT ( 'NONE',  ( -12.27209645382210113, 15.00000000000000000, -127.2227734861304782 ) ) ;
#6735=CARTESIAN_POINT ( 'NONE',  ( -4.924771681124648026, 0.000000000000000000, -137.0932397189673111 ) ) ;
#6740=CARTESIAN_POINT ( 'NONE',  ( -5.325284192974351960, 14.84655678240134868, -103.7367053080723593 ) ) ;
#6743=CARTESIAN_POINT ( 'NONE',  ( -5.388443496774984354, 10.00000000000000178, -115.7979535283634931 ) ) ;
#6746=CARTESIAN_POINT ( 'NONE',  ( 3.226485357636315499, 4.342686168579469097, 5.175911514346425157 ) ) ;
#6747=CARTESIAN_POINT ( 'NONE',  ( 9.939878312292615092, 5.000000000000000888, -115.2320631035898373 ) ) ;
#6748=EDGE_LOOP ( 'NONE', ( #8201, #4016, #14040, #8767 ) ) ;
#6758=CARTESIAN_POINT ( 'NONE',  ( -7.646413850410871405, 13.39228090183835285, -104.8572026217608482 ) ) ;
#6759=EDGE_CURVE ( 'NONE', #10593, #1043, #9903, .T. ) ;
#6760=( NAMED_UNIT ( * ) SI_UNIT ( $, .STERADIAN. ) SOLID_ANGLE_UNIT ( ) );
#6761=AXIS2_PLACEMENT_3D ( 'NONE', #12194, #9803, #6158 ) ;
#6765=FACE_OUTER_BOUND ( 'NONE', #1736, .T. ) ;
#6775=AXIS2_PLACEMENT_3D ( 'NONE', #12947, #9376, #3590 ) ;
#6781=EDGE_CURVE ( 'NONE', #2896, #8666, #8471, .T. ) ;
#6785=CIRCLE ( 'NONE', #14704, 11.99999999999995559 ) ;
#6793=CARTESIAN_POINT ( 'NONE',  ( -1.813969075506799422, 7.379999999999995453, -48.97454890480479861 ) ) ;
#6798=EDGE_LOOP ( 'NONE', ( #1641, #7056, #13182, #301 ) ) ;
#6800=CARTESIAN_POINT ( 'NONE',  ( -59.92301775443486633, 15.00000000000000000, -171.2216082921338227 ) ) ;
#6802=ORIENTED_EDGE ( 'NONE', *, *, #12814, .T. ) ;
#6803=CARTESIAN_POINT ( 'NONE',  ( -10.59890792386395475, 14.99999999999880629, -125.3997871708591703 ) ) ;
#6804=CARTESIAN_POINT ( 'NONE',  ( 6.089666224640344794, 15.00000000000000000, -124.6062682140657074 ) ) ;
#6808=DIRECTION ( 'NONE',  ( -0.08794243244722427244, 0.000000000000000000, -0.9961255586397055328 ) ) ;
#6810=DIRECTION ( 'NONE',  ( 0.08794243244722427244, 0.000000000000000000, 0.9961255586397055328 ) ) ;
#6811=LINE ( 'NONE', #9207, #12848 ) ;
#6815=CARTESIAN_POINT ( 'NONE',  ( 3.212062097439680741, 3.696815382486504653, 5.047156548192035963 ) ) ;
#6817=EDGE_LOOP ( 'NONE', ( #2512, #9442, #10931, #10854 ) ) ;
#6823=CARTESIAN_POINT ( 'NONE',  ( -8.602511405380996123, 2.500000000000000444, -105.7492080835845485 ) ) ;
#6827=CARTESIAN_POINT ( 'NONE',  ( -8.357321192833575552, 12.30945435311018521, -105.2297795656583759 ) ) ;
#6854=EDGE_LOOP ( 'NONE', ( #11660, #3670, #14559, #10602 ) ) ;
#6858=ADVANCED_FACE ( 'NONE', ( #5604 ), #7775, .F. ) ;
#6861=CARTESIAN_POINT ( 'NONE',  ( -65.78451708959967448, 14.92583229181892612, -188.0906790823463268 ) ) ;
#6862=CARTESIAN_POINT ( 'NONE',  ( 0.7644969749118040170, 5.000000000000000000, -138.4027240657576101 ) ) ;
#6864=CARTESIAN_POINT ( 'NONE',  ( -10.02475322368603194, 5.000000000000000000, -286.9457450322071281 ) ) ;
#6866=DIRECTION ( 'NONE',  ( 0.9207838613340401102, 0.000000000000000000, -0.3900731735287307211 ) ) ;
#6870=CARTESIAN_POINT ( 'NONE',  ( -60.74056104668384393, 9.999999999999998224, -188.2485173983553466 ) ) ;
#6873=CARTESIAN_POINT ( 'NONE',  ( 3.136841903360911843, 5.000000000000000888, -104.4936450199714812 ) ) ;
#6881=DIRECTION ( 'NONE',  ( -0.05964429961207245307, 0.000000000000000000, -0.9982196940171964572 ) ) ;
#6884=CYLINDRICAL_SURFACE ( 'NONE', #6028, 3.500000000000013323 ) ;
#6886=DIRECTION ( 'NONE',  ( 0.000000000000000000, -1.000000000000000000, 0.000000000000000000 ) ) ;
#6889=ORIENTED_EDGE ( 'NONE', *, *, #224, .F. ) ;
#6893=CARTESIAN_POINT ( 'NONE',  ( -6.488009013026156957, 4.336808689942017736E-16, -104.2969138198227910 ) ) ;
#6896=CARTESIAN_POINT ( 'NONE',  ( -47.48189921986828921, 15.00000000000000000, -141.5723758807981483 ) ) ;
#6898=CARTESIAN_POINT ( 'NONE',  ( -8.659743771704308202, 12.30945435306794877, -104.4813518601836790 ) ) ;
#6904=CYLINDRICAL_SURFACE ( 'NONE', #4206, 3.000000000000002665 ) ;
#6906=DIRECTION ( 'NONE',  ( -0.000000000000000000, 1.000000000000000000, -0.000000000000000000 ) ) ;
#6918=AXIS2_PLACEMENT_3D ( 'NONE', #11916, #6045, #14652 ) ;
#6924=AXIS2_PLACEMENT_3D ( 'NONE', #12, #10674, #1100 ) ;
#6927=VECTOR ( 'NONE', #10209, 1000.000000000000000 ) ;
#6935=CARTESIAN_POINT ( 'NONE',  ( -64.60583417973334974, 13.85924130109725283, -199.3306212659461494 ) ) ;
#6936=CARTESIAN_POINT ( 'NONE',  ( -0.8169061489538727017, 1.565995602528241992, -138.1029328351367553 ) ) ;
#6938=FACE_OUTER_BOUND ( 'NONE', #1919, .T. ) ;
#6947=CARTESIAN_POINT ( 'NONE',  ( -68.00022065852073183, 15.00000000000000000, -200.6045152126381197 ) ) ;
#6964=EDGE_CURVE ( 'NONE', #11483, #14924, #2560, .T. ) ;
#6967=CARTESIAN_POINT ( 'NONE',  ( 3.221353676048400061, 14.96825566296426935, -12.98096750502963381 ) ) ;
#6968=CARTESIAN_POINT ( 'NONE',  ( -63.60348060676458459, 15.00000000000000000, -180.2685449772604045 ) ) ;
#6970=ORIENTED_EDGE ( 'NONE', *, *, #625, .F. ) ;
#6974=CARTESIAN_POINT ( 'NONE',  ( 4.047901359262597865, 14.99999999996766675, -106.4041221357216216 ) ) ;
#6979=B_SPLINE_CURVE_WITH_KNOTS ( 'NONE', 3,
 ( #4963, #7110, #410, #249, #9678, #14409, #14324, #1412, #3649, #2650 ),
 .UNSPECIFIED., .F., .F.,
 ( 4, 2, 2, 2, 4 ),
 ( 0.002313672523134014964, 0.002886887860852135976, 0.003460103198570256555, 0.004033318536288377568, 0.004606533874006498580 ),
 .UNSPECIFIED. ) ;
#6980=CARTESIAN_POINT ( 'NONE',  ( -8.201734205038356151, 12.60136528525868371, -105.1471006946589881 ) ) ;
#6987=CARTESIAN_POINT ( 'NONE',  ( -0.8709518826452680162, 14.99999999999999645, -118.3049497858321217 ) ) ;
#6994=ORIENTED_EDGE ( 'NONE', *, *, #15170, .T. ) ;
#7000=FACE_OUTER_BOUND ( 'NONE', #13338, .T. ) ;
#7009=CARTESIAN_POINT ( 'NONE',  ( -64.01558189167985802, 12.98106818083026681, -201.5482190537578902 ) ) ;
#7010=CARTESIAN_POINT ( 'NONE',  ( 0.7195110302018304926, 4.291397982413823975, -138.3948393236508139 ) ) ;
#7013=CARTESIAN_POINT ( 'NONE',  ( -2.691470893477765802, 4.336808689942017736E-16, -114.7599528768529495 ) ) ;
#7020=CARTESIAN_POINT ( 'NONE',  ( -6.683304552674627530, 4.336808689942017736E-16, -104.1296019027812179 ) ) ;
#7022=VERTEX_POINT ( 'NONE', #3516 ) ;
#7023=CARTESIAN_POINT ( 'NONE',  ( -6.708306528330162166, 9.999999999999998224, -119.6038561065980446 ) ) ;
#7035=CARTESIAN_POINT ( 'NONE',  ( 2.700353918670075792, 15.00000000003971223, -24.42150847873306319 ) ) ;
#7036=CARTESIAN_POINT ( 'NONE',  ( 7.353370788917347411, 9.030812432661041239E-12, -111.8370434415751475 ) ) ;
#7038=ORIENTED_EDGE ( 'NONE', *, *, #12446, .F. ) ;
#7042=CARTESIAN_POINT ( 'NONE',  ( 3.136841903360914952, 15.00000000000000711, -104.4936450199714812 ) ) ;
#7043=VERTEX_POINT ( 'NONE', #4605 ) ;
#7045=( BOUNDED_SURFACE ( )  B_SPLINE_SURFACE ( 3, 2, ( 
 ( #8414, #2632, #7334 ),
 ( #12287, #1697, #6178 ),
 ( #313, #8651, #1394 ),
 ( #545, #9746, #3706 ),
 ( #5104, #228, #3871 ),
 ( #7259, #9894, #13147 ),
 ( #4029, #2556, #12045 ),
 ( #5027, #6097, #14474 ),
 ( #10812, #6261, #4944 ),
 ( #9659, #13305, #2707 ),
 ( #13385, #12132, #1548 ),
 ( #10978, #395, #8733 ),
 ( #2790, #7492, #13466 ),
 ( #12211, #1626, #6339 ),
 ( #11053, #12588, #699 ),
 ( #11278, #2081, #12438 ),
 ( #1778, #13616, #5404 ),
 ( #14782, #10201, #6566 ) ),
 .UNSPECIFIED., .F., .F., .T. ) 
 B_SPLINE_SURFACE_WITH_KNOTS ( ( 4, 2, 2, 2, 2, 2, 2, 2, 4 ),
 ( 3, 3 ),
 ( 0.000000000000000000, 0.0007443649107546155674, 0.001488729821509231135, 0.002233094732263846485, 0.002977459643018462269, 0.003721824553773077620, 0.004466189464527692971, 0.005210554375282308755, 0.005954919286036924539 ),
 ( 0.000000000000000000, 1.000000000000000000 ),
 .UNSPECIFIED. ) 
 GEOMETRIC_REPRESENTATION_ITEM ( )  RATIONAL_B_SPLINE_SURFACE ( (
 ( 1.000000000000000000, 0.7071067811865460184, 1.000000000000000000),
 ( 1.000000000000000000, 0.6972119573952525462, 1.000000000000000000),
 ( 1.000000000000000000, 0.6862390331242504971, 1.000000000000000000),
 ( 1.000000000000000000, 0.6643322149117374398, 1.000000000000000000),
 ( 1.000000000000000000, 0.6532829606877528228, 1.000000000000000000),
 ( 1.000000000000000000, 0.6342007904900059945, 1.000000000000000000),
 ( 1.000000000000000000, 0.6261622867538135795, 1.000000000000000000),
 ( 1.000000000000000000, 0.6149761046979081991, 1.000000000000000000),
 ( 1.000000000000000000, 0.6119284778760083476, 1.000000000000000000),
 ( 1.000000000000000000, 0.6119088882623058279, 1.000000000000000000),
 ( 1.000000000000000000, 0.6148452971779246878, 1.000000000000000000),
 ( 1.000000000000000000, 0.6260511252444348473, 1.000000000000000000),
 ( 1.000000000000000000, 0.6341360142629537400, 1.000000000000000000),
 ( 1.000000000000000000, 0.6531158155794938303, 1.000000000000000000),
 ( 1.000000000000000000, 0.6641411866188042801, 1.000000000000000000),
 ( 1.000000000000000000, 0.6862036393175137139, 1.000000000000000000),
 ( 1.000000000000000000, 0.6972164765192375713, 1.000000000000000000),
 ( 1.000000000000000000, 0.7071067811865491270, 1.000000000000000000) ) ) 
 REPRESENTATION_ITEM ( '' )  SURFACE ( )  );
#7052=CARTESIAN_POINT ( 'NONE',  ( 0.7644969749118040170, 5.000000000000000000, -138.4027240657576101 ) ) ;
#7053=ORIENTED_EDGE ( 'NONE', *, *, #9281, .T. ) ;
#7056=ORIENTED_EDGE ( 'NONE', *, *, #9712, .T. ) ;
#7066=CARTESIAN_POINT ( 'NONE',  ( -7.011153618232597751, 0.01937457977056467398, -104.1953234560537425 ) ) ;
#7070=CARTESIAN_POINT ( 'NONE',  ( -50.03010188096263988, 15.00000000000000000, -151.4930374104633870 ) ) ;
#7071=VERTEX_POINT ( 'NONE', #13968 ) ;
#7074=PLANE ( 'NONE',  #4465 ) ;
#7075=CARTESIAN_POINT ( 'NONE',  ( -66.00101815392289950, 14.98497452121014994, -193.2201357435544082 ) ) ;
#7080=CARTESIAN_POINT ( 'NONE',  ( 4.856804767890306351, 14.90536770052033866, -1.840041787218210878 ) ) ;
#7084=CARTESIAN_POINT ( 'NONE',  ( -60.56192452144297533, 9.999999999999998224, -187.5450233986887554 ) ) ;
#7088=CARTESIAN_POINT ( 'NONE',  ( -7.119867912863494297, 15.00000000000182077, -107.3464651433156121 ) ) ;
#7089=CARTESIAN_POINT ( 'NONE',  ( -28.38930394846591909, 15.00000000000000000, -151.9126338648069918 ) ) ;
#7090=CARTESIAN_POINT ( 'NONE',  ( -19.94423925787078034, 15.00000000000000000, -150.2885610952392881 ) ) ;
#7096=CARTESIAN_POINT ( 'NONE',  ( 0.7644969749118040170, 5.000000000000000000, -138.4027240657576101 ) ) ;
#7098=DIRECTION ( 'NONE',  ( 0.05964429961207245307, 0.000000000000000000, 0.9982196940171964572 ) ) ;
#7103=CARTESIAN_POINT ( 'NONE',  ( 8.595858757291594543, 5.000000000000000888, -113.5677547687719624 ) ) ;
#7105=ORIENTED_EDGE ( 'NONE', *, *, #9905, .T. ) ;
#7106=CARTESIAN_POINT ( 'NONE',  ( -7.218906882678753689, 2.645201729013087203E-12, -107.2047439206050399 ) ) ;
#7110=CARTESIAN_POINT ( 'NONE',  ( -17.43524186648903296, 0.7231160150647996110, -130.1141235465726425 ) ) ;
#7111=ORIENTED_EDGE ( 'NONE', *, *, #997, .T. ) ;
#7113=CARTESIAN_POINT ( 'NONE',  ( -49.70557948973527118, 9.999999999999998224, -143.6055563701139306 ) ) ;
#7119=ORIENTED_EDGE ( 'NONE', *, *, #1205, .F. ) ;
#7122=CARTESIAN_POINT ( 'NONE',  ( 0.4711736884522539359, 9.999999999999998224, 5.336993082470237404 ) ) ;
#7124=VERTEX_POINT ( 'NONE', #3828 ) ;
#7126=( BOUNDED_CURVE ( )  B_SPLINE_CURVE ( 3, ( #7487, #14986, #464, #12570 ),
 .UNSPECIFIED., .F., .F. ) 
 B_SPLINE_CURVE_WITH_KNOTS ( ( 4, 4 ),
 ( 3.460670697713912336, 3.568893446053258867 ),
 .UNSPECIFIED. ) 
 CURVE ( )  GEOMETRIC_REPRESENTATION_ITEM ( )  RATIONAL_B_SPLINE_CURVE ( ( 1.000000000000000000, 0.9990242245225531281, 0.9990242245225531281, 1.000000000000000000 ) ) 
 REPRESENTATION_ITEM ( '' )  );
#7134=CARTESIAN_POINT ( 'NONE',  ( -5.208811060977222240, 2.500000000000000888, -111.9226923171489432 ) ) ;
#7139=EDGE_CURVE ( 'NONE', #9693, #6034, #6265, .T. ) ;
#7143=AXIS2_PLACEMENT_3D ( 'NONE', #14025, #817, #5520 ) ;
#7148=CARTESIAN_POINT ( 'NONE',  ( -63.24235068824187067, 10.57596889784981720, -203.5428763147797611 ) ) ;
#7151=AXIS2_PLACEMENT_3D ( 'NONE', #8966, #6725, #785 ) ;
#7153=VECTOR ( 'NONE', #5519, 1000.000000000000227 ) ;
#7156=CARTESIAN_POINT ( 'NONE',  ( 0.7552767017137625993, 15.00000000000000178, -110.7727649483667989 ) ) ;
#7161=DIRECTION ( 'NONE',  ( -0.000000000000000000, -1.000000000000000000, -0.000000000000000000 ) ) ;
#7165=CARTESIAN_POINT ( 'NONE',  ( -0.4878245559413970089, 15.00000000000000000, -109.9489936375345280 ) ) ;
#7166=CARTESIAN_POINT ( 'NONE',  ( 0.7827419278469371910, 12.28707364804876612, 2.610748976233180585 ) ) ;
#7167=CARTESIAN_POINT ( 'NONE',  ( 10.01939027896081669, 9.999999999999998224, -127.6977514918621637 ) ) ;
#7174=CARTESIAN_POINT ( 'NONE',  ( 2.957952336870751875, 14.53460293439382767, 0.6370940153772954861 ) ) ;
#7176=CARTESIAN_POINT ( 'NONE',  ( -8.814455821404541425, 1.837399608813588214, -105.4684601932094665 ) ) ;
#7179=CARTESIAN_POINT ( 'NONE',  ( -5.397979047513929984, 14.84615269367921719, -103.5376357543976980 ) ) ;
#7180=CARTESIAN_POINT ( 'NONE',  ( -63.23328683196935174, 10.53727328510970551, -203.5631487748948700 ) ) ;
#7181=ORIENTED_EDGE ( 'NONE', *, *, #14293, .F. ) ;
#7184=CARTESIAN_POINT ( 'NONE',  ( -5.137754182254912649, 2.500000000000000444, -114.0283549521523696 ) ) ;
#7195=CARTESIAN_POINT ( 'NONE',  ( -68.83694965420261269, 15.00000000000000000, -180.7144811896928331 ) ) ;
#7199=CARTESIAN_POINT ( 'NONE',  ( 20.38723710659885313, 7.321094445766561876, -31.17704722822712426 ) ) ;
#7208=ORIENTED_EDGE ( 'NONE', *, *, #9025, .F. ) ;
#7218=CARTESIAN_POINT ( 'NONE',  ( -7.952046529484080750, 0.3056169037709979275, -104.3879148205416385 ) ) ;
#7219=CARTESIAN_POINT ( 'NONE',  ( -53.86916490710522964, 10.00000000000000355, -170.7116325868586557 ) ) ;
#7220=CARTESIAN_POINT ( 'NONE',  ( -49.62396416653276532, 15.00000000000000178, -157.5220014270338424 ) ) ;
#7224=CARTESIAN_POINT ( 'NONE',  ( -63.60348060676458459, 15.00000000000000000, -180.2685449772604045 ) ) ;
#7226=ORIENTED_EDGE ( 'NONE', *, *, #10165, .F. ) ;
#7228=CARTESIAN_POINT ( 'NONE',  ( -6.435381799839732686, 9.999999999999998224, -129.7490639376177626 ) ) ;
#7235=EDGE_CURVE ( 'NONE', #11957, #12332, #10457, .T. ) ;
#7236=CARTESIAN_POINT ( 'NONE',  ( -67.59193506824016140, 10.78987469597949556, -204.3712682500590176 ) ) ;
#7243=AXIS2_PLACEMENT_3D ( 'NONE', #6351, #12225, #5271 ) ;
#7247=CARTESIAN_POINT ( 'NONE',  ( -69.15427381923166195, 9.999999999999998224, -182.3943105425532281 ) ) ;
#7250=CARTESIAN_POINT ( 'NONE',  ( -5.541218901405696506, 15.00000000000060929, -110.3933575420945630 ) ) ;
#7251=CARTESIAN_POINT ( 'NONE',  ( 2.088366663672936774, 13.96978715545234095, 1.558942282566567972 ) ) ;
#7252=CARTESIAN_POINT ( 'NONE',  ( -14.37903708479884557, 14.99999999998933120, -152.3617959900740289 ) ) ;
#7254=VECTOR ( 'NONE', #2299, 1000.000000000000114 ) ;
#7256=EDGE_CURVE ( 'NONE', #5560, #6301, #13193, .T. ) ;
#7259=CARTESIAN_POINT ( 'NONE',  ( -3.517668735334777530, 10.45885036913166033, -46.62850106167113040 ) ) ;
#7261=CARTESIAN_POINT ( 'NONE',  ( 1.128730403528703130, 12.89415287894916595, 2.354358630481084624 ) ) ;
#7262=DIRECTION ( 'NONE',  ( 0.9961255586397050887, -0.000000000000000000, -0.08794243244723005948 ) ) ;
#7267=DIRECTION ( 'NONE',  ( -0.05964429961207245307, 0.000000000000000000, -0.9982196940171964572 ) ) ;
#7268=ORIENTED_EDGE ( 'NONE', *, *, #12215, .F. ) ;
#7271=CARTESIAN_POINT ( 'NONE',  ( -2.708352249312388160, 0.000000000000000000, -111.7675805608782014 ) ) ;
#7275=CARTESIAN_POINT ( 'NONE',  ( -18.09353981420494151, 5.000000000000000000, -129.3374956033359240 ) ) ;
#7279=CARTESIAN_POINT ( 'NONE',  ( -69.93026694898610174, 15.00000000000057554, -195.9981257600232993 ) ) ;
#7286=ORIENTED_EDGE ( 'NONE', *, *, #10264, .T. ) ;
#7290=VERTEX_POINT ( 'NONE', #12247 ) ;
#7295=ORIENTED_EDGE ( 'NONE', *, *, #10937, .T. ) ;
#7296=CARTESIAN_POINT ( 'NONE',  ( 0.2625675448779695720, 15.00000000000000000, 2.974107436473219401 ) ) ;
#7298=CARTESIAN_POINT ( 'NONE',  ( -5.787114392161415211, 2.500000000000000444, -109.6579705534062157 ) ) ;
#7299=CARTESIAN_POINT ( 'NONE',  ( -45.48687283825000804, 9.999999999999996447, -160.5939636279570948 ) ) ;
#7300=CARTESIAN_POINT ( 'NONE',  ( -47.48189921986827500, 5.000000000000000888, -141.5723758807981483 ) ) ;
#7311=CARTESIAN_POINT ( 'NONE',  ( -63.88640454979729100, 11.48906216229545585, -211.3082455422185433 ) ) ;
#7312=DIRECTION ( 'NONE',  ( 0.000000000000000000, 0.000000000000000000, -1.000000000000000000 ) ) ;
#7319=EDGE_LOOP ( 'NONE', ( #12747, #8684, #8050, #1830 ) ) ;
#7324=CARTESIAN_POINT ( 'NONE',  ( -60.01991856039841622, 10.00000000000000000, -157.4353610330038009 ) ) ;
#7327=CARTESIAN_POINT ( 'NONE',  ( -6.178332509794770999, 14.99999999999909051, -118.3334666057659916 ) ) ;
#7330=CARTESIAN_POINT ( 'NONE',  ( -3.942526376278688627, 15.00000000000000000, -136.1336533158506370 ) ) ;
#7331=DIRECTION ( 'NONE',  ( 0.000000000000000000, 0.000000000000000000, -1.000000000000000000 ) ) ;
#7334=CARTESIAN_POINT ( 'NONE',  ( -4.254413237569943718, 9.999999999999998224, -48.18981741835666099 ) ) ;
#7336=CARTESIAN_POINT ( 'NONE',  ( 3.700411912290352490, 12.62857015470723177, 4.325284914432235617 ) ) ;
#7338=CARTESIAN_POINT ( 'NONE',  ( -8.338108546337810623, 0.8313257340310024057, -105.1551276366440248 ) ) ;
#7340=CARTESIAN_POINT ( 'NONE',  ( 2.850044070969222076, 9.999999999999998224, -103.0233998225063345 ) ) ;
#7345=ORIENTED_EDGE ( 'NONE', *, *, #14826, .T. ) ;
#7348=CARTESIAN_POINT ( 'NONE',  ( -5.346294835628299325, 2.500000000000000444, -111.0961406517456993 ) ) ;
#7352=CARTESIAN_POINT ( 'NONE',  ( 7.788671722263528885, 7.321094445766561876, -20.36947622874119546 ) ) ;
#7353=ORIENTED_EDGE ( 'NONE', *, *, #2711, .F. ) ;
#7357=CARTESIAN_POINT ( 'NONE',  ( -69.93026694944160226, 9.999999999999998224, -195.9981257600672677 ) ) ;
#7364=ORIENTED_EDGE ( 'NONE', *, *, #7971, .F. ) ;
#7366=ORIENTED_EDGE ( 'NONE', *, *, #1022, .F. ) ;
#7368=DIRECTION ( 'NONE',  ( -0.4304374328763156954, 0.000000000000000000, 0.9026204165532970558 ) ) ;
#7375=CARTESIAN_POINT ( 'NONE',  ( -8.969994997769484613, 1.369616766891445847, -104.6043171117432706 ) ) ;
#7379=FACE_BOUND ( 'NONE', #9443, .T. ) ;
#7385=EDGE_CURVE ( 'NONE', #6553, #2743, #10431, .T. ) ;
#7386=CARTESIAN_POINT ( 'NONE',  ( -63.45039389062857538, 11.65026692810642750, -203.0695002964987452 ) ) ;
#7392=CARTESIAN_POINT ( 'NONE',  ( -66.38120458380359423, 14.83440734456928567, -190.9480611771427618 ) ) ;
#7397=CARTESIAN_POINT ( 'NONE',  ( -8.310659720356554203, 0.7968074792153430064, -105.1373346920393885 ) ) ;
#7401=DIRECTION ( 'NONE',  ( 0.000000000000000000, 0.000000000000000000, 1.000000000000000000 ) ) ;
#7410=CARTESIAN_POINT ( 'NONE',  ( 0.1382019290192771088, 2.747583163733381184, 1.565415805761777301 ) ) ;
#7412=CARTESIAN_POINT ( 'NONE',  ( 4.571546931304953709, 14.29157444506172681, 2.042986306426028076 ) ) ;
#7417=CARTESIAN_POINT ( 'NONE',  ( -66.44604053271804389, 5.000000000000000000, -157.9117883361228394 ) ) ;
#7425=CARTESIAN_POINT ( 'NONE',  ( -8.886921396801742645, 15.00000000000000000, -105.5168766094550676 ) ) ;
#7430=CARTESIAN_POINT ( 'NONE',  ( 3.136841903360915396, 9.999999999999998224, -104.4936450199714955 ) ) ;
#7431=EDGE_LOOP ( 'NONE', ( #13199, #12501, #9945, #4467 ) ) ;
#7436=CARTESIAN_POINT ( 'NONE',  ( -64.76906036157818392, 9.999999999999998224, -167.3305518093513058 ) ) ;
#7449=AXIS2_PLACEMENT_3D ( 'NONE', #9001, #2840, #8700 ) ;
#7452=CARTESIAN_POINT ( 'NONE',  ( -1.376260179405571993, 5.000000000000000000, -106.6458321843530541 ) ) ;
#7462=CARTESIAN_POINT ( 'NONE',  ( -46.92959355634174301, 10.00000000000000355, -161.8336071854139959 ) ) ;
#7473=CARTESIAN_POINT ( 'NONE',  ( -65.57061560049943694, 15.27140727398749220, -203.4644505317938865 ) ) ;
#7477=CARTESIAN_POINT ( 'NONE',  ( -67.58462422314151752, 10.27684056475513685, -204.5041005603981716 ) ) ;
#7478=FACE_BOUND ( 'NONE', #9679, .T. ) ;
#7483=CARTESIAN_POINT ( 'NONE',  ( -8.886921396801763962, 2.500000000000000444, -105.5168766094550676 ) ) ;
#7487=CARTESIAN_POINT ( 'NONE',  ( 7.427446726622309647, 5.321094445766562764, -26.41501464507892294 ) ) ;
#7488=CARTESIAN_POINT ( 'NONE',  ( -10.46704385831657902, 2.500000000000000000, -128.9524512386204549 ) ) ;
#7492=CARTESIAN_POINT ( 'NONE',  ( -3.940180586764666870, 10.47454284640667055, -44.50268400149392534 ) ) ;
#7494=VECTOR ( 'NONE', #8321, 1000.000000000000000 ) ;
#7495=CARTESIAN_POINT ( 'NONE',  ( 4.290161713843189339, 13.86208356708933920, 2.954600283075418332 ) ) ;
#7496=AXIS2_PLACEMENT_3D ( 'NONE', #1074, #5556, #10503 ) ;
#7503=EDGE_CURVE ( 'NONE', #14756, #14271, #14244, .T. ) ;
#7515=CARTESIAN_POINT ( 'NONE',  ( -61.92089974418476572, 15.00000000000000000, -174.1061791381038404 ) ) ;
#7519=AXIS2_PLACEMENT_3D ( 'NONE', #4633, #1000, #14066 ) ;
#7525=DIRECTION ( 'NONE',  ( -0.08794243244722420305, 1.868163743359636407E-15, -0.9961255586397055328 ) ) ;
#7528=CARTESIAN_POINT ( 'NONE',  ( -65.53364736412717662, 15.00000000000000000, -203.4171941195418754 ) ) ;
#7534=ORIENTED_EDGE ( 'NONE', *, *, #14289, .T. ) ;
#7537=CARTESIAN_POINT ( 'NONE',  ( -4.090890948359604984, 15.00000000000000000, -103.1929727064838147 ) ) ;
#7538=CARTESIAN_POINT ( 'NONE',  ( -2.256557393256121369, 5.321094445766560987, -25.56006732368493317 ) ) ;
#7547=ORIENTED_EDGE ( 'NONE', *, *, #8268, .T. ) ;
#7548=DIRECTION ( 'NONE',  ( 0.000000000000000000, 0.000000000000000000, -1.000000000000000000 ) ) ;
#7549=( BOUNDED_SURFACE ( )  B_SPLINE_SURFACE ( 3, 1, ( 
 ( #1362, #8462 ),
 ( #6380, #13196 ),
 ( #2601, #9861 ),
 ( #9709, #7300 ) ),
 .UNSPECIFIED., .F., .F., .T. ) 
 B_SPLINE_SURFACE_WITH_KNOTS ( ( 4, 4 ),
 ( 2, 2 ),
 ( 0.000000000000000000, 1.000000000000000000 ),
 ( 0.000000000000000000, 1.000000000000000000 ),
 .UNSPECIFIED. ) 
 GEOMETRIC_REPRESENTATION_ITEM ( )  RATIONAL_B_SPLINE_SURFACE ( (
 ( 1.000000000000000000, 1.000000000000000000),
 ( 0.6867676532959785529, 0.6867676532959785529),
 ( 0.6867676532959785529, 0.6867676532959785529),
 ( 1.000000000000000000, 1.000000000000000000) ) ) 
 REPRESENTATION_ITEM ( '' )  SURFACE ( )  );
#7551=CARTESIAN_POINT ( 'NONE',  ( 7.375268436326912536, 3.304579630018633196, -22.32553049743219376 ) ) ;
#7552=CARTESIAN_POINT ( 'NONE',  ( 3.111877744625329623, 1.934442845508696607, 4.175147216457742338 ) ) ;
#7555=CARTESIAN_POINT ( 'NONE',  ( -67.58984843273714205, 10.68251503306532690, -204.4107792426363801 ) ) ;
#7557=ORIENTED_EDGE ( 'NONE', *, *, #13517, .F. ) ;
#7568=CARTESIAN_POINT ( 'NONE',  ( 0.2553636793526916082, 4.345756845072476615, 2.892509118448076677 ) ) ;
#7579=CYLINDRICAL_SURFACE ( 'NONE', #7243, 2.500000000000000444 ) ;
#7588=CARTESIAN_POINT ( 'NONE',  ( -8.090126491280004828, 5.000000000000000000, -136.8653377734624996 ) ) ;
#7605=B_SPLINE_CURVE_WITH_KNOTS ( 'NONE', 3,
 ( #13234, #11819, #2636, #14237, #3638, #7338, #8340, #12051, #10746, #6182, #7176, #10901, #319, #1323 ),
 .UNSPECIFIED., .F., .F.,
 ( 4, 2, 2, 2, 2, 2, 4 ),
 ( -1.076617132515563425E-05, 0.0009993995386319133676, 0.002009565248588982347, 0.002514648103567523017, 0.003019730958546064121, 0.003524813813524604791, 0.004029896668503145027 ),
 .UNSPECIFIED. ) ;
#7608=CARTESIAN_POINT ( 'NONE',  ( -8.886921396801742645, 2.500000000000000444, -105.5168766094550676 ) ) ;
#7611=EDGE_CURVE ( 'NONE', #5990, #3511, #14669, .T. ) ;
#7623=CARTESIAN_POINT ( 'NONE',  ( 0.1865797813170224362, 3.107330460720267418, 2.113392633384786556 ) ) ;
#7625=ADVANCED_FACE ( 'NONE', ( #11219 ), #8746, .T. ) ;
#7632=CARTESIAN_POINT ( 'NONE',  ( -69.52150835262156647, 10.00000000000000178, -199.0124118306254957 ) ) ;
#7635=CARTESIAN_POINT ( 'NONE',  ( -5.285700560996287045, 15.00000000000000000, -102.0031443936493787 ) ) ;
#7642=DIRECTION ( 'NONE',  ( 0.000000000000000000, -1.000000000000000000, 0.000000000000000000 ) ) ;
#7643=DIRECTION ( 'NONE',  ( -0.08794243244722425856, -0.000000000000000000, -0.9961255586397054218 ) ) ;
#7653=CARTESIAN_POINT ( 'NONE',  ( -47.49849438531821733, 9.999999999999998224, -162.3383809241888400 ) ) ;
#7658=CARTESIAN_POINT ( 'NONE',  ( -8.167870570054514445, 5.000000000000000888, -136.8278529952039264 ) ) ;
#7663=CARTESIAN_POINT ( 'NONE',  ( -15.73004658022870927, 0.000000000000000000, -131.7446186346720367 ) ) ;
#7665=CARTESIAN_POINT ( 'NONE',  ( -69.06832266641278295, 15.00000000000115463, -200.7467498276384106 ) ) ;
#7667=DIRECTION ( 'NONE',  ( 0.08794243244723021213, 0.000000000000000000, 0.9961255586397049777 ) ) ;
#7671=CARTESIAN_POINT ( 'NONE',  ( -5.538855545106806666, 10.00000000000000000, -110.3982026382703765 ) ) ;
#7672=AXIS2_PLACEMENT_3D ( 'NONE', #13527, #6325, #4167 ) ;
#7675=CARTESIAN_POINT ( 'NONE',  ( 3.158745454532927877, 2.478737181588197558, 4.576782562779927233 ) ) ;
#7688=CARTESIAN_POINT ( 'NONE',  ( -6.167185496248319687, 14.52912145062034455, -104.1275751645885776 ) ) ;
#7694=TOROIDAL_SURFACE ( 'NONE', #10162, 2.000000000000011990, 1.000000000000000000 ) ;
#7703=DIRECTION ( 'NONE',  ( -0.05964429961207245307, 0.000000000000000000, -0.9982196940171964572 ) ) ;
#7704=CARTESIAN_POINT ( 'NONE',  ( 0.2550590916302901690, 4.348754961233985306, 2.889059047683731229 ) ) ;
#7713=ADVANCED_FACE ( 'NONE', ( #2020 ), #5006, .T. ) ;
#7715=CARTESIAN_POINT ( 'NONE',  ( -7.575942540376401801, 9.999999999999998224, -106.7905032256467734 ) ) ;
#7723=LINE ( 'NONE', #6641, #3731 ) ;
#7728=TOROIDAL_SURFACE ( 'NONE', #11676, 2.000000000000016431, 5.000000000000000000 ) ;
#7732=CARTESIAN_POINT ( 'NONE',  ( -36.12930860109405273, 9.999999999999998224, -156.3173234977680011 ) ) ;
#7735=LINE ( 'NONE', #7425, #1336 ) ;
#7737=ADVANCED_FACE ( 'NONE', ( #10131 ), #11290, .F. ) ;
#7738=DIRECTION ( 'NONE',  ( 0.000000000000000000, 0.000000000000000000, 1.000000000000000000 ) ) ;
#7746=LINE ( 'NONE', #5575, #3961 ) ;
#7747=LINE ( 'NONE', #1572, #2232 ) ;
#7750=CARTESIAN_POINT ( 'NONE',  ( 4.891108815300913015, 14.90343850142792270, -1.429801464957401347 ) ) ;
#7752=CIRCLE ( 'NONE', #6278, 2.326940983401415419 ) ;
#7766=CARTESIAN_POINT ( 'NONE',  ( -6.486570821710966328, 2.500000000000000000, -108.2546719218867253 ) ) ;
#7769=AXIS2_PLACEMENT_3D ( 'NONE', #13920, #3318, #2234 ) ;
#7775=CYLINDRICAL_SURFACE ( 'NONE', #8978, 3.250000000000005329 ) ;
#7777=VERTEX_POINT ( 'NONE', #7959 ) ;
#7783=CARTESIAN_POINT ( 'NONE',  ( 7.302490728567498479, 3.561478500444579698, -24.97446755075041125 ) ) ;
#7784=CARTESIAN_POINT ( 'NONE',  ( 0.2568603580465786962, 4.429590276632575652, 2.909462025691655462 ) ) ;
#7787=ADVANCED_FACE ( 'NONE', ( #4190 ), #3028, .T. ) ;
#7791=ORIENTED_EDGE ( 'NONE', *, *, #11038, .F. ) ;
#7795=DIRECTION ( 'NONE',  ( -0.7220210382022110851, 0.000000000000000000, 0.6918711009959885860 ) ) ;
#7806=ORIENTED_EDGE ( 'NONE', *, *, #2241, .T. ) ;
#7808=CARTESIAN_POINT ( 'NONE',  ( 2.159942170319879562, 0.000000000000000000, -121.5147849362692369 ) ) ;
#7809=CARTESIAN_POINT ( 'NONE',  ( -42.39238649434224726, 15.00000000000000000, -152.9358431397373863 ) ) ;
#7811=ORIENTED_EDGE ( 'NONE', *, *, #14894, .F. ) ;
#7814=CARTESIAN_POINT ( 'NONE',  ( -3.331919393530990092, 10.52300174851617953, -44.71933215806485151 ) ) ;
#7820=CARTESIAN_POINT ( 'NONE',  ( -63.59489740953759451, 14.99999999999999822, -201.2970526385593644 ) ) ;
#7821=CARTESIAN_POINT ( 'NONE',  ( -7.876768715742058724, 13.10813300872041154, -104.9763684901371050 ) ) ;
#7823=( BOUNDED_SURFACE ( )  B_SPLINE_SURFACE ( 3, 2, ( 
 ( #7537, #4149, #14821 ),
 ( #12323, #5229, #1742 ),
 ( #14672, #4077, #10164 ),
 ( #7688, #13509, #738 ),
 ( #666, #2905, #5445 ),
 ( #6452, #591, #5303 ),
 ( #5373, #2046, #7914 ),
 ( #6758, #9077, #9000 ),
 ( #7840, #13797, #12634 ),
 ( #8134, #10242, #891 ),
 ( #6980, #7988, #11696 ),
 ( #6827, #4368, #6898 ),
 ( #11620, #15045, #12710 ),
 ( #11473, #13727, #5664 ),
 ( #5593, #11543, #3127 ),
 ( #10307, #15200, #3275 ),
 ( #12863, #5817, #4518 ),
 ( #12556, #15124, #3197 ) ),
 .UNSPECIFIED., .F., .F., .T. ) 
 B_SPLINE_SURFACE_WITH_KNOTS ( ( 4, 2, 2, 2, 2, 2, 2, 2, 4 ),
 ( 3, 3 ),
 ( -1.470352482839513217E-05, 0.001632328272403186327, 0.002455844171018977187, 0.003279360069634767831, 0.004102875968250558475, 0.004514633917558453363, 0.004926391866866349119, 0.005749907765482139763, 0.006573423664097930406 ),
 ( 0.000000000000000000, 1.000000000000000000 ),
 .UNSPECIFIED. ) 
 GEOMETRIC_REPRESENTATION_ITEM ( )  RATIONAL_B_SPLINE_SURFACE ( (
 ( 1.000000000000000000, 1.000000000000000000, 1.000000000000000000),
 ( 1.000000000000000000, 1.000008545743839683, 1.000000000000000000),
 ( 1.000000000000000000, 0.9960198085043022731, 1.000000000000000000),
 ( 1.000000000000000000, 0.9835033616513570998, 1.000000000000000000),
 ( 1.000000000000000000, 0.9783561813779146910, 1.000000000000000000),
 ( 1.000000000000000000, 0.9664106271237844492, 1.000000000000000000),
 ( 1.000000000000000000, 0.9595652232277900318, 1.000000000000000000),
 ( 1.000000000000000000, 0.9448633500193042156, 1.000000000000000000),
 ( 1.000000000000000000, 0.9371864357976944504, 1.000000000000000000),
 ( 1.000000000000000000, 0.9259039669434644404, 1.000000000000000000),
 ( 1.000000000000000000, 0.9221838447129829808, 1.000000000000000000),
 ( 1.000000000000000000, 0.9149767654785520010, 1.000000000000000000),
 ( 1.000000000000000000, 0.9114704760577250209, 1.000000000000000000),
 ( 1.000000000000000000, 0.9018026765161173408, 1.000000000000000000),
 ( 1.000000000000000000, 0.8964349246879487199, 1.000000000000000000),
 ( 1.000000000000000000, 0.8889503419939598361, 1.000000000000000000),
 ( 1.000000000000000000, 0.8868438094748841705, 1.000000000000000000),
 ( 1.000000000000000000, 0.8868705507870419114, 1.000000000000000000) ) ) 
 REPRESENTATION_ITEM ( '' )  SURFACE ( )  );
#7825=CARTESIAN_POINT ( 'NONE',  ( -65.53364736412717662, 5.000000000000000000, -205.7441351029432894 ) ) ;
#7826=CARTESIAN_POINT ( 'NONE',  ( 4.912189190728483368, 14.88796584897967890, -1.019724683141319810 ) ) ;
#7828=CARTESIAN_POINT ( 'NONE',  ( 2.891442464128509027, 0.5021605422368213834, 2.425309775607110030 ) ) ;
#7829=CARTESIAN_POINT ( 'NONE',  ( -3.955596480971199203, 2.500000000000000000, -118.5438621456188173 ) ) ;
#7832=DIRECTION ( 'NONE',  ( -0.000000000000000000, -1.000000000000000000, -0.000000000000000000 ) ) ;
#7839=LINE ( 'NONE', #5302, #9150 ) ;
#7840=CARTESIAN_POINT ( 'NONE',  ( -7.848833331099569044, 13.14512866485396181, -104.9618519593132078 ) ) ;
#7851=ORIENTED_EDGE ( 'NONE', *, *, #1020, .T. ) ;
#7854=CARTESIAN_POINT ( 'NONE',  ( 7.781170200712294260, 5.000000000000000888, -20.49502329017444424 ) ) ;
#7855=CARTESIAN_POINT ( 'NONE',  ( 0.2483469068648843925, 4.114088372968399021, 2.813030006718263643 ) ) ;
#7859=DIRECTION ( 'NONE',  ( 0.08794243244723021213, 0.000000000000000000, 0.9961255586397049777 ) ) ;
#7869=CARTESIAN_POINT ( 'NONE',  ( 4.916379274077837813, 14.85715077789358673, -0.5990194345177435320 ) ) ;
#7870=ADVANCED_FACE ( 'NONE', ( #5415 ), #7579, .T. ) ;
#7873=ORIENTED_EDGE ( 'NONE', *, *, #13873, .F. ) ;
#7875=CARTESIAN_POINT ( 'NONE',  ( -51.02532656535751698, 9.999999999999998224, -166.3766172518998587 ) ) ;
#7878=CARTESIAN_POINT ( 'NONE',  ( 7.101058424337646890, 5.000000000000000888, -131.4073749499507642 ) ) ;
#7879=CARTESIAN_POINT ( 'NONE',  ( 0.7644969749118040170, 5.000000000000000000, -138.4027240657576101 ) ) ;
#7880=CARTESIAN_POINT ( 'NONE',  ( -8.272624645278304101, 14.99999999999999822, -140.4230430975193258 ) ) ;
#7883=EDGE_CURVE ( 'NONE', #1674, #6652, #7735, .T. ) ;
#7896=AXIS2_PLACEMENT_3D ( 'NONE', #9153, #4295, #13878 ) ;
#7914=CARTESIAN_POINT ( 'NONE',  ( -7.398019396816514437, 13.84373920337187691, -104.1012393012796764 ) ) ;
#7915=FACE_OUTER_BOUND ( 'NONE', #4619, .T. ) ;
#7920=ORIENTED_EDGE ( 'NONE', *, *, #8092, .F. ) ;
#7923=VECTOR ( 'NONE', #11974, 1000.000000000000000 ) ;
#7935=CARTESIAN_POINT ( 'NONE',  ( -0.3545318111937544869, 10.00000000000000178, -139.6177279649697596 ) ) ;
#7937=CARTESIAN_POINT ( 'NONE',  ( -37.86885108244810283, 15.00000000000000000, -139.8897182464016566 ) ) ;
#7944=CARTESIAN_POINT ( 'NONE',  ( -64.87526564358481096, 14.94604455467652571, -187.2214054586863483 ) ) ;
#7945=ORIENTED_EDGE ( 'NONE', *, *, #834, .F. ) ;
#7951=LINE ( 'NONE', #12593, #6041 ) ;
#7955=CARTESIAN_POINT ( 'NONE',  ( -42.37771161479906112, 15.00000000000000000, -158.4861704486624774 ) ) ;
#7957=ORIENTED_EDGE ( 'NONE', *, *, #2330, .F. ) ;
#7958=CARTESIAN_POINT ( 'NONE',  ( -11.40820045156521623, 15.00000000000000000, -126.3212311507313217 ) ) ;
#7959=CARTESIAN_POINT ( 'NONE',  ( -8.351752737786036107, 9.999999999999998224, -94.60045770897244211 ) ) ;
#7966=AXIS2_PLACEMENT_3D ( 'NONE', #12351, #2783, #11117 ) ;
#7968=CARTESIAN_POINT ( 'NONE',  ( -4.716550020523635922, 14.96884535972561103, -103.4640810165829237 ) ) ;
#7969=CARTESIAN_POINT ( 'NONE',  ( -0.3732829694918187724, 15.00000000000000000, -108.7490593617764461 ) ) ;
#7970=DIRECTION ( 'NONE',  ( -0.9961255586397056438, -0.000000000000000000, 0.08794243244722427244 ) ) ;
#7971=EDGE_CURVE ( 'NONE', #12098, #3600, #13151, .T. ) ;
#7974=CARTESIAN_POINT ( 'NONE',  ( -7.234633885585873614, 5.000000000000000888, -146.9955140158000404 ) ) ;
#7976=CARTESIAN_POINT ( 'NONE',  ( -49.91314714375069173, 0.000000000000000000, -125.9106517931341500 ) ) ;
#7977=EDGE_LOOP ( 'NONE', ( #1139, #984, #2435, #10987 ) ) ;
#7978=ORIENTED_EDGE ( 'NONE', *, *, #15306, .F. ) ;
#7984=CARTESIAN_POINT ( 'NONE',  ( 5.079523875935373134, 9.999999999999998224, -108.2552591983082806 ) ) ;
#7985=ORIENTED_EDGE ( 'NONE', *, *, #12426, .T. ) ;
#7988=CARTESIAN_POINT ( 'NONE',  ( -8.470420019481499807, 12.69254319550381283, -104.8380799168281214 ) ) ;
#7993=EDGE_CURVE ( 'NONE', #9274, #447, #9193, .T. ) ;
#7995=CYLINDRICAL_SURFACE ( 'NONE', #10600, 2.500000000000000000 ) ;
#8001=ORIENTED_EDGE ( 'NONE', *, *, #1205, .T. ) ;
#8010=CARTESIAN_POINT ( 'NONE',  ( -13.68460728451510633, 7.499999999999991118, -92.46488696946715891 ) ) ;
#8020=CARTESIAN_POINT ( 'NONE',  ( -33.91109452335874153, 5.000000000000000000, -156.1716796081737471 ) ) ;
#8021=CARTESIAN_POINT ( 'NONE',  ( -63.60348060676461301, 15.00000000000000000, -180.2685449772604329 ) ) ;
#8026=CARTESIAN_POINT ( 'NONE',  ( -2.893252786143252653, 4.336808689942017736E-16, -110.6524584094670445 ) ) ;
#8032=CARTESIAN_POINT ( 'NONE',  ( -53.69697306021766536, 9.999999999999998224, -170.4167521506420258 ) ) ;
#8035=CARTESIAN_POINT ( 'NONE',  ( 7.220173501946012706, 9.999999999999996447, -111.8642345870615458 ) ) ;
#8047=CARTESIAN_POINT ( 'NONE',  ( 3.891364641103943978, 14.90536770052034932, -1.768596708628486613 ) ) ;
#8048=LINE ( 'NONE', #11385, #9622 ) ;
#8050=ORIENTED_EDGE ( 'NONE', *, *, #1280, .F. ) ;
#8060=ADVANCED_FACE ( 'NONE', ( #9275 ), #13572, .F. ) ;
#8063=CARTESIAN_POINT ( 'NONE',  ( -13.86049214940955387, 7.499999999999991118, -94.45713808674658196 ) ) ;
#8071=ORIENTED_EDGE ( 'NONE', *, *, #11100, .F. ) ;
#8078=DIRECTION ( 'NONE',  ( 0.6005713924789962688, 0.000000000000000000, -0.7995711366325319869 ) ) ;
#8092=EDGE_CURVE ( 'NONE', #14091, #3511, #374, .T. ) ;
#8095=CARTESIAN_POINT ( 'NONE',  ( -64.45835881414798507, 14.99074302885292198, -184.2213710543591958 ) ) ;
#8096=CARTESIAN_POINT ( 'NONE',  ( 0.4151132296555069545, 3.270056657667109956, -138.3403225835776311 ) ) ;
#8104=CARTESIAN_POINT ( 'NONE',  ( -66.89175632424894502, 14.99999999999999822, -193.0526493258840048 ) ) ;
#8108=LINE ( 'NONE', #3399, #11446 ) ;
#8116=CARTESIAN_POINT ( 'NONE',  ( -8.886921396801785278, 10.34135959593272780, -105.5168766094550250 ) ) ;
#8118=CARTESIAN_POINT ( 'NONE',  ( 3.698847099818734829, 12.64700925907840023, 4.332249626577416635 ) ) ;
#8121=CARTESIAN_POINT ( 'NONE',  ( -2.729969426660547871, 9.999999999999998224, -110.6850855677400602 ) ) ;
#8122=ORIENTED_EDGE ( 'NONE', *, *, #14442, .T. ) ;
#8123=VERTEX_POINT ( 'NONE', #5792 ) ;
#8127=CARTESIAN_POINT ( 'NONE',  ( -7.534724830497282255, 2.500000000000000444, -106.8248685501097839 ) ) ;
#8132=CARTESIAN_POINT ( 'NONE',  ( -54.45540687913352684, 15.00000000000000000, -149.0501727868689557 ) ) ;
#8134=CARTESIAN_POINT ( 'NONE',  ( -8.117864242877150360, 12.74145370066594118, -105.1028050937847098 ) ) ;
#8136=CARTESIAN_POINT ( 'NONE',  ( -2.810094634146505399, 7.379999999999995453, -48.88660647235757040 ) ) ;
#8148=ORIENTED_EDGE ( 'NONE', *, *, #4578, .F. ) ;
#8156=FACE_OUTER_BOUND ( 'NONE', #4979, .T. ) ;
#8159=AXIS2_PLACEMENT_3D ( 'NONE', #14925, #5473, #4322 ) ;
#8165=CARTESIAN_POINT ( 'NONE',  ( -2.573490212646732278, 5.321094445766561876, -29.14997122992682321 ) ) ;
#8169=CARTESIAN_POINT ( 'NONE',  ( -67.33687266635307367, 14.30069434016096430, -197.3216639972416715 ) ) ;
#8172=CARTESIAN_POINT ( 'NONE',  ( -2.640059788692800335, 4.336808689942017736E-16, -114.1739744175401512 ) ) ;
#8177=ORIENTED_EDGE ( 'NONE', *, *, #10144, .F. ) ;
#8178=ADVANCED_FACE ( 'NONE', ( #9117 ), #15155, .T. ) ;
#8181=EDGE_CURVE ( 'NONE', #3117, #2896, #4064, .T. ) ;
#8182=CARTESIAN_POINT ( 'NONE',  ( -66.12309802906914058, 15.00000000000000000, -189.2880876859682644 ) ) ;
#8183=EDGE_CURVE ( 'NONE', #8353, #7290, #620, .T. ) ;
#8186=CARTESIAN_POINT ( 'NONE',  ( -5.117107008561104564, 15.00000000000121858, -113.5915292474848854 ) ) ;
#8192=DIRECTION ( 'NONE',  ( 0.08794243244722427244, 0.000000000000000000, 0.9961255586397054218 ) ) ;
#8193=DIRECTION ( 'NONE',  ( 0.000000000000000000, 0.000000000000000000, -1.000000000000000000 ) ) ;
#8197=EDGE_CURVE ( 'NONE', #4481, #14016, #8208, .T. ) ;
#8198=CARTESIAN_POINT ( 'NONE',  ( -4.751975593842658441, 14.96875058370196321, -103.3648980062157818 ) ) ;
#8199=CARTESIAN_POINT ( 'NONE',  ( 9.939878312292631080, -7.806255641895631925E-15, -115.2320631035898657 ) ) ;
#8200=ORIENTED_EDGE ( 'NONE', *, *, #11038, .T. ) ;
#8201=ORIENTED_EDGE ( 'NONE', *, *, #6313, .F. ) ;
#8208=CIRCLE ( 'NONE', #14147, 0.5000000000000004441 ) ;
#8218=AXIS2_PLACEMENT_3D ( 'NONE', #13104, #12879, #8078 ) ;
#8219=CARTESIAN_POINT ( 'NONE',  ( -5.317082570419811915, 15.00000000000000178, -126.7958533838912700 ) ) ;
#8224=( BOUNDED_SURFACE ( )  B_SPLINE_SURFACE ( 3, 2, ( 
 ( #11822, #2339, #5730 ),
 ( #11682, #7035, #12775 ),
 ( #6967, #2182, #11749 ),
 ( #8047, #15187, #1171 ) ),
 .UNSPECIFIED., .F., .F., .T. ) 
 B_SPLINE_SURFACE_WITH_KNOTS ( ( 4, 4 ),
 ( 3, 3 ),
 ( 4.712388980384689674, 4.907255421178648547 ),
 ( 0.000000000000000000, 1.000000000000000000 ),
 .UNSPECIFIED. ) 
 GEOMETRIC_REPRESENTATION_ITEM ( )  RATIONAL_B_SPLINE_SURFACE ( (
 ( 1.000000000000000000, 1.000000000000000000, 1.000000000000000000),
 ( 1.000000000000000000, 1.000004279931538065, 1.000000000000000000),
 ( 1.000000000000000000, 0.9936567599901997561, 1.000000000000000000),
 ( 1.000000000000000000, 0.9810773865977353569, 1.000000000000000000) ) ) 
 REPRESENTATION_ITEM ( '' )  SURFACE ( )  );
#8232=CIRCLE ( 'NONE', #1078, 3.187847681061608540 ) ;
#8234=DIRECTION ( 'NONE',  ( 0.08794243244722427244, 0.000000000000000000, 0.9961255586397055328 ) ) ;
#8237=CARTESIAN_POINT ( 'NONE',  ( -61.23004053993285112, 15.00000000000000355, -172.1684668291862863 ) ) ;
#8238=ORIENTED_EDGE ( 'NONE', *, *, #7256, .F. ) ;
#8239=AXIS2_PLACEMENT_3D ( 'NONE', #4421, #14615, #13369 ) ;
#8245=CARTESIAN_POINT ( 'NONE',  ( -67.48102662054394330, 13.98401442981596077, -198.9466073721665396 ) ) ;
#8248=TOROIDAL_SURFACE ( 'NONE', #3074, 5.000000000000001776, 5.000000000000000000 ) ;
#8256=CARTESIAN_POINT ( 'NONE',  ( -59.62538729150122663, 15.00000000000000000, -184.0486941882522842 ) ) ;
#8258=ORIENTED_EDGE ( 'NONE', *, *, #2307, .F. ) ;
#8259=CARTESIAN_POINT ( 'NONE',  ( -6.422940335267006695, 14.99999999999267963, -108.3014594333919973 ) ) ;
#8260=CARTESIAN_POINT ( 'NONE',  ( -25.82983890416511841, 9.999999999999998224, -152.2527639562405000 ) ) ;
#8261=DIRECTION ( 'NONE',  ( 0.000000000000000000, 0.000000000000000000, -1.000000000000000000 ) ) ;
#8265=LINE ( 'NONE', #10441, #3227 ) ;
#8267=CARTESIAN_POINT ( 'NONE',  ( 1.893911505664648054, 15.00000000000000000, -1.663006917529762152 ) ) ;
#8268=EDGE_CURVE ( 'NONE', #9864, #11348, #14905, .T. ) ;
#8269=DIRECTION ( 'NONE',  ( -0.000000000000000000, -1.000000000000000000, -0.000000000000000000 ) ) ;
#8271=CARTESIAN_POINT ( 'NONE',  ( 3.230086961373112242, 9.999999999999998224, 5.208283729180105404 ) ) ;
#8273=CARTESIAN_POINT ( 'NONE',  ( -5.714611007916760244, 14.75484434184808613, -103.6239156122758942 ) ) ;
#8274=CARTESIAN_POINT ( 'NONE',  ( -3.691420245339818607, 9.999999999999998224, -128.6724311331325339 ) ) ;
#8276=EDGE_LOOP ( 'NONE', ( #3160, #14818, #12587, #486 ) ) ;
#8277=CARTESIAN_POINT ( 'NONE',  ( -5.257674075046501194, 4.336808689942017736E-16, -105.6497928282025214 ) ) ;
#8282=ORIENTED_EDGE ( 'NONE', *, *, #5701, .T. ) ;
#8286=EDGE_CURVE ( 'NONE', #13498, #10617, #1815, .T. ) ;
#8293=VERTEX_POINT ( 'NONE', #389 ) ;
#8295=DIRECTION ( 'NONE',  ( 0.000000000000000000, 0.000000000000000000, -1.000000000000000000 ) ) ;
#8305=CARTESIAN_POINT ( 'NONE',  ( -5.247127501425628893, 2.500000000000000444, -111.6612542950777254 ) ) ;
#8306=CARTESIAN_POINT ( 'NONE',  ( -3.234594381879578151, 7.379999999999995453, -42.32384790875221370 ) ) ;
#8312=ORIENTED_EDGE ( 'NONE', *, *, #15306, .T. ) ;
#8316=CARTESIAN_POINT ( 'NONE',  ( -63.81341264818736647, 12.59430211938071764, -202.1382658931505887 ) ) ;
#8321=DIRECTION ( 'NONE',  ( -0.000000000000000000, -1.000000000000000000, -0.000000000000000000 ) ) ;
#8322=CARTESIAN_POINT ( 'NONE',  ( -16.02909037268676329, 1.021521734388686209E-15, -131.4942061907987068 ) ) ;
#8326=FACE_OUTER_BOUND ( 'NONE', #12002, .T. ) ;
#8328=ORIENTED_EDGE ( 'NONE', *, *, #10642, .T. ) ;
#8329=CARTESIAN_POINT ( 'NONE',  ( -5.447453277264131088, 15.00000000000000178, -116.0587048211255166 ) ) ;
#8330=UNCERTAINTY_MEASURE_WITH_UNIT (LENGTH_MEASURE( 1.000000000000000082E-05 ), #2275, 'distance_accuracy_value', 'NONE');
#8332=CARTESIAN_POINT ( 'NONE',  ( 8.054779650714358752, 9.999999999999998224, -130.1950568140816813 ) ) ;
#8333=FACE_OUTER_BOUND ( 'NONE', #13789, .T. ) ;
#8338=CARTESIAN_POINT ( 'NONE',  ( 2.858579147729096714, 14.48245223601180953, 0.7576670880602638380 ) ) ;
#8339=CARTESIAN_POINT ( 'NONE',  ( -3.805429041573433313, 11.11311992875805288, -44.52694620552966853 ) ) ;
#8340=CARTESIAN_POINT ( 'NONE',  ( -8.429367341598160479, 0.9564791310987349471, -105.2145337967942282 ) ) ;
#8343=CYLINDRICAL_SURFACE ( 'NONE', #4711, 14.80000000000025651 ) ;
#8344=CARTESIAN_POINT ( 'NONE',  ( -63.35291325964459475, 11.28823943156841203, -203.2975719163582653 ) ) ;
#8348=CARTESIAN_POINT ( 'NONE',  ( -5.114912396505194359, 2.500000000000000444, -113.5322278711313260 ) ) ;
#8353=VERTEX_POINT ( 'NONE', #8724 ) ;
#8355=CARTESIAN_POINT ( 'NONE',  ( -63.69159315064205629, 9.999999999999998224, -164.7787203863022967 ) ) ;
#8363=ORIENTED_EDGE ( 'NONE', *, *, #76, .T. ) ;
#8364=CARTESIAN_POINT ( 'NONE',  ( -0.5514805362514287879, 14.99999999999999645, -109.6828893904346813 ) ) ;
#8366=EDGE_LOOP ( 'NONE', ( #12796, #10770 ) ) ;
#8368=ORIENTED_EDGE ( 'NONE', *, *, #9798, .F. ) ;
#8391=AXIS2_PLACEMENT_3D ( 'NONE', #2620, #7161, #8559 ) ;
#8392=CARTESIAN_POINT ( 'NONE',  ( -63.22816877820476833, 10.40788280221283735, -203.5738002078235809 ) ) ;
#8395=AXIS2_PLACEMENT_3D ( 'NONE', #9436, #7262, #4646 ) ;
#8398=LINE ( 'NONE', #3618, #7494 ) ;
#8403=CARTESIAN_POINT ( 'NONE',  ( -68.72755137142191018, 10.00000000000000355, -180.2525548315512083 ) ) ;
#8408=CARTESIAN_POINT ( 'NONE',  ( -1.167553989851729979, 15.00000000000000000, -119.2042076268937336 ) ) ;
#8409=CARTESIAN_POINT ( 'NONE',  ( 0.2625675448779695720, 9.999999999999998224, 2.974107436473218957 ) ) ;
#8410=CARTESIAN_POINT ( 'NONE',  ( -11.91260474549187798, 9.999999999999998224, -150.3549708560018132 ) ) ;
#8414=CARTESIAN_POINT ( 'NONE',  ( -3.724891368794485125, 9.650666666666664284, -47.87745094654707145 ) ) ;
#8416=CARTESIAN_POINT ( 'NONE',  ( 1.518127423188106340, 13.34476997861058933, 4.548776429828005341 ) ) ;
#8419=B_SPLINE_CURVE_WITH_KNOTS ( 'NONE', 3,
 ( #14300, #6170, #3699, #9428, #9740, #7166, #5861, #10892, #308, #5022, #1389, #7251, #10580, #3865, #13141, #11968, #2551, #1310, #9572, #5938, #4937, #14154 ),
 .UNSPECIFIED., .F., .F.,
 ( 4, 2, 2, 2, 2, 2, 2, 2, 2, 2, 4 ),
 ( 5.421010862427521568E-20, 0.001104514646399055826, 0.002209029292798111652, 0.002761286615997639998, 0.003313543939197167477, 0.004418058585596228507, 0.005522573231995289537, 0.006627087878394349700, 0.007731602524793410730, 0.008283859847992942546, 0.008836117171192472627 ),
 .UNSPECIFIED. ) ;
#8428=CARTESIAN_POINT ( 'NONE',  ( -5.191659272572687556, 2.500000000000000444, -112.0623128200284953 ) ) ;
#8433=ORIENTED_EDGE ( 'NONE', *, *, #1280, .T. ) ;
#8438=CARTESIAN_POINT ( 'NONE',  ( -67.50271866717234559, 9.999999999999998224, -175.2102855837734978 ) ) ;
#8449=ORIENTED_EDGE ( 'NONE', *, *, #4138, .F. ) ;
#8450=ORIENTED_EDGE ( 'NONE', *, *, #9130, .T. ) ;
#8456=ORIENTED_EDGE ( 'NONE', *, *, #6455, .T. ) ;
#8462=CARTESIAN_POINT ( 'NONE',  ( -67.58382170693636226, 5.000000000000000888, -204.5178482451963191 ) ) ;
#8471=CIRCLE ( 'NONE', #4300, 6.999999999999950262 ) ;
#8473=CARTESIAN_POINT ( 'NONE',  ( -67.61523983689153283, 11.65026692799600205, -203.8419816591213021 ) ) ;
#8480=VECTOR ( 'NONE', #2164, 1000.000000000000000 ) ;
#8482=CARTESIAN_POINT ( 'NONE',  ( -2.141054399116760543, 9.999999999999998224, -102.7251783244459631 ) ) ;
#8484=ORIENTED_EDGE ( 'NONE', *, *, #2215, .F. ) ;
#8490=CARTESIAN_POINT ( 'NONE',  ( -5.170287126184733850, 15.00000000000000000, -112.1835598689884108 ) ) ;
#8496=CARTESIAN_POINT ( 'NONE',  ( -3.691420245339825712, 15.00000000000000000, -128.6724311331325339 ) ) ;
#8498=CARTESIAN_POINT ( 'NONE',  ( 0.3534949980169243555, 11.00682189557416990, 2.912326207404907219 ) ) ;
#8499=CARTESIAN_POINT ( 'NONE',  ( -4.022906649771232246, 11.02829952875353392, -46.76855065446253690 ) ) ;
#8500=DIRECTION ( 'NONE',  ( 0.05964429961207245307, -0.000000000000000000, 0.9982196940171964572 ) ) ;
#8504=CARTESIAN_POINT ( 'NONE',  ( -65.18383229995919237, 14.84510318562159448, -190.8261455846306660 ) ) ;
#8507=ORIENTED_EDGE ( 'NONE', *, *, #2711, .T. ) ;
#8508=CARTESIAN_POINT ( 'NONE',  ( -5.131649475085241718, 2.500000000000000444, -112.7947322869679709 ) ) ;
#8518=CARTESIAN_POINT ( 'NONE',  ( -64.24938361218754324, 15.00000000000000000, -199.4097214783338643 ) ) ;
#8524=ORIENTED_EDGE ( 'NONE', *, *, #12426, .F. ) ;
#8539=CARTESIAN_POINT ( 'NONE',  ( -48.00729659322606580, 15.00000000000000178, -156.2075853427034247 ) ) ;
#8548=CARTESIAN_POINT ( 'NONE',  ( -65.52812891407587870, 15.29456201715631813, -203.7013355924380278 ) ) ;
#8554=CARTESIAN_POINT ( 'NONE',  ( 4.371113732131426843, 2.850949024098341860E-47, -126.7907979241013408 ) ) ;
#8559=DIRECTION ( 'NONE',  ( 0.000000000000000000, 0.000000000000000000, -1.000000000000000000 ) ) ;
#8565=ADVANCED_FACE ( 'NONE', ( #11342 ), #10946, .T. ) ;
#8567=ADVANCED_FACE ( 'NONE', ( #9100 ), #11501, .T. ) ;
#8572=CARTESIAN_POINT ( 'NONE',  ( 0.2611203624075133511, 4.669981294363242164, 2.957715173867767167 ) ) ;
#8574=CARTESIAN_POINT ( 'NONE',  ( 3.666659101104859264, 12.53633980302105755, 4.393427362251489221 ) ) ;
#8577=CARTESIAN_POINT ( 'NONE',  ( -17.32624372123753886, 15.00000000000000000, -122.3796757791585321 ) ) ;
#8580=CARTESIAN_POINT ( 'NONE',  ( 3.136841903360910067, 5.000000000000000888, -104.4936450199714812 ) ) ;
#8584=CARTESIAN_POINT ( 'NONE',  ( -6.654685603881863365, 7.806255641895631925E-15, -108.0058818677553774 ) ) ;
#8589=ORIENTED_EDGE ( 'NONE', *, *, #3152, .F. ) ;
#8593=CARTESIAN_POINT ( 'NONE',  ( -61.28061730015007669, 15.00000000000000711, -159.7704501039084448 ) ) ;
#8594=FACE_OUTER_BOUND ( 'NONE', #4154, .T. ) ;
#8601=CARTESIAN_POINT ( 'NONE',  ( -8.205916711996726676, 7.499999999999991118, -92.94857034792688921 ) ) ;
#8603=VERTEX_POINT ( 'NONE', #10789 ) ;
#8608=AXIS2_PLACEMENT_3D ( 'NONE', #14789, #703, #12291 ) ;
#8614=CARTESIAN_POINT ( 'NONE',  ( -62.13313392481989439, 9.999999999999998224, -194.8801037569120069 ) ) ;
#8623=( BOUNDED_SURFACE ( )  B_SPLINE_SURFACE ( 3, 2, ( 
 ( #10721, #135, #682 ),
 ( #6467, #11183, #14989 ),
 ( #10258, #4163, #4387 ),
 ( #7784, #14688, #5388 ),
 ( #7704, #9094, #525 ),
 ( #13523, #1840, #14765 ),
 ( #7855, #1679, #11416 ),
 ( #835, #609, #5240 ),
 ( #13815, #5540, #1914 ),
 ( #6548, #11104, #7552 ),
 ( #12270, #4089, #2921 ),
 ( #7623, #8793, #1987 ),
 ( #6392, #8865, #6627 ),
 ( #12339, #9950, #1759 ),
 ( #5315, #10028, #11260 ),
 ( #14919, #2999, #8943 ),
 ( #13594, #12417, #10102 ),
 ( #14839, #4239, #13671 ),
 ( #12497, #3070, #11334 ),
 ( #757, #5467, #10184 ) ),
 .UNSPECIFIED., .F., .F., .T. ) 
 B_SPLINE_SURFACE_WITH_KNOTS ( ( 4, 2, 2, 2, 2, 2, 2, 2, 2, 4 ),
 ( 3, 3 ),
 ( 0.01021656723133482908, 0.01070697027993146831, 0.01095217180422978706, 0.01119737332852810754, 0.01168777637712474678, 0.01217817942572138601, 0.01266858247431802524, 0.01315898552291466447, 0.01364938857151130371, 0.01413979162010794294 ),
 ( 0.000000000000000000, 1.000000000000000000 ),
 .UNSPECIFIED. ) 
 GEOMETRIC_REPRESENTATION_ITEM ( )  RATIONAL_B_SPLINE_SURFACE ( (
 ( 1.000000000000000000, 0.6693962893781482126, 1.000000000000000000),
 ( 1.000000000000000000, 0.6693971655676271837, 1.000000000000000000),
 ( 1.000000000000000000, 0.6695055079298116718, 1.000000000000000000),
 ( 1.000000000000000000, 0.6698470843657819973, 1.000000000000000000),
 ( 1.000000000000000000, 0.6699916310626345961, 1.000000000000000000),
 ( 1.000000000000000000, 0.6703393818075829014, 1.000000000000000000),
 ( 1.000000000000000000, 0.6705430798865028574, 1.000000000000000000),
 ( 1.000000000000000000, 0.6712520209205289357, 1.000000000000000000),
 ( 1.000000000000000000, 0.6718564003725113754, 1.000000000000000000),
 ( 1.000000000000000000, 0.6734024997055334527, 1.000000000000000000),
 ( 1.000000000000000000, 0.6743323796560330985, 1.000000000000000000),
 ( 1.000000000000000000, 0.6766315243239030552, 1.000000000000000000),
 ( 1.000000000000000000, 0.6779734166346523816, 1.000000000000000000),
 ( 1.000000000000000000, 0.6812445256750346845, 1.000000000000000000),
 ( 1.000000000000000000, 0.6831973919983876931, 1.000000000000000000),
 ( 1.000000000000000000, 0.6879353199740830815, 1.000000000000000000),
 ( 1.000000000000000000, 0.6907034268515229725, 1.000000000000000000),
 ( 1.000000000000000000, 0.6976421491555230281, 1.000000000000000000),
 ( 1.000000000000000000, 0.7018548256397145746, 1.000000000000000000),
 ( 1.000000000000000000, 0.7071067811865475727, 1.000000000000000000) ) ) 
 REPRESENTATION_ITEM ( '' )  SURFACE ( )  );
#8625=CARTESIAN_POINT ( 'NONE',  ( -67.60114792446165666, 11.17285071187519385, -204.1860880824393405 ) ) ;
#8638=CARTESIAN_POINT ( 'NONE',  ( -8.570785970181212576, 1.189964233097702939, -105.3070837849071353 ) ) ;
#8647=CIRCLE ( 'NONE', #8395, 3.250000000000005329 ) ;
#8651=CARTESIAN_POINT ( 'NONE',  ( -4.211572975458966361, 9.962993690351991560, -47.49266443388843584 ) ) ;
#8653=CARTESIAN_POINT ( 'NONE',  ( 1.598485290837698969, 13.49296761261617661, 1.982191991666128361 ) ) ;
#8658=CIRCLE ( 'NONE', #3990, 2.500000000000000000 ) ;
#8661=AXIS2_PLACEMENT_3D ( 'NONE', #13564, #10075, #7525 ) ;
#8666=VERTEX_POINT ( 'NONE', #10717 ) ;
#8667=CARTESIAN_POINT ( 'NONE',  ( -65.53364736412717662, 5.000000000000000000, -203.4171941195418754 ) ) ;
#8671=CARTESIAN_POINT ( 'NONE',  ( -3.421798459318232677, 10.60800287581505508, -46.00651939675768176 ) ) ;
#8676=CARTESIAN_POINT ( 'NONE',  ( -69.84691631978306248, 15.00000000000114575, -196.7709020263189643 ) ) ;
#8684=ORIENTED_EDGE ( 'NONE', *, *, #4662, .F. ) ;
#8685=CARTESIAN_POINT ( 'NONE',  ( -3.520407287333055635, 7.379999999999995453, -45.56125597433126018 ) ) ;
#8690=DIRECTION ( 'NONE',  ( 8.673617379884027583E-16, 0.000000000000000000, -1.000000000000000000 ) ) ;
#8695=DIRECTION ( 'NONE',  ( -0.000000000000000000, 1.000000000000000000, -0.000000000000000000 ) ) ;
#8697=DIRECTION ( 'NONE',  ( 0.6527336816407245390, 0.000000000000000000, -0.7575874476598363216 ) ) ;
#8699=CARTESIAN_POINT ( 'NONE',  ( -8.484329074657676273, 2.500000000000001776, -105.8548167551525836 ) ) ;
#8700=DIRECTION ( 'NONE',  ( -0.08794243244722436958, 0.000000000000000000, -0.9961255586397055328 ) ) ;
#8707=ORIENTED_EDGE ( 'NONE', *, *, #1294, .T. ) ;
#8708=CARTESIAN_POINT ( 'NONE',  ( 2.159942170319879562, 15.00000000000000000, -121.5147849362692369 ) ) ;
#8715=CARTESIAN_POINT ( 'NONE',  ( -64.90982034444132864, 14.98923205054743946, -184.4898348768445544 ) ) ;
#8716=CARTESIAN_POINT ( 'NONE',  ( 2.159942170319879562, 5.000000000000000888, -121.5147849362692369 ) ) ;
#8724=CARTESIAN_POINT ( 'NONE',  ( -1.724164254788412842, 7.321094445766562764, -19.52964039877223712 ) ) ;
#8726=CARTESIAN_POINT ( 'NONE',  ( -65.53364736412717662, 5.000000000000000000, -203.4171941195418754 ) ) ;
#8728=ADVANCED_FACE ( 'NONE', ( #5992 ), #12415, .F. ) ;
#8733=CARTESIAN_POINT ( 'NONE',  ( -3.805829833685401287, 11.11844615798745828, -44.54564306111133476 ) ) ;
#8746=PLANE ( 'NONE',  #6004 ) ;
#8750=DIRECTION ( 'NONE',  ( 0.000000000000000000, 0.000000000000000000, -1.000000000000000000 ) ) ;
#8752=EDGE_CURVE ( 'NONE', #15312, #411, #2374, .T. ) ;
#8767=ORIENTED_EDGE ( 'NONE', *, *, #11118, .F. ) ;
#8777=ADVANCED_FACE ( 'NONE', ( #1444 ), #6388, .T. ) ;
#8793=CARTESIAN_POINT ( 'NONE',  ( 0.3429446965881275955, 1.040318156481846001, 3.884540920300163958 ) ) ;
#8803=CARTESIAN_POINT ( 'NONE',  ( -7.575942540335539377, 15.00000000000153122, -106.7905032256090294 ) ) ;
#8811=CARTESIAN_POINT ( 'NONE',  ( 4.374104445797671659, 15.00089282178949013, -1.804052482945163405 ) ) ;
#8816=DIRECTION ( 'NONE',  ( 0.000000000000000000, 1.000000000000000000, 0.000000000000000000 ) ) ;
#8819=CARTESIAN_POINT ( 'NONE',  ( -40.43640613370096304, 15.00000000000000000, -157.5381262016960875 ) ) ;
#8821=ORIENTED_EDGE ( 'NONE', *, *, #12124, .F. ) ;
#8825=CARTESIAN_POINT ( 'NONE',  ( -3.724891368794482904, 9.650666666666662508, -47.87745094654707145 ) ) ;
#8829=DIRECTION ( 'NONE',  ( -0.7575874476598363216, -0.000000000000000000, -0.6527336816407245390 ) ) ;
#8832=CARTESIAN_POINT ( 'NONE',  ( -5.799297919316144245, 10.00000000000000355, -109.6563063839760588 ) ) ;
#8836=CARTESIAN_POINT ( 'NONE',  ( 10.01939027896081491, 0.000000000000000000, -127.6977514918621637 ) ) ;
#8844=EDGE_LOOP ( 'NONE', ( #8914, #3913, #6348, #6802 ) ) ;
#8846=PRODUCT_DEFINITION ( 'UNKNOWN', '', #12333, #6498 ) ;
#8848=DIRECTION ( 'NONE',  ( 0.000000000000000000, -1.000000000000000000, 0.000000000000000000 ) ) ;
#8855=EDGE_CURVE ( 'NONE', #13498, #973, #289, .T. ) ;
#8864=CARTESIAN_POINT ( 'NONE',  ( 7.349173144666838020, 3.814570804032795692, -25.35250733039552884 ) ) ;
#8865=CARTESIAN_POINT ( 'NONE',  ( 0.3189473520463899647, 0.8338976723007026637, 3.612722554896655947 ) ) ;
#8870=EDGE_CURVE ( 'NONE', #8603, #6034, #3524, .T. ) ;
#8871=ORIENTED_EDGE ( 'NONE', *, *, #7256, .T. ) ;
#8877=DIRECTION ( 'NONE',  ( 0.08794243244722413366, 0.000000000000000000, 0.9961255586397056438 ) ) ;
#8883=ORIENTED_EDGE ( 'NONE', *, *, #935, .T. ) ;
#8886=CARTESIAN_POINT ( 'NONE',  ( 4.052988422354451004, 9.999999999999998224, -106.4147896264523467 ) ) ;
#8892=CARTESIAN_POINT ( 'NONE',  ( -45.52432922698630335, 15.00000000000539480, -160.5926188986776992 ) ) ;
#8899=AXIS2_PLACEMENT_3D ( 'NONE', #4199, #12463, #14571 ) ;
#8900=CARTESIAN_POINT ( 'NONE',  ( -3.345593546076259361, 10.60898574532662941, -45.14660385735189152 ) ) ;
#8902=CARTESIAN_POINT ( 'NONE',  ( -32.48742309669081862, 9.999999999999998224, -156.1716796081720133 ) ) ;
#8904=CARTESIAN_POINT ( 'NONE',  ( -68.19209817482972369, 15.00000000000174438, -203.2686135464926451 ) ) ;
#8905=CIRCLE ( 'NONE', #6184, 3.750000000000003109 ) ;
#8906=CARTESIAN_POINT ( 'NONE',  ( 0.9234955565201180550, -1.734723475976807094E-15, -138.4305453062657421 ) ) ;
#8908=CIRCLE ( 'NONE', #3975, 6.999999999999950262 ) ;
#8909=DIRECTION ( 'NONE',  ( -0.000000000000000000, 1.000000000000000000, -0.000000000000000000 ) ) ;
#8912=CARTESIAN_POINT ( 'NONE',  ( 3.230086961373113130, 5.000000000000000888, 5.208283729180105404 ) ) ;
#8914=ORIENTED_EDGE ( 'NONE', *, *, #11404, .F. ) ;
#8915=CARTESIAN_POINT ( 'NONE',  ( 7.786518181264857397, 5.211846493442710226, -20.40551834929134856 ) ) ;
#8921=CIRCLE ( 'NONE', #3484, 5.000000000000000000 ) ;
#8933=VERTEX_POINT ( 'NONE', #5004 ) ;
#8938=DIRECTION ( 'NONE',  ( -0.9961255586397050887, -0.000000000000000000, 0.08794243244723005948 ) ) ;
#8942=CARTESIAN_POINT ( 'NONE',  ( -60.91137729732987793, 5.000000000000000888, -175.0198515626273661 ) ) ;
#8943=CARTESIAN_POINT ( 'NONE',  ( 2.803776756569541284, 0.2483257210975995111, 1.809827704450910568 ) ) ;
#8948=ORIENTED_EDGE ( 'NONE', *, *, #2913, .T. ) ;
#8952=LINE ( 'NONE', #1773, #11688 ) ;
#8966=CARTESIAN_POINT ( 'NONE',  ( -14.68073284315481253, 7.499999999999991118, -92.37694453701993780 ) ) ;
#8967=CARTESIAN_POINT ( 'NONE',  ( -29.69515346086419072, 9.999999999999998224, -156.7390981038714983 ) ) ;
#8973=CARTESIAN_POINT ( 'NONE',  ( -3.332125856844564638, 10.29293441821257282, -44.11502059987310531 ) ) ;
#8976=CIRCLE ( 'NONE', #8218, 5.000000000000000000 ) ;
#8978=AXIS2_PLACEMENT_3D ( 'NONE', #13808, #12565, #11554 ) ;
#8979=DIRECTION ( 'NONE',  ( 0.000000000000000000, -1.000000000000000000, 0.000000000000000000 ) ) ;
#8981=DIRECTION ( 'NONE',  ( -0.08794243244722413366, 0.000000000000000000, -0.9961255586397056438 ) ) ;
#8988=CARTESIAN_POINT ( 'NONE',  ( 10.01939027896081669, 5.000000000000000888, -127.6977514918621637 ) ) ;
#9000=CARTESIAN_POINT ( 'NONE',  ( -7.885911378209643274, 13.39228090171942931, -104.2457333304612206 ) ) ;
#9001=CARTESIAN_POINT ( 'NONE',  ( -4.018470066652908734, 7.379999999999995453, -45.51728475810764962 ) ) ;
#9002=CARTESIAN_POINT ( 'NONE',  ( -25.82983890416511841, 15.00000000000000000, -142.4527639562402328 ) ) ;
#9008=ORIENTED_EDGE ( 'NONE', *, *, #6202, .F. ) ;
#9011=CARTESIAN_POINT ( 'NONE',  ( -17.32624372123753886, 2.500000000000000444, -122.3796757791585321 ) ) ;
#9016=DIRECTION ( 'NONE',  ( 0.08794243244722425856, 0.000000000000000000, 0.9961255586397054218 ) ) ;
#9018=CARTESIAN_POINT ( 'NONE',  ( -33.91109452335874153, 10.00000000000000178, -156.1716796081737471 ) ) ;
#9019=CARTESIAN_POINT ( 'NONE',  ( -47.48189921986828210, 15.00000000000000000, -141.5723758807981483 ) ) ;
#9025=EDGE_CURVE ( 'NONE', #12332, #15113, #10099, .T. ) ;
#9029=CARTESIAN_POINT ( 'NONE',  ( -9.302736714094232084, 2.500000000000000444, -123.7731201992051098 ) ) ;
#9037=CARTESIAN_POINT ( 'NONE',  ( -5.054995719515170904, 4.336808689942017736E-16, -105.8433260022760294 ) ) ;
#9041=ORIENTED_EDGE ( 'NONE', *, *, #12833, .T. ) ;
#9045=ADVANCED_FACE ( 'NONE', ( #4234 ), #11490, .F. ) ;
#9046=CARTESIAN_POINT ( 'NONE',  ( -48.42971706878667959, 9.999999999999998224, -163.2864622073098246 ) ) ;
#9047=ADVANCED_FACE ( 'NONE', ( #2139 ), #7728, .T. ) ;
#9058=DIRECTION ( 'NONE',  ( 0.08794243244723000397, 0.000000000000000000, 0.9961255586397049777 ) ) ;
#9062=CARTESIAN_POINT ( 'NONE',  ( 4.798865512804554534, 14.61883240900064607, 1.001995710397592498 ) ) ;
#9064=CARTESIAN_POINT ( 'NONE',  ( 10.01939027896081313, 9.999999999999998224, -127.6977514918621637 ) ) ;
#9065=CARTESIAN_POINT ( 'NONE',  ( -8.886921396801799489, 2.500000000000000444, -105.5168766094550250 ) ) ;
#9066=ORIENTED_EDGE ( 'NONE', *, *, #12215, .T. ) ;
#9073=ORIENTED_EDGE ( 'NONE', *, *, #13279, .F. ) ;
#9074=B_SPLINE_CURVE_WITH_KNOTS ( 'NONE', 3,
 ( #5012, #12115, #8715, #13289, #5244, #7392, #381, #10962, #13526, #9953, #4093, #2924, #1612, #1452, #13450, #4013, #2773, #6324, #1684, #2855, #13600, #7555, #12274, #7477, #456, #1533 ),
 .UNSPECIFIED., .F., .F.,
 ( 4, 2, 2, 2, 2, 2, 2, 2, 2, 2, 2, 2, 4 ),
 ( -8.569047602456792291E-05, 0.006541394408673478593, 0.009854936851022505842, 0.01316847929337153396, 0.01648202173572056381, 0.01979556417806959193, 0.02145233539924410598, 0.02310910662041862351, 0.02393749223100587881, 0.02476587784159313757, 0.02559426345218039980, 0.02600845625747404133, 0.02642264906276768632 ),
 .UNSPECIFIED. ) ;
#9077=CARTESIAN_POINT ( 'NONE',  ( -7.841189678847138467, 13.47270973785375148, -104.5808338560114663 ) ) ;
#9082=ORIENTED_EDGE ( 'NONE', *, *, #6102, .F. ) ;
#9094=CARTESIAN_POINT ( 'NONE',  ( 0.4903027347542082137, 3.623355825888509241, 5.553668143684391545 ) ) ;
#9098=EDGE_LOOP ( 'NONE', ( #13921, #14829, #1407, #12622, #2747 ) ) ;
#9100=FACE_OUTER_BOUND ( 'NONE', #5842, .T. ) ;
#9106=CARTESIAN_POINT ( 'NONE',  ( -64.15738946500745499, 15.00000000058060934, -182.2117518801574931 ) ) ;
#9114=CARTESIAN_POINT ( 'NONE',  ( -42.75031104224877510, 15.00000000000000000, -153.0915108332807790 ) ) ;
#9117=FACE_OUTER_BOUND ( 'NONE', #2264, .T. ) ;
#9118=DIRECTION ( 'NONE',  ( 0.000000000000000000, 1.000000000000000000, 0.000000000000000000 ) ) ;
#9125=EDGE_CURVE ( 'NONE', #2807, #2289, #12919, .T. ) ;
#9128=( BOUNDED_CURVE ( )  B_SPLINE_CURVE ( 3, ( #1398, #7417, #2796, #4872 ),
 .UNSPECIFIED., .F., .F. ) 
 B_SPLINE_CURVE_WITH_KNOTS ( ( 4, 4 ),
 ( 3.902948386497334887, 5.926982624441428094 ),
 .UNSPECIFIED. ) 
 CURVE ( )  GEOMETRIC_REPRESENTATION_ITEM ( )  RATIONAL_B_SPLINE_CURVE ( ( 1.000000000000000000, 0.6867676532959785529, 0.6867676532959785529, 1.000000000000000000 ) ) 
 REPRESENTATION_ITEM ( '' )  );
#9130=EDGE_CURVE ( 'NONE', #9880, #11483, #8976, .T. ) ;
#9133=CARTESIAN_POINT ( 'NONE',  ( -5.142992306533066937, 10.00000000000000178, -113.9900399291647659 ) ) ;
#9145=DIRECTION ( 'NONE',  ( 0.000000000000000000, -1.000000000000000000, 0.000000000000000000 ) ) ;
#9146=ORIENTED_EDGE ( 'NONE', *, *, #3152, .T. ) ;
#9150=VECTOR ( 'NONE', #13796, 1000.000000000000114 ) ;
#9152=AXIS2_PLACEMENT_3D ( 'NONE', #8716, #13452, #5245 ) ;
#9153=CARTESIAN_POINT ( 'NONE',  ( -65.53364736412719083, 10.00000000000000000, -203.4171941195418754 ) ) ;
#9162=ORIENTED_EDGE ( 'NONE', *, *, #4578, .T. ) ;
#9174=DIRECTION ( 'NONE',  ( 0.000000000000000000, -1.000000000000000000, 0.000000000000000000 ) ) ;
#9184=CARTESIAN_POINT ( 'NONE',  ( -2.263856268268321870, 0.5959694101612306172, -137.7878962296450140 ) ) ;
#9186=CARTESIAN_POINT ( 'NONE',  ( -3.435988495369542761, 4.336808689942017736E-16, -118.2234283277027487 ) ) ;
#9193=CIRCLE ( 'NONE', #9972, 2.326940983401415419 ) ;
#9194=CARTESIAN_POINT ( 'NONE',  ( -56.64898049675471015, 9.999999999999998224, -176.0284089207397358 ) ) ;
#9206=DIRECTION ( 'NONE',  ( -0.9961255586397050887, 0.000000000000000000, 0.08794243244723005948 ) ) ;
#9207=CARTESIAN_POINT ( 'NONE',  ( -6.435381799839732686, 15.00000000000000000, -129.7490639376177626 ) ) ;
#9209=CARTESIAN_POINT ( 'NONE',  ( 3.263686447136663116, 10.81848946384218912, 5.150370076467488012 ) ) ;
#9211=CARTESIAN_POINT ( 'NONE',  ( -8.959045066952105785, 11.66127071243621316, -104.5743688023792828 ) ) ;
#9212=CARTESIAN_POINT ( 'NONE',  ( -3.955596480971199203, 9.999999999999998224, -118.5438621456188173 ) ) ;
#9217=CIRCLE ( 'NONE', #346, 2.326940983401415419 ) ;
#9220=CARTESIAN_POINT ( 'NONE',  ( -65.53364736412719083, 10.00000000000000000, -203.4171941195418754 ) ) ;
#9224=CARTESIAN_POINT ( 'NONE',  ( -56.93825309386823363, 9.999999999999998224, -152.5131710537346805 ) ) ;
#9226=DIRECTION ( 'NONE',  ( 0.000000000000000000, 0.000000000000000000, 1.000000000000000000 ) ) ;
#9231=B_SPLINE_CURVE_WITH_KNOTS ( 'NONE', 3,
 ( #4031, #6489, #5260, #6412, #8886, #12441 ),
 .UNSPECIFIED., .F., .F.,
 ( 4, 2, 4 ),
 ( 1.734723475976807094E-18, 0.006358156888686363438, 0.01271631377737272514 ),
 .UNSPECIFIED. ) ;
#9232=FACE_BOUND ( 'NONE', #11478, .T. ) ;
#9234=ORIENTED_EDGE ( 'NONE', *, *, #1189, .F. ) ;
#9245=EDGE_LOOP ( 'NONE', ( #2218, #4598, #7364 ) ) ;
#9252=CYLINDRICAL_SURFACE ( 'NONE', #5475, 6.999999999999950262 ) ;
#9261=CARTESIAN_POINT ( 'NONE',  ( -63.60348060676461301, 15.00000000000000000, -180.2685449772604045 ) ) ;
#9265=CARTESIAN_POINT ( 'NONE',  ( -2.783652268060036850, 4.336808689942017736E-16, -111.2342432958199367 ) ) ;
#9268=CARTESIAN_POINT ( 'NONE',  ( -22.00712180358226533, 9.999999999999998224, -133.4290821151669206 ) ) ;
#9272=CARTESIAN_POINT ( 'NONE',  ( -65.95211062277772385, 15.00000000000000000, -188.5353794584724483 ) ) ;
#9274=VERTEX_POINT ( 'NONE', #3991 ) ;
#9275=FACE_OUTER_BOUND ( 'NONE', #5047, .T. ) ;
#9276=FACE_OUTER_BOUND ( 'NONE', #13734, .T. ) ;
#9281=EDGE_CURVE ( 'NONE', #1413, #10593, #9723, .T. ) ;
#9283=FACE_OUTER_BOUND ( 'NONE', #11461, .T. ) ;
#9284=CARTESIAN_POINT ( 'NONE',  ( -7.676911175420229050, 13.35713519559141638, -104.8728676159044966 ) ) ;
#9285=CARTESIAN_POINT ( 'NONE',  ( -9.541039381253360929, 10.00000000000000355, -124.0820960698317066 ) ) ;
#9288=CARTESIAN_POINT ( 'NONE',  ( -6.328185151855761248, 14.51326209089783248, -103.7941250579298895 ) ) ;
#9289=DIRECTION ( 'NONE',  ( 0.000000000000000000, -1.000000000000000000, 0.000000000000000000 ) ) ;
#9295=CARTESIAN_POINT ( 'NONE',  ( -7.414180893040303921, 4.336808689942017736E-16, -103.4903665579796410 ) ) ;
#9298=EDGE_CURVE ( 'NONE', #12551, #10617, #435, .T. ) ;
#9299=CARTESIAN_POINT ( 'NONE',  ( -50.48705678711692002, 15.00000000000000000, -152.0942671431891142 ) ) ;
#9302=ADVANCED_FACE ( 'NONE', ( #5144 ), #10137, .T. ) ;
#9306=DIRECTION ( 'NONE',  ( 0.08794243244722413366, 0.000000000000000000, 0.9961255586397056438 ) ) ;
#9308=CARTESIAN_POINT ( 'NONE',  ( -7.768256104199515732, 15.00000000000000000, -129.7494471864078491 ) ) ;
#9324=CARTESIAN_POINT ( 'NONE',  ( 1.818748563159308773, 10.00000000000000178, -137.3269871014800003 ) ) ;
#9333=DIRECTION ( 'NONE',  ( 0.08794243244722427244, 0.000000000000000000, 0.9961255586397056438 ) ) ;
#9336=CARTESIAN_POINT ( 'NONE',  ( -66.92994642267662186, 14.64660082127883811, -194.1686397956628127 ) ) ;
#9337=CARTESIAN_POINT ( 'NONE',  ( -0.2256904824989624803, 2.216033281584864678, -138.2198612530219179 ) ) ;
#9343=ORIENTED_EDGE ( 'NONE', *, *, #11314, .T. ) ;
#9347=ORIENTED_EDGE ( 'NONE', *, *, #3758, .F. ) ;
#9354=CARTESIAN_POINT ( 'NONE',  ( -8.205916711996726676, 7.499999999999991118, -92.94857034792688921 ) ) ;
#9360=CARTESIAN_POINT ( 'NONE',  ( -63.68025975125228655, 12.30547768668273001, -202.4996554109041540 ) ) ;
#9369=CARTESIAN_POINT ( 'NONE',  ( -55.30796743870962473, 9.999999999999998224, -150.1894123919774700 ) ) ;
#9376=DIRECTION ( 'NONE',  ( 0.000000000000000000, -1.000000000000000000, 0.000000000000000000 ) ) ;
#9383=ADVANCED_FACE ( 'NONE', ( #3629 ), #3909, .T. ) ;
#9384=ORIENTED_EDGE ( 'NONE', *, *, #14442, .F. ) ;
#9388=ORIENTED_EDGE ( 'NONE', *, *, #1558, .T. ) ;
#9390=ADVANCED_FACE ( 'NONE', ( #13300 ), #6016, .F. ) ;
#9392=TOROIDAL_SURFACE ( 'NONE', #3475, 11.99999999999994138, 5.000000000000000000 ) ;
#9394=AXIS2_PLACEMENT_3D ( 'NONE', #4725, #6100, #8193 ) ;
#9403=CIRCLE ( 'NONE', #4715, 4.999999999999998224 ) ;
#9405=ORIENTED_EDGE ( 'NONE', *, *, #3387, .T. ) ;
#9419=AXIS2_PLACEMENT_3D ( 'NONE', #15272, #9226, #12943 ) ;
#9423=CARTESIAN_POINT ( 'NONE',  ( -7.004554049466862331, -1.494908006873514903E-15, -104.1936728214014636 ) ) ;
#9426=CARTESIAN_POINT ( 'NONE',  ( -5.997216956328301762, 9.999999999999998224, -109.1002327433092915 ) ) ;
#9427=EDGE_CURVE ( 'NONE', #2695, #1413, #8952, .T. ) ;
#9428=CARTESIAN_POINT ( 'NONE',  ( 0.4539486869273933189, 11.45452110608535179, 2.843399008810883366 ) ) ;
#9435=DIRECTION ( 'NONE',  ( -0.000000000000000000, -1.000000000000000000, -0.000000000000000000 ) ) ;
#9436=CARTESIAN_POINT ( 'NONE',  ( -2.524281728693007043, 7.379999999999995453, -45.64919840677852392 ) ) ;
#9438=CARTESIAN_POINT ( 'NONE',  ( -25.68053481550299111, -5.000000000000000888, -142.4798935003980773 ) ) ;
#9441=CARTESIAN_POINT ( 'NONE',  ( -64.64338443439244486, 14.97268095330599458, -185.5119884393937184 ) ) ;
#9442=ORIENTED_EDGE ( 'NONE', *, *, #13475, .F. ) ;
#9443=EDGE_LOOP ( 'NONE', ( #499, #9008 ) ) ;
#9444=CARTESIAN_POINT ( 'NONE',  ( -4.724265062691370254, 4.336808689942017736E-16, -106.3929389433132400 ) ) ;
#9464=DIRECTION ( 'NONE',  ( 0.000000000000000000, -1.000000000000000000, 0.000000000000000000 ) ) ;
#9470=ORIENTED_EDGE ( 'NONE', *, *, #8183, .F. ) ;
#9474=CARTESIAN_POINT ( 'NONE',  ( -7.262467309341673172, 2.500000000000000444, -120.6566834617809008 ) ) ;
#9478=CARTESIAN_POINT ( 'NONE',  ( 1.893911505664648054, 5.000000000000000888, -1.663006917529762152 ) ) ;
#9480=VERTEX_POINT ( 'NONE', #6257 ) ;
#9481=VECTOR ( 'NONE', #4133, 1000.000000000000000 ) ;
#9485=CARTESIAN_POINT ( 'NONE',  ( -67.61300297071448995, 11.57753352799745450, -203.9033284969760302 ) ) ;
#9488=VECTOR ( 'NONE', #6185, 1000.000000000000227 ) ;
#9491=EDGE_CURVE ( 'NONE', #9927, #8353, #6482, .T. ) ;
#9492=CARTESIAN_POINT ( 'NONE',  ( -32.49979969806455671, 5.000000000000000888, -156.1716796081737186 ) ) ;
#9493=CARTESIAN_POINT ( 'NONE',  ( -17.21625625355589762, 0.5158708274082715040, -130.3505683864442517 ) ) ;
#9494=ORIENTED_EDGE ( 'NONE', *, *, #11100, .T. ) ;
#9498=CARTESIAN_POINT ( 'NONE',  ( -61.24268700632901385, 9.999999999999998224, -190.3758570956422886 ) ) ;
#9502=CARTESIAN_POINT ( 'NONE',  ( -2.850962077074172818, 15.00000000000000000, -123.0244887426839284 ) ) ;
#9510=CARTESIAN_POINT ( 'NONE',  ( 1.959483780728543234, 13.86208356520140583, 1.676081107764974654 ) ) ;
#9511=CARTESIAN_POINT ( 'NONE',  ( -3.982786732524661755, 11.11191381569369696, -46.53277667289602704 ) ) ;
#9512=EDGE_CURVE ( 'NONE', #11588, #12487, #6263, .T. ) ;
#9515=EDGE_CURVE ( 'NONE', #14402, #5826, #594, .T. ) ;
#9516=DIRECTION ( 'NONE',  ( -0.000000000000000000, -1.000000000000000000, -0.000000000000000000 ) ) ;
#9518=CARTESIAN_POINT ( 'NONE',  ( -9.240119717576693148, 10.34205777577377106, -104.6630069175297848 ) ) ;
#9519=CARTESIAN_POINT ( 'NONE',  ( -64.71949702661652282, 14.00248011326570641, -198.7579215201884324 ) ) ;
#9522=CARTESIAN_POINT ( 'NONE',  ( -2.633607816330602258, 4.336808689942017736E-16, -112.6800763249241015 ) ) ;
#9530=CARTESIAN_POINT ( 'NONE',  ( -51.27420002594509896, 15.00000000000000000, -153.1456608506698274 ) ) ;
#9538=CARTESIAN_POINT ( 'NONE',  ( -0.08788760335059413176, 15.00000000000000178, -112.5413916789569129 ) ) ;
#9540=VERTEX_POINT ( 'NONE', #4103 ) ;
#9541=ORIENTED_EDGE ( 'NONE', *, *, #11314, .F. ) ;
#9545=ORIENTED_EDGE ( 'NONE', *, *, #5327, .F. ) ;
#9548=CARTESIAN_POINT ( 'NONE',  ( -6.764825266738188070, 1.389134033497039984E-16, -104.1458598414970993 ) ) ;
#9551=CARTESIAN_POINT ( 'NONE',  ( 0.03998412334521189021, 2.500000000000000444, 0.4529009045602680472 ) ) ;
#9552=AXIS2_PLACEMENT_3D ( 'NONE', #7528, #7832, #11081 ) ;
#9553=ORIENTED_EDGE ( 'NONE', *, *, #6501, .F. ) ;
#9557=CARTESIAN_POINT ( 'NONE',  ( -64.02082625067613719, 12.73504901638480824, -210.7145675674813390 ) ) ;
#9563=DIRECTION ( 'NONE',  ( 0.9982196940171963462, 0.000000000000000000, -0.05964429961207440289 ) ) ;
#9564=ORIENTED_EDGE ( 'NONE', *, *, #979, .F. ) ;
#9567=CARTESIAN_POINT ( 'NONE',  ( -66.90237725336980645, 10.00000000000000178, -173.2413874344579483 ) ) ;
#9571=CARTESIAN_POINT ( 'NONE',  ( -6.078370696271480078, 9.999999999999998224, -118.0777554208214895 ) ) ;
#9572=CARTESIAN_POINT ( 'NONE',  ( 3.834616502859925724, 14.88006226842800750, -1.031466025772356021 ) ) ;
#9573=CARTESIAN_POINT ( 'NONE',  ( -15.11050069339551705, 15.00000000000000000, -146.5097068764709718 ) ) ;
#9574=EDGE_CURVE ( 'NONE', #5270, #14745, #5277, .T. ) ;
#9578=CARTESIAN_POINT ( 'NONE',  ( 0.2625675448779695720, 5.000000000000000888, 2.974107436473219401 ) ) ;
#9580=CARTESIAN_POINT ( 'NONE',  ( 4.871047274049744580, 14.73417332752070230, 0.4127525086329914550 ) ) ;
#9587=CARTESIAN_POINT ( 'NONE',  ( -63.53877297815559189, 11.93648641405965627, -202.8585599469136298 ) ) ;
#9588=ORIENTED_EDGE ( 'NONE', *, *, #10461, .T. ) ;
#9590=ORIENTED_EDGE ( 'NONE', *, *, #7139, .T. ) ;
#9591=CARTESIAN_POINT ( 'NONE',  ( -7.473411123654440047, 2.500000000000000444, -120.9918979907378969 ) ) ;
#9597=EDGE_CURVE ( 'NONE', #8123, #8666, #13436, .T. ) ;
#9601=CARTESIAN_POINT ( 'NONE',  ( -70.02757949954413164, 15.00000000000000000, -189.2441461652899193 ) ) ;
#9608=DIRECTION ( 'NONE',  ( 0.000000000000000000, 0.000000000000000000, -1.000000000000000000 ) ) ;
#9609=ORIENTED_EDGE ( 'NONE', *, *, #4980, .F. ) ;
#9612=EDGE_LOOP ( 'NONE', ( #13483, #5953, #809, #2642 ) ) ;
#9620=EDGE_CURVE ( 'NONE', #10989, #6383, #10205, .T. ) ;
#9622=VECTOR ( 'NONE', #5652, 1000.000000000000000 ) ;
#9623=CARTESIAN_POINT ( 'NONE',  ( -5.154409584717598136, 2.500000000000000888, -114.2587629972653360 ) ) ;
#9625=CARTESIAN_POINT ( 'NONE',  ( -60.52034210924323787, 15.00000000000000178, -172.5548809364130705 ) ) ;
#9628=CARTESIAN_POINT ( 'NONE',  ( 7.427446726622309647, 5.321094445766562764, -26.41501464507892294 ) ) ;
#9636=CARTESIAN_POINT ( 'NONE',  ( -63.64301171304934002, 12.20966866758287850, -202.5945476619451142 ) ) ;
#9641=CIRCLE ( 'NONE', #12113, 5.000000000000010658 ) ;
#9646=ORIENTED_EDGE ( 'NONE', *, *, #15104, .T. ) ;
#9649=CARTESIAN_POINT ( 'NONE',  ( -7.860067106259624126, 0.2490491084495508878, -104.5911971696796599 ) ) ;
#9653=CARTESIAN_POINT ( 'NONE',  ( -6.078370696252020089, 15.00000000000000000, -118.0777554208285665 ) ) ;
#9659=CARTESIAN_POINT ( 'NONE',  ( -3.357934391919316308, 10.63007166822767680, -45.36073661948301350 ) ) ;
#9661=CARTESIAN_POINT ( 'NONE',  ( 4.619430714695810458, 14.36106363918124096, 1.856711022170560499 ) ) ;
#9662=TOROIDAL_SURFACE ( 'NONE', #290, 9.499999999999941380, 2.500000000000000000 ) ;
#9664=ADVANCED_FACE ( 'NONE', ( #14776 ), #5477, .T. ) ;
#9670=ORIENTED_EDGE ( 'NONE', *, *, #3850, .T. ) ;
#9674=CARTESIAN_POINT ( 'NONE',  ( -5.114912396279929219, 1.317715228986242930E-13, -113.5322278711262101 ) ) ;
#9678=CARTESIAN_POINT ( 'NONE',  ( -17.80444947669341360, 1.250643348872871874, -129.6916459345341650 ) ) ;
#9679=EDGE_LOOP ( 'NONE', ( #7111, #3027 ) ) ;
#9684=CARTESIAN_POINT ( 'NONE',  ( -64.33489900431855801, 14.99999999999999822, -199.0892663431833114 ) ) ;
#9693=VERTEX_POINT ( 'NONE', #10302 ) ;
#9694=ADVANCED_FACE ( 'NONE', ( #1032 ), #1829, .T. ) ;
#9696=VERTEX_POINT ( 'NONE', #15266 ) ;
#9707=CARTESIAN_POINT ( 'NONE',  ( -7.789898380477169759, 2.500000000000000888, -121.5509192307600586 ) ) ;
#9708=CARTESIAN_POINT ( 'NONE',  ( -46.45656087453430416, 10.00000000000000000, -161.4072483220047047 ) ) ;
#9709=CARTESIAN_POINT ( 'NONE',  ( -47.48189921986827500, 10.00000000000000000, -141.5723758807981483 ) ) ;
#9712=EDGE_CURVE ( 'NONE', #9696, #2695, #9217, .T. ) ;
#9723=( BOUNDED_CURVE ( )  B_SPLINE_CURVE ( 3, ( #1592, #11019, #792, #5496 ),
 .UNSPECIFIED., .F., .T. ) 
 B_SPLINE_CURVE_WITH_KNOTS ( ( 4, 4 ),
 ( 4.862919461057368054, 6.283185307179586232 ),
 .UNSPECIFIED. ) 
 CURVE ( )  GEOMETRIC_REPRESENTATION_ITEM ( )  RATIONAL_B_SPLINE_CURVE ( ( 1.000000000000000000, 0.8388501503673407855, 0.8388501503673407855, 1.000000000000000000 ) ) 
 REPRESENTATION_ITEM ( '' )  );
#9724=CARTESIAN_POINT ( 'NONE',  ( -67.63300625564886559, 12.31334483152244452, -203.1194105661006404 ) ) ;
#9732=AXIS2_PLACEMENT_3D ( 'NONE', #11014, #429, #8690 ) ;
#9736=CARTESIAN_POINT ( 'NONE',  ( -9.220836928148449019, 2.148733653916489406, -104.6587943809631156 ) ) ;
#9739=DIRECTION ( 'NONE',  ( -1.000000000000000000, -0.000000000000000000, -0.000000000000000000 ) ) ;
#9740=CARTESIAN_POINT ( 'NONE',  ( 0.5667764127758471160, 11.79980322240585622, 2.765452941203609072 ) ) ;
#9741=CARTESIAN_POINT ( 'NONE',  ( -1.843872751587880776, 15.00000000000000000, -133.9216539038988003 ) ) ;
#9746=CARTESIAN_POINT ( 'NONE',  ( -4.180890075922867766, 10.20972115200646257, -47.12409091164020936 ) ) ;
#9748=CARTESIAN_POINT ( 'NONE',  ( 0.4077082524506932537, 11.25215624784117274, 2.875278165707306766 ) ) ;
#9752=DIRECTION ( 'NONE',  ( 0.000000000000000000, -1.000000000000000000, 0.000000000000000000 ) ) ;
#9759=CARTESIAN_POINT ( 'NONE',  ( -5.689254933302104966, 2.500000000000000444, -117.0567294044985829 ) ) ;
#9766=CARTESIAN_POINT ( 'NONE',  ( -64.68844199977228016, 15.00000000000000000, -197.4748239606827553 ) ) ;
#9771=LINE ( 'NONE', #12241, #12091 ) ;
#9772=ORIENTED_EDGE ( 'NONE', *, *, #2239, .F. ) ;
#9781=ADVANCED_FACE ( 'NONE', ( #11466 ), #3533, .T. ) ;
#9787=CARTESIAN_POINT ( 'NONE',  ( -5.511151914899733661, 2.500000000000000000, -116.3187303629814551 ) ) ;
#9788=CARTESIAN_POINT ( 'NONE',  ( -59.56434992273744200, 9.999999999999994671, -183.8842187088368121 ) ) ;
#9791=DIRECTION ( 'NONE',  ( -0.9961255586397049777, -0.000000000000000000, 0.08794243244723005948 ) ) ;
#9798=EDGE_CURVE ( 'NONE', #5990, #5060, #10830, .T. ) ;
#9799=CARTESIAN_POINT ( 'NONE',  ( -64.96615686214629193, 15.33131988198272744, -206.4716339831645087 ) ) ;
#9803=DIRECTION ( 'NONE',  ( 0.000000000000000000, -1.000000000000000000, 0.000000000000000000 ) ) ;
#9808=CARTESIAN_POINT ( 'NONE',  ( -48.59171165233305345, 9.999999999999998224, -142.5285849061865804 ) ) ;
#9819=CARTESIAN_POINT ( 'NONE',  ( 0.09756493787362907621, 2.578155857656784455, 1.105119855559491437 ) ) ;
#9821=CARTESIAN_POINT ( 'NONE',  ( 4.913233174174957085, 14.82748211479344747, -0.2684095748386393088 ) ) ;
#9825=CARTESIAN_POINT ( 'NONE',  ( -25.82983890416511841, 5.000000000000000000, -142.4527639562402328 ) ) ;
#9829=ORIENTED_EDGE ( 'NONE', *, *, #8181, .T. ) ;
#9835=ORIENTED_EDGE ( 'NONE', *, *, #10998, .T. ) ;
#9838=CARTESIAN_POINT ( 'NONE',  ( -65.10000466134623309, 15.00000000000000000, -191.5398038754765935 ) ) ;
#9845=VERTEX_POINT ( 'NONE', #7430 ) ;
#9846=CARTESIAN_POINT ( 'NONE',  ( -4.090890948359609425, 15.00000000000000000, -103.1929727064838289 ) ) ;
#9848=ORIENTED_EDGE ( 'NONE', *, *, #6268, .F. ) ;
#9855=CARTESIAN_POINT ( 'NONE',  ( -37.86885108244810283, 9.999999999999998224, -139.8897182464016566 ) ) ;
#9857=DIRECTION ( 'NONE',  ( 0.7779936141972744190, 0.000000000000000000, 0.6282721832679388774 ) ) ;
#9861=CARTESIAN_POINT ( 'NONE',  ( -66.44604053271804389, 5.000000000000000888, -157.9117883361228394 ) ) ;
#9864=VERTEX_POINT ( 'NONE', #6280 ) ;
#9873=CARTESIAN_POINT ( 'NONE',  ( -49.26721305452313260, 5.000000000000000888, -156.1716796081737471 ) ) ;
#9878=FACE_OUTER_BOUND ( 'NONE', #11042, .T. ) ;
#9879=AXIS2_PLACEMENT_3D ( 'NONE', #12691, #6590, #11299 ) ;
#9880=VERTEX_POINT ( 'NONE', #2414 ) ;
#9882=CARTESIAN_POINT ( 'NONE',  ( -9.108435135009571582, 1.571332947940224045, -105.1067939785190219 ) ) ;
#9885=CARTESIAN_POINT ( 'NONE',  ( -8.241439964468746382, 15.00000000000000888, -106.0832790697330239 ) ) ;
#9888=DIRECTION ( 'NONE',  ( 0.05964429961207241837, 0.000000000000000000, 0.9982196940171965682 ) ) ;
#9894=CARTESIAN_POINT ( 'NONE',  ( -4.119321715443209797, 10.47408532934288772, -46.53149779072169423 ) ) ;
#9898=DIRECTION ( 'NONE',  ( -0.9961255586397050887, 0.000000000000000000, 0.08794243244723005948 ) ) ;
#9902=AXIS2_PLACEMENT_3D ( 'NONE', #4977, #9464, #8295 ) ;
#9903=( BOUNDED_CURVE ( )  B_SPLINE_CURVE ( 3, ( #8020, #2157, #15156, #3382 ),
 .UNSPECIFIED., .F., .T. ) 
 B_SPLINE_CURVE_WITH_KNOTS ( ( 4, 4 ),
 ( 0.000000000000000000, 0.1427305759106287653 ),
 .UNSPECIFIED. ) 
 CURVE ( )  GEOMETRIC_REPRESENTATION_ITEM ( )  RATIONAL_B_SPLINE_CURVE ( ( 1.000000000000000000, 0.9983030522886272573, 0.9983030522886272573, 1.000000000000000000 ) ) 
 REPRESENTATION_ITEM ( '' )  );
#9905=EDGE_CURVE ( 'NONE', #3117, #5060, #6979, .T. ) ;
#9915=( BOUNDED_CURVE ( )  B_SPLINE_CURVE ( 3, ( #14555, #14637, #11057, #6570 ),
 .UNSPECIFIED., .F., .F. ) 
 B_SPLINE_CURVE_WITH_KNOTS ( ( 4, 4 ),
 ( 0.3190780441241196641, 2.822514609465673452 ),
 .UNSPECIFIED. ) 
 CURVE ( )  GEOMETRIC_REPRESENTATION_ITEM ( )  RATIONAL_B_SPLINE_CURVE ( ( 1.000000000000000000, 0.5424608492517398739, 0.5424608492517398739, 1.000000000000000000 ) ) 
 REPRESENTATION_ITEM ( '' )  );
#9918=CARTESIAN_POINT ( 'NONE',  ( -70.04737159589244300, 9.999999999999998224, -194.4639900966930099 ) ) ;
#9919=B_SPLINE_CURVE_WITH_KNOTS ( 'NONE', 3,
 ( #564, #14798, #5275, #5200, #8973, #4193, #7814, #8900, #12526, #13552, #8671, #12300, #3030, #13704, #485, #4124, #10133, #8825 ),
 .UNSPECIFIED., .F., .F.,
 ( 4, 2, 2, 2, 2, 2, 2, 2, 4 ),
 ( 0.000000000000000000, 0.0006487559250799439540, 0.001297511850159887908, 0.001946267775239831754, 0.002595023700319775816, 0.003243779625399719879, 0.003892535550479663507, 0.004541291475559607570, 0.005190047400639551632 ),
 .UNSPECIFIED. ) ;
#9922=CARTESIAN_POINT ( 'NONE',  ( -7.068384139542111200, 10.00000000000000355, -107.3966098791943864 ) ) ;
#9927=VERTEX_POINT ( 'NONE', #7352 ) ;
#9945=ORIENTED_EDGE ( 'NONE', *, *, #9130, .F. ) ;
#9948=AXIS2_PLACEMENT_3D ( 'NONE', #13824, #3226, #2077 ) ;
#9950=CARTESIAN_POINT ( 'NONE',  ( 0.2677563320781928824, 0.4815089180969744365, 3.032880925044830978 ) ) ;
#9953=CARTESIAN_POINT ( 'NONE',  ( -67.35192000380439481, 14.27092917653249238, -197.4726913168000237 ) ) ;
#9955=ORIENTED_EDGE ( 'NONE', *, *, #14342, .F. ) ;
#9958=CARTESIAN_POINT ( 'NONE',  ( -4.018470066652908734, 7.379999999999995453, -45.51728475810764962 ) ) ;
#9962=DIRECTION ( 'NONE',  ( 0.000000000000000000, 0.000000000000000000, -1.000000000000000000 ) ) ;
#9963=CARTESIAN_POINT ( 'NONE',  ( -9.623069100187665370, 4.336808689942017736E-16, -128.0716982634005774 ) ) ;
#9972=AXIS2_PLACEMENT_3D ( 'NONE', #8667, #13398, #11064 ) ;
#9976=CARTESIAN_POINT ( 'NONE',  ( -1.376260179405573547, 0.000000000000000000, -106.6458321843530541 ) ) ;
#9977=CARTESIAN_POINT ( 'NONE',  ( -30.85915506350906412, 15.00000000000000000, -156.4241655054801754 ) ) ;
#9984=AXIS2_PLACEMENT_3D ( 'NONE', #11094, #5307, #514 ) ;
#9986=CARTESIAN_POINT ( 'NONE',  ( -25.97807323962435078, 15.00000000000000000, -142.5647913107548277 ) ) ;
#9999=CARTESIAN_POINT ( 'NONE',  ( -20.05675593593863582, 15.00000000000000000, -128.8251628084967706 ) ) ;
#10006=ADVANCED_BREP_SHAPE_REPRESENTATION ( '', ( #12195, #9419 ), #11867 ) ;
#10011=EDGE_LOOP ( 'NONE', ( #11625, #3239, #13344, #9541 ) ) ;
#10015=CARTESIAN_POINT ( 'NONE',  ( -7.397649731168717935, 2.500000000000001332, -106.9840814774545237 ) ) ;
#10027=CARTESIAN_POINT ( 'NONE',  ( -33.91109452335874153, 5.000000000000000888, -156.1716796081737471 ) ) ;
#10028=CARTESIAN_POINT ( 'NONE',  ( 0.2402936566864277979, 0.3344966542995999603, 2.721810693018832161 ) ) ;
#10038=CARTESIAN_POINT ( 'NONE',  ( -7.267596910945437472, 14.99999999999849187, -107.1579542029594876 ) ) ;
#10039=DIRECTION ( 'NONE',  ( 0.003262051938530752433, 0.000000000000000000, 0.9999946794944213346 ) ) ;
#10048=CARTESIAN_POINT ( 'NONE',  ( 3.659874141851102713, 14.82748211452489961, -0.4834174797602786011 ) ) ;
#10054=VECTOR ( 'NONE', #6127, 1000.000000000000000 ) ;
#10055=CARTESIAN_POINT ( 'NONE',  ( -42.91596092838683774, 9.999999999999998224, -158.7990843558010852 ) ) ;
#10072=FACE_OUTER_BOUND ( 'NONE', #3720, .T. ) ;
#10074=CARTESIAN_POINT ( 'NONE',  ( 2.011321487292375032, 5.000000000000000888, -137.8771695030452520 ) ) ;
#10075=DIRECTION ( 'NONE',  ( -0.9961255586397056438, -0.000000000000000000, 0.08794243244722427244 ) ) ;
#10076=ORIENTED_EDGE ( 'NONE', *, *, #6589, .T. ) ;
#10084=EDGE_LOOP ( 'NONE', ( #1635, #12476, #15001, #8148, #8433 ) ) ;
#10087=CARTESIAN_POINT ( 'NONE',  ( -8.102584368418263239, 2.500000000000000888, -106.2168020716806467 ) ) ;
#10088=LINE ( 'NONE', #11091, #4250 ) ;
#10098=ORIENTED_EDGE ( 'NONE', *, *, #8268, .F. ) ;
#10099=LINE ( 'NONE', #12649, #13669 ) ;
#10102=CARTESIAN_POINT ( 'NONE',  ( 2.757434015334491395, 0.1558106922034525610, 1.501509930864733056 ) ) ;
#10129=ORIENTED_EDGE ( 'NONE', *, *, #11678, .T. ) ;
#10131=FACE_OUTER_BOUND ( 'NONE', #14618, .T. ) ;
#10133=CARTESIAN_POINT ( 'NONE',  ( -3.711466206438381654, 9.806991768140566279, -47.72538388426938383 ) ) ;
#10134=CIRCLE ( 'NONE', #13107, 5.000000000000002665 ) ;
#10137=CYLINDRICAL_SURFACE ( 'NONE', #5513, 4.999999999999995559 ) ;
#10141=CARTESIAN_POINT ( 'NONE',  ( -68.82095148260327733, 9.999999999999998224, -201.5743162695746662 ) ) ;
#10144=EDGE_CURVE ( 'NONE', #5809, #7071, #9919, .T. ) ;
#10147=AXIS2_PLACEMENT_3D ( 'NONE', #718, #11227, #8981 ) ;
#10151=CARTESIAN_POINT ( 'NONE',  ( -1.437999228988334544, 8.673617379884035472E-16, -140.6782968106692522 ) ) ;
#10159=EDGE_LOOP ( 'NONE', ( #10232, #4506, #14536, #8258 ) ) ;
#10162=AXIS2_PLACEMENT_3D ( 'NONE', #11817, #4, #6810 ) ;
#10164=CARTESIAN_POINT ( 'NONE',  ( -5.378945654756269512, 14.88217507582766963, -103.5310234877412796 ) ) ;
#10165=EDGE_CURVE ( 'NONE', #12545, #10989, #12425, .T. ) ;
#10169=VECTOR ( 'NONE', #13743, 1000.000000000000000 ) ;
#10182=FACE_OUTER_BOUND ( 'NONE', #10613, .T. ) ;
#10184=CARTESIAN_POINT ( 'NONE',  ( 2.530298019944475563, 8.673617379884035472E-16, 0.2330448234422082265 ) ) ;
#10192=DIRECTION ( 'NONE',  ( 0.7859448108640930686, 0.000000000000000000, -0.6182966555592913638 ) ) ;
#10195=AXIS2_PLACEMENT_3D ( 'NONE', #8708, #2849, #7548 ) ;
#10196=CARTESIAN_POINT ( 'NONE',  ( -7.754603562235517167, 2.500000000000000444, -121.4663199874671307 ) ) ;
#10200=ORIENTED_EDGE ( 'NONE', *, *, #8092, .T. ) ;
#10201=CARTESIAN_POINT ( 'NONE',  ( -3.813985985191490347, 9.650666666666664284, -43.20108978589184545 ) ) ;
#10205=CIRCLE ( 'NONE', #5029, 3.500000000000013323 ) ;
#10209=DIRECTION ( 'NONE',  ( 0.000000000000000000, 1.000000000000000000, 0.000000000000000000 ) ) ;
#10210=CARTESIAN_POINT ( 'NONE',  ( -39.01706460775102414, 15.00000000000000000, -156.9624841731871072 ) ) ;
#10213=CARTESIAN_POINT ( 'NONE',  ( -9.110371329404767238, 15.00000000000119194, -123.5182978442195463 ) ) ;
#10214=DIRECTION ( 'NONE',  ( 0.000000000000000000, -1.000000000000000000, 0.000000000000000000 ) ) ;
#10224=CARTESIAN_POINT ( 'NONE',  ( -5.622987266627582414, 14.75541105728024682, -103.8730693452872771 ) ) ;
#10229=CIRCLE ( 'NONE', #6761, 14.80000000000025651 ) ;
#10231=CARTESIAN_POINT ( 'NONE',  ( 8.881449363785039353, 15.00000000000000000, -2.080517014814270205 ) ) ;
#10232=ORIENTED_EDGE ( 'NONE', *, *, #13499, .T. ) ;
#10238=EDGE_LOOP ( 'NONE', ( #7873, #8328, #14888, #4215 ) ) ;
#10242=CARTESIAN_POINT ( 'NONE',  ( -8.373832254232995709, 12.83239838503939900, -104.7981674252878008 ) ) ;
#10253=EDGE_CURVE ( 'NONE', #15113, #13758, #13677, .T. ) ;
#10258=CARTESIAN_POINT ( 'NONE',  ( 0.2611509734078907852, 4.672652403575303204, 2.958061905235128464 ) ) ;
#10264=EDGE_CURVE ( 'NONE', #114, #1674, #12945, .T. ) ;
#10275=ORIENTED_EDGE ( 'NONE', *, *, #2622, .T. ) ;
#10278=CARTESIAN_POINT ( 'NONE',  ( -33.77251566124358817, 9.999999999999998224, -156.1614337057717989 ) ) ;
#10282=CARTESIAN_POINT ( 'NONE',  ( 1.893911505664648054, 9.999999999999998224, -1.663006917529762152 ) ) ;
#10283=ADVANCED_FACE ( 'NONE', ( #14874 ), #791, .T. ) ;
#10293=CARTESIAN_POINT ( 'NONE',  ( -8.918093633295288925, 10.00000000000000355, -123.2478653285129724 ) ) ;
#10296=CARTESIAN_POINT ( 'NONE',  ( 2.543998210650478597, 8.673617379884035472E-16, -136.5336064733026831 ) ) ;
#10302=CARTESIAN_POINT ( 'NONE',  ( -1.376260179405573547, 0.000000000000000000, -106.6458321843530541 ) ) ;
#10306=CARTESIAN_POINT ( 'NONE',  ( 8.881449363785039353, 5.000000000000000888, -2.080517014814270205 ) ) ;
#10307=CARTESIAN_POINT ( 'NONE',  ( -8.851953732384830076, 10.69856349026787612, -105.4975849175705918 ) ) ;
#10308=CARTESIAN_POINT ( 'NONE',  ( -3.520407287333055635, 7.379999999999995453, -45.56125597433126018 ) ) ;
#10315=ORIENTED_EDGE ( 'NONE', *, *, #12923, .F. ) ;
#10330=CARTESIAN_POINT ( 'NONE',  ( 28.21756277010331004, 6.321094445766561876, -25.21174485404201704 ) ) ;
#10335=CARTESIAN_POINT ( 'NONE',  ( -65.20864362898224442, 14.64660082145764619, -194.2756847103777318 ) ) ;
#10337=CARTESIAN_POINT ( 'NONE',  ( 0.7644969749116201641, 4.641615622421193521, -138.4027240657578375 ) ) ;
#10339=CARTESIAN_POINT ( 'NONE',  ( -3.376139687035127235, 4.336808689942017736E-16, -108.9613800447800003 ) ) ;
#10342=EDGE_CURVE ( 'NONE', #6678, #8603, #8108, .T. ) ;
#10345=B_SPLINE_CURVE_WITH_KNOTS ( 'NONE', 3,
 ( #7224, #2214, #202, #10633, #8237, #12810, #3677, #11645, #12890, #127, #11718, #7070, #53, #2372, #4914, #3375 ),
 .UNSPECIFIED., .F., .F.,
 ( 4, 2, 2, 2, 2, 2, 2, 4 ),
 ( 0.000000000000000000, 0.005034478876242980301, 0.01006895775248596060, 0.02013791550497199406, 0.02517239438121500819, 0.03020687325745802579, 0.03524135213370103992, 0.04027583100994405751 ),
 .UNSPECIFIED. ) ;
#10348=DIRECTION ( 'NONE',  ( 0.000000000000000000, 0.000000000000000000, -1.000000000000000000 ) ) ;
#10349=CARTESIAN_POINT ( 'NONE',  ( -64.40997231175244053, 15.00000000000000000, -182.5864378953727396 ) ) ;
#10352=CARTESIAN_POINT ( 'NONE',  ( -5.080258480092867401, 15.00000000000000000, -126.4829214896701899 ) ) ;
#10353=CARTESIAN_POINT ( 'NONE',  ( -10.50399746317070715, 15.00000000000000178, -142.5005062768583741 ) ) ;
#10359=TOROIDAL_SURFACE ( 'NONE', #5903, 2.250000000000003553, 1.000000000000000000 ) ;
#10361=CARTESIAN_POINT ( 'NONE',  ( 6.089666224640344794, 0.000000000000000000, -124.6062682140657074 ) ) ;
#10363=CARTESIAN_POINT ( 'NONE',  ( 0.2625675443133231868, 10.25843542206809822, 2.974107430077547409 ) ) ;
#10365=ADVANCED_FACE ( 'NONE', ( #9276 ), #5523, .T. ) ;
#10380=CARTESIAN_POINT ( 'NONE',  ( -1.376260179405575323, 15.00000000000000000, -106.6458321843530541 ) ) ;
#10385=CIRCLE ( 'NONE', #5205, 4.999999999999998224 ) ;
#10386=CARTESIAN_POINT ( 'NONE',  ( -48.64052431954574729, 14.99999999999769074, -142.5706416667350425 ) ) ;
#10389=CARTESIAN_POINT ( 'NONE',  ( -2.141054399116760543, 5.000000000000000000, -102.7251783244459631 ) ) ;
#10400=ORIENTED_EDGE ( 'NONE', *, *, #9491, .T. ) ;
#10401=ORIENTED_EDGE ( 'NONE', *, *, #9597, .F. ) ;
#10421=CARTESIAN_POINT ( 'NONE',  ( -64.43123794286421457, 13.62327337436093799, -200.0781115302953310 ) ) ;
#10424=CARTESIAN_POINT ( 'NONE',  ( -8.871427270046806868, 4.336808689942020694E-16, -127.2226661771092040 ) ) ;
#10431=CIRCLE ( 'NONE', #11174, 6.999999999999950262 ) ;
#10432=CARTESIAN_POINT ( 'NONE',  ( -61.24268700630520357, 15.00000000000266986, -190.3758570956361211 ) ) ;
#10441=CARTESIAN_POINT ( 'NONE',  ( 3.136841903360915396, 15.00000000000000000, -104.4936450199714955 ) ) ;
#10444=CARTESIAN_POINT ( 'NONE',  ( -1.990360824022270991, 6.321094445766561876, -22.54485386122858515 ) ) ;
#10449=DIRECTION ( 'NONE',  ( -0.000000000000000000, -1.000000000000000000, -0.000000000000000000 ) ) ;
#10450=CARTESIAN_POINT ( 'NONE',  ( -12.27209645382209402, 9.999999999999998224, -127.2227734861304782 ) ) ;
#10457=CIRCLE ( 'NONE', #12428, 3.250000000000005329 ) ;
#10461=EDGE_CURVE ( 'NONE', #6301, #11483, #12486, .T. ) ;
#10468=AXIS2_PLACEMENT_3D ( 'NONE', #12834, #11443, #2021 ) ;
#10471=DIRECTION ( 'NONE',  ( 0.000000000000000000, 0.000000000000000000, -1.000000000000000000 ) ) ;
#10472=DIRECTION ( 'NONE',  ( -0.000000000000000000, -1.000000000000000000, -0.000000000000000000 ) ) ;
#10473=EDGE_LOOP ( 'NONE', ( #6889, #4321, #7345, #2073 ) ) ;
#10482=EDGE_LOOP ( 'NONE', ( #11685, #14378, #14794, #403 ) ) ;
#10489=CIRCLE ( 'NONE', #7769, 0.5000000000000000000 ) ;
#10491=CARTESIAN_POINT ( 'NONE',  ( -17.32624372123753886, 2.500000000000000444, -122.3796757791585321 ) ) ;
#10495=EDGE_LOOP ( 'NONE', ( #11012, #3099, #3529, #9609 ) ) ;
#10500=CARTESIAN_POINT ( 'NONE',  ( -65.88169384473235368, 15.09374676575395924, -201.3968192357596934 ) ) ;
#10503=DIRECTION ( 'NONE',  ( -8.673617379884027583E-16, 0.000000000000000000, -1.000000000000000000 ) ) ;
#10509=CARTESIAN_POINT ( 'NONE',  ( -67.64066136719213773, 14.99999999999999822, -197.5793268429668217 ) ) ;
#10520=CARTESIAN_POINT ( 'NONE',  ( -3.797473941148798104, 10.19338465826168516, -43.01405755766484162 ) ) ;
#10521=EDGE_CURVE ( 'NONE', #10617, #3600, #8419, .T. ) ;
#10522=CARTESIAN_POINT ( 'NONE',  ( -6.563559844847487668, 10.00000000000000178, -119.2393675976817491 ) ) ;
#10527=CARTESIAN_POINT ( 'NONE',  ( -64.50864733187511035, 13.73033652205686472, -199.7707221509654403 ) ) ;
#10533=CARTESIAN_POINT ( 'NONE',  ( 9.939878312292631080, 15.00000000000000888, -115.2320631035898657 ) ) ;
#10541=DIRECTION ( 'NONE',  ( 0.000000000000000000, -1.000000000000000000, 0.000000000000000000 ) ) ;
#10566=CARTESIAN_POINT ( 'NONE',  ( -65.15039301591723131, 14.86702644047977451, -190.2334373523178783 ) ) ;
#10567=CARTESIAN_POINT ( 'NONE',  ( -1.362135537567234378, 1.125083754270053138, -137.9888685449287777 ) ) ;
#10569=FACE_BOUND ( 'NONE', #1151, .T. ) ;
#10571=CARTESIAN_POINT ( 'NONE',  ( 3.867493089945844620, 14.96835584425696730, -13.04672393183693480 ) ) ;
#10576=CARTESIAN_POINT ( 'NONE',  ( -6.683304552674631971, 4.336808689942017736E-16, -104.1296019027812463 ) ) ;
#10578=VERTEX_POINT ( 'NONE', #4789 ) ;
#10579=CARTESIAN_POINT ( 'NONE',  ( -1.535122803310335238, 15.00000000000000000, -120.1898458067378641 ) ) ;
#10580=CARTESIAN_POINT ( 'NONE',  ( 2.321679137609549137, 14.14938758934379237, 1.340907874341730199 ) ) ;
#10581=CARTESIAN_POINT ( 'NONE',  ( -11.91260474553833504, 15.00000000000000000, -150.3549708559484088 ) ) ;
#10584=DIRECTION ( 'NONE',  ( -0.000000000000000000, -1.000000000000000000, -0.000000000000000000 ) ) ;
#10586=LINE ( 'NONE', #12920, #13180 ) ;
#10589=CARTESIAN_POINT ( 'NONE',  ( 3.481334635432024260, 11.96985545825839914, 4.757046313331589005 ) ) ;
#10591=DIRECTION ( 'NONE',  ( 0.000000000000000000, 0.000000000000000000, -1.000000000000000000 ) ) ;
#10592=CARTESIAN_POINT ( 'NONE',  ( 0.7552767017676234040, 8.673617379884035472E-16, -110.7727649483481400 ) ) ;
#10593=VERTEX_POINT ( 'NONE', #10737 ) ;
#10596=CARTESIAN_POINT ( 'NONE',  ( -5.223664414429025626, 3.333353350040314295E-13, -111.8183263698978607 ) ) ;
#10600=AXIS2_PLACEMENT_3D ( 'NONE', #12716, #4668, #9608 ) ;
#10601=CARTESIAN_POINT ( 'NONE',  ( 8.595858757335200551, 15.00000000000202860, -113.5677547687581779 ) ) ;
#10602=ORIENTED_EDGE ( 'NONE', *, *, #468, .T. ) ;
#10608=AXIS2_PLACEMENT_3D ( 'NONE', #10389, #11397, #1037 ) ;
#10613=EDGE_LOOP ( 'NONE', ( #9646, #12312, #14907, #11063 ) ) ;
#10617=VERTEX_POINT ( 'NONE', #8409 ) ;
#10625=CIRCLE ( 'NONE', #9879, 8.000000000000007105 ) ;
#10629=DIRECTION ( 'NONE',  ( -0.9961255586397056438, 0.000000000000000000, 0.08794243244722428632 ) ) ;
#10633=CARTESIAN_POINT ( 'NONE',  ( -61.77944655731723600, 14.99999999999999822, -173.7574396188045114 ) ) ;
#10642=EDGE_CURVE ( 'NONE', #14924, #6350, #14175, .T. ) ;
#10644=EDGE_CURVE ( 'NONE', #7777, #745, #10963, .T. ) ;
#10645=CARTESIAN_POINT ( 'NONE',  ( -67.58911133235071134, 10.63074368436302741, -204.4236580053128023 ) ) ;
#10651=CARTESIAN_POINT ( 'NONE',  ( -29.69515346086419427, 10.00000000000000178, -156.7390981038714983 ) ) ;
#10652=CARTESIAN_POINT ( 'NONE',  ( -16.31428614604211091, 0.05127365841283874903, -131.2397266576497543 ) ) ;
#10654=VERTEX_POINT ( 'NONE', #7089 ) ;
#10657=CARTESIAN_POINT ( 'NONE',  ( -51.02532656527229449, 14.99999999999733724, -166.3766172519595727 ) ) ;
#10660=CARTESIAN_POINT ( 'NONE',  ( -0.3098342781321086759, 15.00000000000000000, -115.8337115950633063 ) ) ;
#10661=CARTESIAN_POINT ( 'NONE',  ( -2.141054399116760543, 0.000000000000000000, -102.7251783244459631 ) ) ;
#10662=CARTESIAN_POINT ( 'NONE',  ( -8.272624645314563097, 15.00000000000000000, -140.4230430975476054 ) ) ;
#10669=CARTESIAN_POINT ( 'NONE',  ( 0.5436898071449285386, 11.71486000072444433, 2.780856639695837185 ) ) ;
#10670=CARTESIAN_POINT ( 'NONE',  ( -4.103993793088339892, 10.80977419301392928, -47.22237253197440765 ) ) ;
#10674=DIRECTION ( 'NONE',  ( 0.000000000000000000, -1.000000000000000000, 0.000000000000000000 ) ) ;
#10678=CARTESIAN_POINT ( 'NONE',  ( -5.248276757888013400, 2.500000000000000444, -115.0315526420553738 ) ) ;
#10683=ORIENTED_EDGE ( 'NONE', *, *, #76, .F. ) ;
#10684=VECTOR ( 'NONE', #11179, 1000.000000000000000 ) ;
#10686=CARTESIAN_POINT ( 'NONE',  ( -51.71514206966925542, 14.99999999999999467, -145.7302012132438165 ) ) ;
#10694=VECTOR ( 'NONE', #13009, 1000.000000000000000 ) ;
#10696=AXIS2_PLACEMENT_3D ( 'NONE', #6864, #13918, #854 ) ;
#10700=DIRECTION ( 'NONE',  ( -0.000000000000000000, 1.000000000000000000, -0.000000000000000000 ) ) ;
#10703=VERTEX_POINT ( 'NONE', #10661 ) ;
#10717=CARTESIAN_POINT ( 'NONE',  ( -12.27209645382210823, 2.500000000000000444, -127.2227734861304782 ) ) ;
#10720=CARTESIAN_POINT ( 'NONE',  ( -67.59870530518044518, 11.08167271862595094, -204.2373993420885370 ) ) ;
#10721=CARTESIAN_POINT ( 'NONE',  ( 0.2625675448779695720, 5.000000000001672440, 2.974107436473219401 ) ) ;
#10723=VECTOR ( 'NONE', #1807, 1000.000000000000000 ) ;
#10727=DIRECTION ( 'NONE',  ( -0.08794243244722420305, 0.000000000000000000, -0.9961255586397055328 ) ) ;
#10733=CARTESIAN_POINT ( 'NONE',  ( -61.39244834783638538, 10.00000000000000000, -159.9779749835793723 ) ) ;
#10735=ORIENTED_EDGE ( 'NONE', *, *, #12814, .F. ) ;
#10736=CARTESIAN_POINT ( 'NONE',  ( -6.708306527933025620, 15.00000000000363798, -119.6038561067746855 ) ) ;
#10737=CARTESIAN_POINT ( 'NONE',  ( -33.91109452335874153, 5.000000000000000000, -156.1716796081737471 ) ) ;
#10742=CARTESIAN_POINT ( 'NONE',  ( -35.49029739244799941, 5.000000000000000000, -131.2404697308744801 ) ) ;
#10744=CARTESIAN_POINT ( 'NONE',  ( 4.021974294543523065, 14.95912548502000838, 0.5602530272244051757 ) ) ;
#10745=CARTESIAN_POINT ( 'NONE',  ( -3.911881252916560747, 11.22597817734345860, -46.04150454295093908 ) ) ;
#10746=CARTESIAN_POINT ( 'NONE',  ( -8.659520330960761569, 1.372957239594033263, -105.3656150850790141 ) ) ;
#10747=DIRECTION ( 'NONE',  ( 0.000000000000000000, -1.000000000000000000, 0.000000000000000000 ) ) ;
#10751=CARTESIAN_POINT ( 'NONE',  ( -65.17119078000779098, 14.57600458215128825, -195.0918058944346569 ) ) ;
#10755=CARTESIAN_POINT ( 'NONE',  ( -6.790118584952986147, -1.321950343203052097E-12, -107.8021323225563179 ) ) ;
#10762=CARTESIAN_POINT ( 'NONE',  ( -69.36122292260984068, 9.999999999999998224, -183.5207230678399810 ) ) ;
#10763=B_SPLINE_CURVE_WITH_KNOTS ( 'NONE', 3,
 ( #1703, #6417, #554, #1472, #5266, #9976 ),
 .UNSPECIFIED., .F., .F.,
 ( 4, 2, 4 ),
 ( 0.000000000000000000, 0.006940540637791397204, 0.01388108127558279441 ),
 .UNSPECIFIED. ) ;
#10770=ORIENTED_EDGE ( 'NONE', *, *, #906, .T. ) ;
#10774=ORIENTED_EDGE ( 'NONE', *, *, #14993, .T. ) ;
#10778=VERTEX_POINT ( 'NONE', #4312 ) ;
#10781=CARTESIAN_POINT ( 'NONE',  ( -7.091927898542184749, 0.03088880688819538659, -104.2116372605956656 ) ) ;
#10782=CARTESIAN_POINT ( 'NONE',  ( -37.06343578980261810, 10.00000000000000355, -156.4760336361639474 ) ) ;
#10783=CARTESIAN_POINT ( 'NONE',  ( -41.68741913287574619, 15.00000000000000178, -152.6276280980627291 ) ) ;
#10785=CARTESIAN_POINT ( 'NONE',  ( -19.94423925787078389, 15.00000000000000000, -150.2885610952392881 ) ) ;
#10789=CARTESIAN_POINT ( 'NONE',  ( 2.850044070969222076, 5.000000000000000888, -103.0233998225063345 ) ) ;
#10792=EDGE_CURVE ( 'NONE', #447, #1413, #7752, .T. ) ;
#10793=CARTESIAN_POINT ( 'NONE',  ( -67.58382171872797528, 10.11977001915115437, -204.5178482232321642 ) ) ;
#10799=CARTESIAN_POINT ( 'NONE',  ( -17.32624372124044854, 0.6199615622964459449, -130.2318118670719116 ) ) ;
#10803=CYLINDRICAL_SURFACE ( 'NONE', #8391, 1.000000000000000888 ) ;
#10806=CARTESIAN_POINT ( 'NONE',  ( -8.431010172718810480, 15.00000000000000000, -122.5582262044626844 ) ) ;
#10808=CARTESIAN_POINT ( 'NONE',  ( -7.136800800249558208, 9.999999999999998224, -146.1984219327868288 ) ) ;
#10812=CARTESIAN_POINT ( 'NONE',  ( -3.395812927963546723, 10.62992796920838678, -45.78929837901311117 ) ) ;
#10814=CARTESIAN_POINT ( 'NONE',  ( 0.6968013826459904525, 11.59070670907840928, 5.520114370516503222 ) ) ;
#10815=EDGE_CURVE ( 'NONE', #11706, #11348, #13740, .T. ) ;
#10816=CARTESIAN_POINT ( 'NONE',  ( -12.27209645382210823, 15.00000000000000000, -127.2227734861304782 ) ) ;
#10821=CARTESIAN_POINT ( 'NONE',  ( -65.22313063405162836, 14.79918553424455041, -191.8929365503416022 ) ) ;
#10826=CARTESIAN_POINT ( 'NONE',  ( -7.473411123415157675, 4.336808689942017736E-16, -120.9918979908683525 ) ) ;
#10830=LINE ( 'NONE', #7275, #10694 ) ;
#10835=CARTESIAN_POINT ( 'NONE',  ( -64.93158582249934341, 15.00000000000000000, -188.2511415724482049 ) ) ;
#10838=CARTESIAN_POINT ( 'NONE',  ( -1.528156170053301510, 7.379999999999995453, -45.73714083922575213 ) ) ;
#10840=CARTESIAN_POINT ( 'NONE',  ( 5.844703153020811115, 0.000000000000000000, -103.2023327213425432 ) ) ;
#10849=EDGE_LOOP ( 'NONE', ( #1834, #13024, #2415, #1434 ) ) ;
#10854=ORIENTED_EDGE ( 'NONE', *, *, #11504, .F. ) ;
#10860=CARTESIAN_POINT ( 'NONE',  ( -43.45809816649217083, 10.00000000000000000, -159.1057901742589422 ) ) ;
#10872=TOROIDAL_SURFACE ( 'NONE', #13363, 3.750000000000003553, 0.5000000000000000000 ) ;
#10873=CARTESIAN_POINT ( 'NONE',  ( -63.93680978957204530, 12.84083462876305859, -201.7870368253884692 ) ) ;
#10879=CARTESIAN_POINT ( 'NONE',  ( -4.924771681124648026, 0.000000000000000000, -137.0932397189673111 ) ) ;
#10886=FACE_OUTER_BOUND ( 'NONE', #5410, .T. ) ;
#10890=CARTESIAN_POINT ( 'NONE',  ( -0.7473297648211070232, 15.00000000000000000, -117.8744674975950488 ) ) ;
#10892=CARTESIAN_POINT ( 'NONE',  ( 1.034717776212374707, 12.74535153223338035, 2.425209233265293918 ) ) ;
#10897=CARTESIAN_POINT ( 'NONE',  ( 0.06918667591891866642, 2.515825626418123573, 0.7836787576023231949 ) ) ;
#10899=CARTESIAN_POINT ( 'NONE',  ( 1.242364750776129290, 13.05645226862330333, 2.267205653757014439 ) ) ;
#10901=CARTESIAN_POINT ( 'NONE',  ( -8.871974675278494260, 2.162842538941835979, -105.5068606680567882 ) ) ;
#10902=DIRECTION ( 'NONE',  ( 0.000000000000000000, 0.000000000000000000, -1.000000000000000000 ) ) ;
#10905=CARTESIAN_POINT ( 'NONE',  ( 3.136841903360914952, -5.204170427930421283E-15, -104.4936450199714812 ) ) ;
#10907=EDGE_CURVE ( 'NONE', #11355, #6678, #7126, .T. ) ;
#10910=CARTESIAN_POINT ( 'NONE',  ( -4.234261469891104745, 4.336808689942017736E-16, -107.1714994797973475 ) ) ;
#10920=CARTESIAN_POINT ( 'NONE',  ( -70.09987374443890928, 9.999999999999998224, -191.4540390840369355 ) ) ;
#10924=CARTESIAN_POINT ( 'NONE',  ( -2.722152201699274521, 7.379999999999995453, -47.89048091371786597 ) ) ;
#10927=DIRECTION ( 'NONE',  ( -0.000000000000000000, -1.000000000000000000, -0.000000000000000000 ) ) ;
#10931=ORIENTED_EDGE ( 'NONE', *, *, #12531, .F. ) ;
#10933=ORIENTED_EDGE ( 'NONE', *, *, #13517, .T. ) ;
#10937=EDGE_CURVE ( 'NONE', #1534, #5560, #4100, .T. ) ;
#10940=EDGE_CURVE ( 'NONE', #882, #12098, #3486, .T. ) ;
#10946=TOROIDAL_SURFACE ( 'NONE', #9948, 9.499999999999941380, 2.500000000000000000 ) ;
#10949=ORIENTED_EDGE ( 'NONE', *, *, #1446, .F. ) ;
#10954=DIRECTION ( 'NONE',  ( 0.000000000000000000, -1.000000000000000000, 0.000000000000000000 ) ) ;
#10958=CARTESIAN_POINT ( 'NONE',  ( -63.77135710064911223, 12.50589072853210482, -202.2543161940598679 ) ) ;
#10962=CARTESIAN_POINT ( 'NONE',  ( -66.93602132738925548, 14.64151217242501701, -194.2073690153594612 ) ) ;
#10963=CIRCLE ( 'NONE', #14684, 3.000000000000010214 ) ;
#10968=CARTESIAN_POINT ( 'NONE',  ( -70.05680446119299631, 10.00000000000000178, -194.6833061307580977 ) ) ;
#10978=CARTESIAN_POINT ( 'NONE',  ( -3.331923142838100205, 10.52305467079069778, -44.71953693998822388 ) ) ;
#10980=CARTESIAN_POINT ( 'NONE',  ( 0.7636165113260954262, 12.24296972256808402, 2.624416505665311927 ) ) ;
#10987=ORIENTED_EDGE ( 'NONE', *, *, #3565, .F. ) ;
#10989=VERTEX_POINT ( 'NONE', #2615 ) ;
#10997=ADVANCED_FACE ( 'NONE', ( #1215 ), #14978, .F. ) ;
#10998=EDGE_CURVE ( 'NONE', #114, #11706, #8398, .T. ) ;
#11000=CARTESIAN_POINT ( 'NONE',  ( -65.10629832468505640, 15.00000000000000000, -192.2002039375829554 ) ) ;
#11001=LINE ( 'NONE', #14497, #5199 ) ;
#11005=LINE ( 'NONE', #13173, #10054 ) ;
#11012=ORIENTED_EDGE ( 'NONE', *, *, #7385, .T. ) ;
#11013=ORIENTED_EDGE ( 'NONE', *, *, #2622, .F. ) ;
#11014=CARTESIAN_POINT ( 'NONE',  ( 2.159942170319879562, 15.00000000000000000, -121.5147849362692369 ) ) ;
#11019=CARTESIAN_POINT ( 'NONE',  ( -60.91137729732986372, 5.000000000000000000, -175.0198515626273661 ) ) ;
#11021=CARTESIAN_POINT ( 'NONE',  ( 6.049910241306244885, 5.000000000000000000, -118.3734240199295300 ) ) ;
#11023=CARTESIAN_POINT ( 'NONE',  ( -40.08271351976077312, 9.999999999999998224, -157.3829028164099668 ) ) ;
#11027=CARTESIAN_POINT ( 'NONE',  ( 27.95136620086945456, 5.321094445766561876, -28.22695831649836151 ) ) ;
#11034=CARTESIAN_POINT ( 'NONE',  ( 7.669049304201897677, 4.117853033264375462, -21.07967015299796643 ) ) ;
#11038=EDGE_CURVE ( 'NONE', #6652, #11706, #13444, .T. ) ;
#11042=EDGE_LOOP ( 'NONE', ( #4189, #4529, #11943, #7119, #9162, #8948, #858, #8363 ) ) ;
#11044=CARTESIAN_POINT ( 'NONE',  ( -7.920839475687911246, 0.2897469122124984864, -104.3814272194790789 ) ) ;
#11047=CARTESIAN_POINT ( 'NONE',  ( -8.998617940277251037, 9.999999999999998224, -105.4241616556761727 ) ) ;
#11049=DIRECTION ( 'NONE',  ( 0.9961255586397056438, -0.000000000000000000, -0.08794243244722428632 ) ) ;
#11053=CARTESIAN_POINT ( 'NONE',  ( -3.334720899819473949, 10.18877393819426302, -43.92196855012799972 ) ) ;
#11057=CARTESIAN_POINT ( 'NONE',  ( 7.497075793982918235, 10.85333879869827456, -25.24968775269402244 ) ) ;
#11063=ORIENTED_EDGE ( 'NONE', *, *, #9427, .F. ) ;
#11064=DIRECTION ( 'NONE',  ( 0.000000000000000000, 0.000000000000000000, -1.000000000000000000 ) ) ;
#11072=CARTESIAN_POINT ( 'NONE',  ( -65.05375779891798516, 15.00000000000000000, -194.1897728445700011 ) ) ;
#11081=DIRECTION ( 'NONE',  ( 0.000000000000000000, 0.000000000000000000, -1.000000000000000000 ) ) ;
#11085=AXIS2_PLACEMENT_3D ( 'NONE', #4799, #7098, #3795 ) ;
#11091=CARTESIAN_POINT ( 'NONE',  ( 0.4711736884522539359, 9.999999999999998224, 5.336993082470237404 ) ) ;
#11092=CARTESIAN_POINT ( 'NONE',  ( -47.17052904438269678, 15.00000000000000178, -155.5945877827988113 ) ) ;
#11094=CARTESIAN_POINT ( 'NONE',  ( -25.82983890416511841, 9.999999999999998224, -142.4527639562402328 ) ) ;
#11100=EDGE_CURVE ( 'NONE', #10578, #14034, #5226, .T. ) ;
#11103=CARTESIAN_POINT ( 'NONE',  ( 7.583870713991609946, 3.811257878336620664, -21.41114937039851540 ) ) ;
#11104=CARTESIAN_POINT ( 'NONE',  ( 0.4075758588480595246, 1.777155427843639446, 4.616619290435463263 ) ) ;
#11113=CARTESIAN_POINT ( 'NONE',  ( -67.93149434159937528, 9.999999999999998224, -203.8702428815593635 ) ) ;
#11115=EDGE_CURVE ( 'NONE', #9540, #4565, #9074, .T. ) ;
#11117=DIRECTION ( 'NONE',  ( -0.9961255586397055328, 0.000000000000000000, 0.08794243244722427244 ) ) ;
#11118=EDGE_CURVE ( 'NONE', #8933, #13770, #10229, .T. ) ;
#11121=CARTESIAN_POINT ( 'NONE',  ( -11.47368464578246794, -7.930776467238262242E-13, -126.3895689753432094 ) ) ;
#11123=CIRCLE ( 'NONE', #7151, 2.000000000000011546 ) ;
#11126=CIRCLE ( 'NONE', #9152, 10.00000000000000888 ) ;
#11129=CARTESIAN_POINT ( 'NONE',  ( 0.1865371907817764130, 3.106934502706220957, 2.112910209604430545 ) ) ;
#11131=CARTESIAN_POINT ( 'NONE',  ( -25.66911763371813038, 15.00000000000000000, -138.9799121221676046 ) ) ;
#11138=CARTESIAN_POINT ( 'NONE',  ( -47.43378631392564415, 15.00000000000000000, -155.7534628402561339 ) ) ;
#11150=CARTESIAN_POINT ( 'NONE',  ( -64.05876861121487309, 15.00000000000000000, -200.0474132877887996 ) ) ;
#11158=DIRECTION ( 'NONE',  ( 0.7779936141972743080, 0.000000000000000000, 0.6282721832679390994 ) ) ;
#11159=ORIENTED_EDGE ( 'NONE', *, *, #9620, .F. ) ;
#11167=CARTESIAN_POINT ( 'NONE',  ( -6.749805820977427651, 0.000000000000000000, -104.8828629986478518 ) ) ;
#11170=FACE_OUTER_BOUND ( 'NONE', #4407, .T. ) ;
#11173=FACE_OUTER_BOUND ( 'NONE', #14404, .T. ) ;
#11174=AXIS2_PLACEMENT_3D ( 'NONE', #13567, #15037, #5295 ) ;
#11179=DIRECTION ( 'NONE',  ( -0.000000000000000000, -1.000000000000000000, -0.000000000000000000 ) ) ;
#11183=CARTESIAN_POINT ( 'NONE',  ( 0.5065669486108499431, 4.652565967668215841, 5.737893194806527042 ) ) ;
#11192=AXIS2_PLACEMENT_3D ( 'NONE', #4434, #9145, #13949 ) ;
#11208=CARTESIAN_POINT ( 'NONE',  ( 3.891364641103005617, 14.90536770052132098, -1.768596708628414449 ) ) ;
#11214=LINE ( 'NONE', #11438, #6927 ) ;
#11215=CARTESIAN_POINT ( 'NONE',  ( -43.45407652371731189, 15.00000000000000000, -153.4178398490312532 ) ) ;
#11219=FACE_OUTER_BOUND ( 'NONE', #6118, .T. ) ;
#11225=CARTESIAN_POINT ( 'NONE',  ( -9.422314331838387957, 0.000000000000000000, -135.7831129423652214 ) ) ;
#11227=DIRECTION ( 'NONE',  ( 0.9961255586397055328, -0.000000000000000000, -0.08794243244722428632 ) ) ;
#11228=CARTESIAN_POINT ( 'NONE',  ( -14.59253236707263213, -1.779437631024875872E-15, -133.7561938577802891 ) ) ;
#11231=CARTESIAN_POINT ( 'NONE',  ( -5.090128371569606180, 10.00000000000000178, -112.6869195057500690 ) ) ;
#11234=DIRECTION ( 'NONE',  ( -0.08794243244722425856, -0.000000000000000000, -0.9961255586397054218 ) ) ;
#11243=ORIENTED_EDGE ( 'NONE', *, *, #14054, .F. ) ;
#11246=DIRECTION ( 'NONE',  ( 0.000000000000000000, 0.000000000000000000, -1.000000000000000000 ) ) ;
#11252=ORIENTED_EDGE ( 'NONE', *, *, #368, .F. ) ;
#11260=CARTESIAN_POINT ( 'NONE',  ( 2.889412549072087444, 0.4949020854232912270, 2.410474734309482336 ) ) ;
#11265=ORIENTED_EDGE ( 'NONE', *, *, #11859, .T. ) ;
#11270=CARTESIAN_POINT ( 'NONE',  ( -8.998617940277251037, 15.00000000000000000, -105.4241616556761585 ) ) ;
#11278=CARTESIAN_POINT ( 'NONE',  ( -3.333302013784147810, 9.945430626687967290, -43.56301687292351232 ) ) ;
#11283=ORIENTED_EDGE ( 'NONE', *, *, #4574, .T. ) ;
#11286=CARTESIAN_POINT ( 'NONE',  ( -48.42971706865863979, 14.99999999999999467, -163.2864622074216356 ) ) ;
#11290=CYLINDRICAL_SURFACE ( 'NONE', #5772, 3.500000000000013323 ) ;
#11291=CARTESIAN_POINT ( 'NONE',  ( -8.243994158936983396, 9.999999999999998224, -104.7509493499769917 ) ) ;
#11298=CYLINDRICAL_SURFACE ( 'NONE', #10147, 3.000000000000010214 ) ;
#11299=DIRECTION ( 'NONE',  ( 0.000000000000000000, 0.000000000000000000, -1.000000000000000000 ) ) ;
#11304=CARTESIAN_POINT ( 'NONE',  ( 2.553779201801159804, 8.673617379884035472E-16, -128.9691103915868382 ) ) ;
#11308=CARTESIAN_POINT ( 'NONE',  ( 7.781170200712294260, 5.000000000000000888, -20.49502329017444424 ) ) ;
#11313=EDGE_LOOP ( 'NONE', ( #6457, #6622, #7366, #6193 ) ) ;
#11314=EDGE_CURVE ( 'NONE', #3493, #4119, #11419, .T. ) ;
#11319=CYLINDRICAL_SURFACE ( 'NONE', #11641, 14.80000000000025651 ) ;
#11334=CARTESIAN_POINT ( 'NONE',  ( 2.595281665815428518, 9.245940400502809730E-16, 0.5467206721942569070 ) ) ;
#11340=CARTESIAN_POINT ( 'NONE',  ( -35.61761402690549261, 15.00000000000000178, -151.2353583422565748 ) ) ;
#11342=FACE_OUTER_BOUND ( 'NONE', #1276, .T. ) ;
#11343=CARTESIAN_POINT ( 'NONE',  ( -5.616965975805494615, 4.336808689942017736E-16, -122.7637103460384935 ) ) ;
#11348=VERTEX_POINT ( 'NONE', #9551 ) ;
#11354=DIRECTION ( 'NONE',  ( 0.000000000000000000, 0.000000000000000000, 1.000000000000000000 ) ) ;
#11355=VERTEX_POINT ( 'NONE', #9628 ) ;
#11358=CARTESIAN_POINT ( 'NONE',  ( -47.49849438536951141, 14.99999999999460520, -162.3383809241247491 ) ) ;
#11363=AXIS2_PLACEMENT_3D ( 'NONE', #12674, #3094, #4338 ) ;
#11372=DIRECTION ( 'NONE',  ( 0.9961255586397056438, 0.000000000000000000, -0.08794243244722427244 ) ) ;
#11374=CARTESIAN_POINT ( 'NONE',  ( -63.16055005427053004, 15.00000000000000000, -202.1988008120308677 ) ) ;
#11376=CARTESIAN_POINT ( 'NONE',  ( -6.985256918799295889, 14.01682499433758444, -104.5239518528136529 ) ) ;
#11382=CARTESIAN_POINT ( 'NONE',  ( -16.94138229547582242, 15.00000000000000000, -154.2864167784019003 ) ) ;
#11384=CARTESIAN_POINT ( 'NONE',  ( -4.254413237569938389, 9.999999999999998224, -48.18981741835666810 ) ) ;
#11385=CARTESIAN_POINT ( 'NONE',  ( -26.78870578381917866, 4.999999999999999112, -139.1599602021251769 ) ) ;
#11397=DIRECTION ( 'NONE',  ( 0.05964429961207439596, 0.000000000000000000, 0.9982196940171963462 ) ) ;
#11404=EDGE_CURVE ( 'NONE', #5270, #1429, #1062, .T. ) ;
#11416=CARTESIAN_POINT ( 'NONE',  ( 3.194064371195536545, 3.228176745887314958, 4.887617669977396773 ) ) ;
#11419=LINE ( 'NONE', #7937, #13931 ) ;
#11424=AXIS2_PLACEMENT_3D ( 'NONE', #1691, #5098, #9962 ) ;
#11434=VECTOR ( 'NONE', #14547, 1000.000000000000227 ) ;
#11438=CARTESIAN_POINT ( 'NONE',  ( -24.86990227130816322, 4.999999999999999112, -145.8847246090277281 ) ) ;
#11439=CARTESIAN_POINT ( 'NONE',  ( -36.83003495301479546, 15.00000000000000000, -151.3633490263993053 ) ) ;
#11443=DIRECTION ( 'NONE',  ( 0.9961255586397056438, 0.000000000000000000, -0.08794243244722427244 ) ) ;
#11446=VECTOR ( 'NONE', #12605, 1000.000000000000000 ) ;
#11452=CARTESIAN_POINT ( 'NONE',  ( -1.528156170053301510, 7.379999999999995453, -45.73714083922575213 ) ) ;
#11453=CARTESIAN_POINT ( 'NONE',  ( -6.470761321916836728, 14.36593687500089089, -104.2727818228492680 ) ) ;
#11455=CARTESIAN_POINT ( 'NONE',  ( -5.966056897915851032, 10.00000000000000355, -117.7917496622050066 ) ) ;
#11456=DIRECTION ( 'NONE',  ( -0.000000000000000000, 1.000000000000000000, -0.000000000000000000 ) ) ;
#11458=VECTOR ( 'NONE', #1885, 1000.000000000000000 ) ;
#11459=CARTESIAN_POINT ( 'NONE',  ( 0.5805642473514114332, 5.000000000000000888, -138.6354391050098229 ) ) ;
#11461=EDGE_LOOP ( 'NONE', ( #11265, #2004, #999, #3592 ) ) ;
#11466=FACE_OUTER_BOUND ( 'NONE', #7431, .T. ) ;
#11473=CARTESIAN_POINT ( 'NONE',  ( -8.621472139734160933, 11.69044914895178700, -105.3716763026984040 ) ) ;
#11477=CARTESIAN_POINT ( 'NONE',  ( 5.844703153020811115, 15.00000000000000000, -103.2023327213425432 ) ) ;
#11478=EDGE_LOOP ( 'NONE', ( #7226, #12140, #11159 ) ) ;
#11479=CIRCLE ( 'NONE', #12718, 5.000000000000004441 ) ;
#11482=B_SPLINE_CURVE_WITH_KNOTS ( 'NONE', 3,
 ( #12011, #9548, #2675, #7066, #10781, #123, #13194, #7218, #280, #11785, #1282, #13271, #7375, #12092, #5984, #198, #1516, #4994 ),
 .UNSPECIFIED., .F., .F.,
 ( 4, 2, 2, 2, 2, 2, 2, 2, 4 ),
 ( -1.076588104275207311E-05, 0.0002386119086020659368, 0.0004879896982468839568, 0.0009867452775365226532, 0.001984256436115799938, 0.002483012015405438363, 0.002981767594695076788, 0.003480523173984714780, 0.003979278753274353639 ),
 .UNSPECIFIED. ) ;
#11483=VERTEX_POINT ( 'NONE', #10785 ) ;
#11490=CYLINDRICAL_SURFACE ( 'NONE', #14412, 3.250000000000005329 ) ;
#11498=FACE_OUTER_BOUND ( 'NONE', #13803, .T. ) ;
#11501=CYLINDRICAL_SURFACE ( 'NONE', #1552, 5.000000000000000888 ) ;
#11504=EDGE_CURVE ( 'NONE', #9540, #3493, #10345, .T. ) ;
#11506=EDGE_CURVE ( 'NONE', #973, #5826, #613, .T. ) ;
#11507=CARTESIAN_POINT ( 'NONE',  ( -64.96178392459071915, 14.30069434053429589, -197.3172887038956844 ) ) ;
#11516=CARTESIAN_POINT ( 'NONE',  ( -7.279638199344828031, 0.04866399238529270366, -104.3603488955697571 ) ) ;
#11519=CARTESIAN_POINT ( 'NONE',  ( -6.786583542010076187, 15.00000000000000000, -128.6396923774024401 ) ) ;
#11526=CARTESIAN_POINT ( 'NONE',  ( 3.230086961373100696, 9.999999999999998224, 5.208283729180108068 ) ) ;
#11534=CARTESIAN_POINT ( 'NONE',  ( -2.729969426660547871, 2.500000000000000000, -110.6850855677400602 ) ) ;
#11540=ORIENTED_EDGE ( 'NONE', *, *, #4662, .T. ) ;
#11543=CARTESIAN_POINT ( 'NONE',  ( -9.081120478662709772, 11.43401422448979687, -105.0943637814115164 ) ) ;
#11552=ORIENTED_EDGE ( 'NONE', *, *, #11115, .F. ) ;
#11554=DIRECTION ( 'NONE',  ( 0.08794243244723003172, 0.000000000000000000, 0.9961255586397049777 ) ) ;
#11557=EDGE_LOOP ( 'NONE', ( #8507, #13926, #15165, #15189 ) ) ;
#11558=CARTESIAN_POINT ( 'NONE',  ( 2.159942170319879562, 9.999999999999998224, -121.5147849362692369 ) ) ;
#11562=CARTESIAN_POINT ( 'NONE',  ( -14.40544493037610430, 9.999999999999998224, -152.3816313692990434 ) ) ;
#11566=CYLINDRICAL_SURFACE ( 'NONE', #2097, 3.187847681061608540 ) ;
#11574=CARTESIAN_POINT ( 'NONE',  ( -65.20134947527711233, 14.82863921652322148, -191.2408552922258878 ) ) ;
#11575=CARTESIAN_POINT ( 'NONE',  ( -3.566158703387691808, 0.1143801738294297626, -137.4717337110981248 ) ) ;
#11577=CARTESIAN_POINT ( 'NONE',  ( -6.708147162979256173, 4.336808689942017736E-16, -124.4601323014835401 ) ) ;
#11579=DIRECTION ( 'NONE',  ( -0.3900731735287306656, 0.000000000000000000, -0.9207838613340399991 ) ) ;
#11585=CARTESIAN_POINT ( 'NONE',  ( -60.74056104667560163, 14.99999999999732836, -188.2485173983686479 ) ) ;
#11586=ADVANCED_FACE ( 'NONE', ( #5233 ), #8248, .T. ) ;
#11588=VERTEX_POINT ( 'NONE', #14598 ) ;
#11589=CARTESIAN_POINT ( 'NONE',  ( 3.136841903360911843, 9.999999999999998224, -104.4936450199714812 ) ) ;
#11599=CARTESIAN_POINT ( 'NONE',  ( -5.162848795631284737, 10.00000000000000178, -114.2525014220538822 ) ) ;
#11603=AXIS2_PLACEMENT_3D ( 'NONE', #1897, #8848, #11246 ) ;
#11605=CARTESIAN_POINT ( 'NONE',  ( -25.82983890416511841, 15.00000000000000000, -142.4527639562402328 ) ) ;
#11617=AXIS2_PLACEMENT_3D ( 'NONE', #4264, #13696, #10348 ) ;
#11620=CARTESIAN_POINT ( 'NONE',  ( -8.429402173688821165, 12.15659329378483200, -105.2683602625900647 ) ) ;
#11625=ORIENTED_EDGE ( 'NONE', *, *, #12531, .T. ) ;
#11626=CARTESIAN_POINT ( 'NONE',  ( -0.9215583806111760090, 14.99999999999999822, -108.4313125253715242 ) ) ;
#11629=ORIENTED_EDGE ( 'NONE', *, *, #9798, .T. ) ;
#11641=AXIS2_PLACEMENT_3D ( 'NONE', #13434, #14595, #4150 ) ;
#11643=CARTESIAN_POINT ( 'NONE',  ( -63.21422130130007133, 9.999999999999998224, -203.6040552426024703 ) ) ;
#11645=CARTESIAN_POINT ( 'NONE',  ( -55.65458104879085255, 15.00000000000000178, -159.9470229874960694 ) ) ;
#11646=ORIENTED_EDGE ( 'NONE', *, *, #10253, .F. ) ;
#11653=CARTESIAN_POINT ( 'NONE',  ( -64.98738446724354390, 14.92583229185657245, -188.2237117130508182 ) ) ;
#11659=CARTESIAN_POINT ( 'NONE',  ( 2.850044070969222076, 15.00000000000000000, -103.0233998225063345 ) ) ;
#11660=ORIENTED_EDGE ( 'NONE', *, *, #4980, .T. ) ;
#11664=CARTESIAN_POINT ( 'NONE',  ( -61.22190880152086123, 15.00000000000000000, -173.9954932429986059 ) ) ;
#11667=ORIENTED_EDGE ( 'NONE', *, *, #14054, .T. ) ;
#11668=CARTESIAN_POINT ( 'NONE',  ( 4.921100845785776556, 9.999999999999996447, -108.2352075023247409 ) ) ;
#11676=AXIS2_PLACEMENT_3D ( 'NONE', #974, #5608, #12492 ) ;
#11677=LINE ( 'NONE', #5867, #14427 ) ;
#11678=EDGE_CURVE ( 'NONE', #11355, #15312, #14447, .T. ) ;
#11679=CARTESIAN_POINT ( 'NONE',  ( -5.219328155730350360, 10.00000000000000178, -114.7721859121468810 ) ) ;
#11682=CARTESIAN_POINT ( 'NONE',  ( 2.538427055334838922, 15.00000000000006395, -24.40947673343477220 ) ) ;
#11685=ORIENTED_EDGE ( 'NONE', *, *, #3452, .F. ) ;
#11686=CARTESIAN_POINT ( 'NONE',  ( -35.49029739244800652, 15.00000000000000000, -131.2404697308744517 ) ) ;
#11688=VECTOR ( 'NONE', #2933, 1000.000000000000000 ) ;
#11691=CARTESIAN_POINT ( 'NONE',  ( 3.136841903360910067, 9.999999999999998224, -104.4936450199714812 ) ) ;
#11694=CARTESIAN_POINT ( 'NONE',  ( -48.84058141567145839, 15.00000000000000000, -150.0510139422299574 ) ) ;
#11695=EDGE_CURVE ( 'NONE', #4145, #3581, #12457, .T. ) ;
#11696=CARTESIAN_POINT ( 'NONE',  ( -8.489924801947323019, 12.60136528530092015, -104.4290565640461068 ) ) ;
#11705=ORIENTED_EDGE ( 'NONE', *, *, #625, .T. ) ;
#11706=VERTEX_POINT ( 'NONE', #3920 ) ;
#11716=LINE ( 'NONE', #13762, #12862 ) ;
#11718=CARTESIAN_POINT ( 'NONE',  ( -52.04402637181858182, 15.00000000000000178, -154.2024637709381807 ) ) ;
#11724=CARTESIAN_POINT ( 'NONE',  ( -63.60348060676461301, 15.00000000000000000, -180.2685449772604045 ) ) ;
#11727=CARTESIAN_POINT ( 'NONE',  ( -3.851617064430881143, 4.336808689942017243E-16, -107.8880831658969157 ) ) ;
#11729=DIRECTION ( 'NONE',  ( -0.000000000000000000, -1.000000000000000000, -0.000000000000000000 ) ) ;
#11733=CARTESIAN_POINT ( 'NONE',  ( -63.02554947706173749, 15.00000000000000000, -201.1265914030478541 ) ) ;
#11737=CARTESIAN_POINT ( 'NONE',  ( -4.286587266701848975, 15.00000000000000000, -125.3643078127527133 ) ) ;
#11738=CARTESIAN_POINT ( 'NONE',  ( 4.190455366039512519, 15.00000000000000000, -127.0204409346084873 ) ) ;
#11749=CARTESIAN_POINT ( 'NONE',  ( 3.869066569140437117, 14.96825566294793752, -13.02889994254487505 ) ) ;
#11750=CARTESIAN_POINT ( 'NONE',  ( 3.235167919087375221, 8.673617379884035472E-16, -114.6791120453254962 ) ) ;
#11753=ADVANCED_FACE ( 'NONE', ( #7379, #12096, #11173 ), #13438, .F. ) ;
#11755=CARTESIAN_POINT ( 'NONE',  ( -6.038383049306157879, 2.646872844878069111E-13, -118.0543633388664659 ) ) ;
#11759=CARTESIAN_POINT ( 'NONE',  ( 7.353370788960563509, 9.999999999999998224, -111.8370434415688663 ) ) ;
#11760=ORIENTED_EDGE ( 'NONE', *, *, #4385, .T. ) ;
#11771=CARTESIAN_POINT ( 'NONE',  ( -2.570858214686514653, 15.00000000000000000, -122.5047453742639050 ) ) ;
#11774=EDGE_CURVE ( 'NONE', #6272, #6350, #14692, .T. ) ;
#11780=ORIENTED_EDGE ( 'NONE', *, *, #7971, .T. ) ;
#11785=CARTESIAN_POINT ( 'NONE',  ( -8.590860326212494513, 0.8276621886826124319, -104.5228840682026288 ) ) ;
#11795=CARTESIAN_POINT ( 'NONE',  ( -65.98103202930056455, 15.04542651531272490, -200.4630988027190881 ) ) ;
#11806=CARTESIAN_POINT ( 'NONE',  ( -65.59210620920288193, 15.00000000000000000, -187.0384419517383776 ) ) ;
#11809=CARTESIAN_POINT ( 'NONE',  ( -5.574230463462276575, 9.999999999999998224, -116.5593450232789223 ) ) ;
#11811=CARTESIAN_POINT ( 'NONE',  ( -7.136800800203102035, 15.00000000000000000, -146.1984219328402048 ) ) ;
#11817=CARTESIAN_POINT ( 'NONE',  ( -13.68460728451510633, 7.499999999999991118, -92.46488696946715891 ) ) ;
#11819=CARTESIAN_POINT ( 'NONE',  ( -6.972928664498794227, 1.021521734388686209E-15, -104.3013574265779795 ) ) ;
#11822=CARTESIAN_POINT ( 'NONE',  ( 1.855481649321456983, 15.00000000000000000, -35.83830032691798806 ) ) ;
#11826=CARTESIAN_POINT ( 'NONE',  ( -5.248276757777016854, 1.059334121087498154E-12, -115.0315526420590118 ) ) ;
#11830=VECTOR ( 'NONE', #5432, 1000.000000000000000 ) ;
#11859=EDGE_CURVE ( 'NONE', #2651, #13498, #1846, .T. ) ;
#11867=( GEOMETRIC_REPRESENTATION_CONTEXT ( 3 ) GLOBAL_UNCERTAINTY_ASSIGNED_CONTEXT ( ( #8330 ) ) GLOBAL_UNIT_ASSIGNED_CONTEXT ( ( #2275, #13879, #6760 ) ) REPRESENTATION_CONTEXT ( 'NONE', 'WORKASPACE' ) );
#11868=( BOUNDED_SURFACE ( )  B_SPLINE_SURFACE ( 3, 1, ( 
 ( #9064, #3184 ),
 ( #1809, #10074 ),
 ( #13563, #7974 ),
 ( #13640, #2964 ) ),
 .UNSPECIFIED., .F., .F., .T. ) 
 B_SPLINE_SURFACE_WITH_KNOTS ( ( 4, 4 ),
 ( 2, 2 ),
 ( 0.000000000000000000, 1.000000000000000000 ),
 ( 0.000000000000000000, 1.000000000000000000 ),
 .UNSPECIFIED. ) 
 GEOMETRIC_REPRESENTATION_ITEM ( )  RATIONAL_B_SPLINE_SURFACE ( (
 ( 1.000000000000000000, 1.000000000000000000),
 ( 0.9719843790119068183, 0.9719843790119068183),
 ( 0.9719843790119068183, 0.9719843790119068183),
 ( 1.000000000000000000, 1.000000000000000000) ) ) 
 REPRESENTATION_ITEM ( '' )  SURFACE ( )  );
#11871=CARTESIAN_POINT ( 'NONE',  ( -64.10403461688579796, 13.26028305253761808, -210.3464984387109951 ) ) ;
#11877=CARTESIAN_POINT ( 'NONE',  ( -31.09209721305613527, 5.000000000000000888, -156.3611406121567597 ) ) ;
#11878=DIRECTION ( 'NONE',  ( 0.05964429961207439596, -0.000000000000000000, 0.9982196940171963462 ) ) ;
#11883=CARTESIAN_POINT ( 'NONE',  ( -8.195698801737231420, 0.4580377701651440203, -104.4390439392078918 ) ) ;
#11886=CARTESIAN_POINT ( 'NONE',  ( -5.418245839020988441, 9.999999999999998224, -110.8346421744379313 ) ) ;
#11888=CARTESIAN_POINT ( 'NONE',  ( -0.3498759111130647081, 9.999999999999998224, -139.6126861213997472 ) ) ;
#11895=CARTESIAN_POINT ( 'NONE',  ( 3.330118040168945637, 11.25215624712264173, 5.031695831575111022 ) ) ;
#11896=CARTESIAN_POINT ( 'NONE',  ( -3.803913621930688382, 10.81208548464482355, -43.82788280992028263 ) ) ;
#11902=FACE_OUTER_BOUND ( 'NONE', #12265, .T. ) ;
#11903=CARTESIAN_POINT ( 'NONE',  ( -63.72793358483406934, 15.00000000000018119, -180.7898741481596403 ) ) ;
#11906=ORIENTED_EDGE ( 'NONE', *, *, #3077, .T. ) ;
#11907=CARTESIAN_POINT ( 'NONE',  ( -4.083223113469290233, 4.336808689942017736E-16, -107.4404827980595769 ) ) ;
#11915=CARTESIAN_POINT ( 'NONE',  ( -68.83694965406208155, 9.999999999999998224, -180.7144811897190948 ) ) ;
#11916=CARTESIAN_POINT ( 'NONE',  ( -3.756350458250083957, 9.999999999999998224, -48.23378863458027155 ) ) ;
#11923=AXIS2_PLACEMENT_3D ( 'NONE', #13684, #5253, #3081 ) ;
#11928=ORIENTED_EDGE ( 'NONE', *, *, #13593, .F. ) ;
#11933=ADVANCED_FACE ( 'NONE', ( #9232, #3355 ), #3509, .F. ) ;
#11938=CARTESIAN_POINT ( 'NONE',  ( -8.934675013019075962, 2.500000000000000444, -123.2708221453725201 ) ) ;
#11939=CARTESIAN_POINT ( 'NONE',  ( -53.54684834582479169, 10.00000000000000355, -170.1666570554936868 ) ) ;
#11940=CARTESIAN_POINT ( 'NONE',  ( -50.40552334055468009, 15.00000000000000000, -158.2257257439712532 ) ) ;
#11943=ORIENTED_EDGE ( 'NONE', *, *, #10342, .T. ) ;
#11944=AXIS2_PLACEMENT_3D ( 'NONE', #14107, #10541, #10471 ) ;
#11948=CARTESIAN_POINT ( 'NONE',  ( -67.58441209323089538, 10.23658426854694170, -204.5076973825927666 ) ) ;
#11955=CARTESIAN_POINT ( 'NONE',  ( -25.68053481550299111, 5.000000000000000888, -142.4798935003980773 ) ) ;
#11957=VERTEX_POINT ( 'NONE', #8136 ) ;
#11961=CARTESIAN_POINT ( 'NONE',  ( -8.870626307758040952, 2.148733653892300310, -105.5059564705872361 ) ) ;
#11965=CARTESIAN_POINT ( 'NONE',  ( -0.1147110668984741289, 15.00000000000000000, -113.7369025357346572 ) ) ;
#11968=CARTESIAN_POINT ( 'NONE',  ( 3.421487705324556483, 14.74649280419825637, -0.009165486442489365060 ) ) ;
#11970=CARTESIAN_POINT ( 'NONE',  ( 4.190470984303368063, 15.00000000000000000, -127.0204210814509196 ) ) ;
#11974=DIRECTION ( 'NONE',  ( -0.05964429961207245307, 0.000000000000000000, -0.9982196940171964572 ) ) ;
#11976=CARTESIAN_POINT ( 'NONE',  ( 4.015443435590369425, 13.35568666415761285, 3.641580877850956632 ) ) ;
#11985=CARTESIAN_POINT ( 'NONE',  ( -5.346294835442622073, -6.653696274010802536E-13, -111.0961406517098027 ) ) ;
#11990=ORIENTED_EDGE ( 'NONE', *, *, #3565, .T. ) ;
#11993=CARTESIAN_POINT ( 'NONE',  ( -70.09987374419694106, 15.00000000000000000, -191.4540390840448367 ) ) ;
#12002=EDGE_LOOP ( 'NONE', ( #9670, #7791, #7945 ) ) ;
#12003=ORIENTED_EDGE ( 'NONE', *, *, #14045, .T. ) ;
#12008=ORIENTED_EDGE ( 'NONE', *, *, #9574, .F. ) ;
#12011=CARTESIAN_POINT ( 'NONE',  ( -6.683304552674626642, 0.000000000000000000, -104.1296019027811894 ) ) ;
#12016=B_SPLINE_CURVE_WITH_KNOTS ( 'NONE', 3,
 ( #5907, #11562, #5687, #2212, #15065, #7935, #9324, #2369, #15146, #2146 ),
 .UNSPECIFIED., .F., .F.,
 ( 4, 2, 2, 2, 4 ),
 ( 3.469446951953614189E-18, 0.009507825141772015265, 0.01901565028354402706, 0.02852347542531603886, 0.03803130056708804718 ),
 .UNSPECIFIED. ) ;
#12018=B_SPLINE_CURVE_WITH_KNOTS ( 'NONE', 3,
 ( #5505, #7750, #7826, #6666, #14961, #9062, #13784, #3182, #2032, #1241, #4501, #13939, #3488, #12694, #8118, #10589, #2336, #9209, #5949, #8271 ),
 .UNSPECIFIED., .F., .F.,
 ( 4, 2, 2, 2, 2, 2, 2, 2, 2, 4 ),
 ( 0.000000000000000000, 0.001232535436417454789, 0.002465070872834909579, 0.003697606309252364151, 0.004930141745669819157, 0.005546409463878545359, 0.006162677182087270694, 0.007395212618504723098, 0.008627748054922173768, 0.009860283491339624437 ),
 .UNSPECIFIED. ) ;
#12021=ORIENTED_EDGE ( 'NONE', *, *, #7235, .T. ) ;
#12025=CARTESIAN_POINT ( 'NONE',  ( -65.01995796243984671, 15.35663992353611995, -206.2218773783315271 ) ) ;
#12033=EDGE_LOOP ( 'NONE', ( #9384, #12021, #14424, #14348, #4430, #14219 ) ) ;
#12036=CARTESIAN_POINT ( 'NONE',  ( -64.97045305008005300, 9.999999999999998224, -167.8253422882257269 ) ) ;
#12039=CARTESIAN_POINT ( 'NONE',  ( -5.418245838931921021, 14.99999999999939071, -110.8346421744157055 ) ) ;
#12041=DIRECTION ( 'NONE',  ( -0.000000000000000000, -1.000000000000000000, -0.000000000000000000 ) ) ;
#12045=CARTESIAN_POINT ( 'NONE',  ( -3.979893100209070056, 11.11731708281460129, -46.51432482832429116 ) ) ;
#12047=CARTESIAN_POINT ( 'NONE',  ( 3.803251406275964808, 12.89415288025766593, 4.113245758263203378 ) ) ;
#12049=ADVANCED_FACE ( 'NONE', ( #10072 ), #14808, .F. ) ;
#12051=CARTESIAN_POINT ( 'NONE',  ( -8.589778368047582546, 1.226453351861508612, -105.3195804397573170 ) ) ;
#12055=( BOUNDED_SURFACE ( )  B_SPLINE_SURFACE ( 3, 2, ( 
 ( #238, #8199, #2340 ),
 ( #7103, #4953, #1246 ),
 ( #4805, #7036, #11750 ),
 ( #1172, #5873, #10592 ),
 ( #324, #14483, #12057 ),
 ( #8580, #10905, #5037 ) ),
 .UNSPECIFIED., .F., .F., .F. ) 
 B_SPLINE_SURFACE_WITH_KNOTS ( ( 4, 2, 4 ),
 ( 3, 3 ),
 ( 0.000000000000000000, 0.006940540637791398938, 0.01388108127558279788 ),
 ( 0.000000000000000000, 1.000000000000000000 ),
 .UNSPECIFIED. ) 
 GEOMETRIC_REPRESENTATION_ITEM ( )  RATIONAL_B_SPLINE_SURFACE ( (
 ( 1.000000000000000000, 0.7071067811865469066, 1.000000000000000000),
 ( 1.000000000000000000, 0.7071067811865469066, 1.000000000000000000),
 ( 1.000000000000000000, 0.7071067811865475727, 1.000000000000000000),
 ( 1.000000000000000000, 0.7071067811865475727, 1.000000000000000000),
 ( 1.000000000000000000, 0.7071067811865471286, 1.000000000000000000),
 ( 1.000000000000000000, 0.7071067811865471286, 1.000000000000000000) ) ) 
 REPRESENTATION_ITEM ( '' )  SURFACE ( )  );
#12057=CARTESIAN_POINT ( 'NONE',  ( -0.3733149413592447008, 8.673617379884035472E-16, -108.7489923163346361 ) ) ;
#12058=EDGE_LOOP ( 'NONE', ( #14448, #12008, #13965, #7957 ) ) ;
#12061=CARTESIAN_POINT ( 'NONE',  ( -5.336847315148803617, 9.283940533607051382E-13, -115.5414184961177000 ) ) ;
#12070=CARTESIAN_POINT ( 'NONE',  ( -65.03533772944689417, 15.00000000000000000, -189.5630629144658599 ) ) ;
#12091=VECTOR ( 'NONE', #3901, 1000.000000000000000 ) ;
#12092=CARTESIAN_POINT ( 'NONE',  ( -9.103428091817445278, 1.676764629372798465, -104.6332280698933346 ) ) ;
#12096=FACE_BOUND ( 'NONE', #4786, .T. ) ;
#12098=VERTEX_POINT ( 'NONE', #13861 ) ;
#12104=CIRCLE ( 'NONE', #14604, 3.250000000000003553 ) ;
#12108=CARTESIAN_POINT ( 'NONE',  ( -63.38919026794945211, 11.42435839034952494, -203.2128261894144998 ) ) ;
#12113=AXIS2_PLACEMENT_3D ( 'NONE', #12997, #5868, #2401 ) ;
#12115=CARTESIAN_POINT ( 'NONE',  ( -64.29981409993189345, 14.99999998638445931, -182.3649568880052243 ) ) ;
#12120=CARTESIAN_POINT ( 'NONE',  ( -69.99910782323208025, 9.999999999999996447, -188.8614012312206398 ) ) ;
#12124=EDGE_CURVE ( 'NONE', #9880, #13770, #6594, .T. ) ;
#12132=CARTESIAN_POINT ( 'NONE',  ( -3.986154284857507779, 10.61173620962768105, -45.11416216203139129 ) ) ;
#12134=CARTESIAN_POINT ( 'NONE',  ( 1.753027082723892072, 13.64326733232996602, 4.258754144511208040 ) ) ;
#12135=TOROIDAL_SURFACE ( 'NONE', #2271, 2.000000000000011990, 1.000000000000000000 ) ;
#12140=ORIENTED_EDGE ( 'NONE', *, *, #2241, .F. ) ;
#12154=CARTESIAN_POINT ( 'NONE',  ( -59.11471918145669946, 15.00000000000000000, -166.7985135386829825 ) ) ;
#12155=CARTESIAN_POINT ( 'NONE',  ( -67.58382170693636226, 10.00000000000000000, -204.5178482451963191 ) ) ;
#12164=DIRECTION ( 'NONE',  ( 0.7859448108640930686, 0.000000000000000000, -0.6182966555592913638 ) ) ;
#12165=DIRECTION ( 'NONE',  ( -0.6282721832679394325, -4.359514022472389650E-16, 0.7779936141972740860 ) ) ;
#12168=CARTESIAN_POINT ( 'NONE',  ( -2.524281728693007043, 7.379999999999995453, -45.64919840677852392 ) ) ;
#12177=CARTESIAN_POINT ( 'NONE',  ( -44.98973890129524733, 10.00000000000000000, -160.2063470242129313 ) ) ;
#12178=CARTESIAN_POINT ( 'NONE',  ( -44.53431849203957427, 15.00000000000000178, -153.9513641047110468 ) ) ;
#12181=CARTESIAN_POINT ( 'NONE',  ( 2.159942170319879562, 5.000000000000000888, -121.5147849362692369 ) ) ;
#12185=ORIENTED_EDGE ( 'NONE', *, *, #6101, .T. ) ;
#12190=CARTESIAN_POINT ( 'NONE',  ( -64.63350576884886323, 14.96734299377280841, -207.9870121967235264 ) ) ;
#12191=CARTESIAN_POINT ( 'NONE',  ( -13.94843458185677676, 7.499999999999991118, -95.45326364538628638 ) ) ;
#12194=CARTESIAN_POINT ( 'NONE',  ( -25.82983890416511841, 5.000000000000000000, -142.4527639562402328 ) ) ;
#12195=MANIFOLD_SOLID_BREP ( 'Cortar-Extruir4', #1662 ) ;
#12201=CARTESIAN_POINT ( 'NONE',  ( -8.886921395968292003, 2.324218168650201921, -105.5168766101546822 ) ) ;
#12206=CARTESIAN_POINT ( 'NONE',  ( 28.48375933933716198, 7.321094445766561876, -22.19653139158566901 ) ) ;
#12211=CARTESIAN_POINT ( 'NONE',  ( -3.332125411039841723, 10.29294005234724629, -44.11502048402191889 ) ) ;
#12213=CARTESIAN_POINT ( 'NONE',  ( 3.243186333997263748, 10.51133653125105027, 5.185517934909010584 ) ) ;
#12215=EDGE_CURVE ( 'NONE', #7043, #4897, #5287, .T. ) ;
#12222=ORIENTED_EDGE ( 'NONE', *, *, #14167, .F. ) ;
#12225=DIRECTION ( 'NONE',  ( -0.08794243244722427244, 0.000000000000000000, -0.9961255586397056438 ) ) ;
#12234=CARTESIAN_POINT ( 'NONE',  ( -55.59493099310168418, 15.00000000000000000, -159.7812792143957950 ) ) ;
#12238=CARTESIAN_POINT ( 'NONE',  ( -7.397953522037811425, 10.00000000000000000, -106.9836120658180221 ) ) ;
#12241=CARTESIAN_POINT ( 'NONE',  ( -97.87133648009834985, 5.000000000000000000, -184.9876713694881971 ) ) ;
#12244=CARTESIAN_POINT ( 'NONE',  ( 7.781170200712294260, 5.000000000000000888, -20.49502329017444424 ) ) ;
#12246=CARTESIAN_POINT ( 'NONE',  ( -1.376260179405574435, 10.00000000000000178, -106.6458321843530541 ) ) ;
#12247=CARTESIAN_POINT ( 'NONE',  ( -2.256557393256121369, 7.321094445766562764, -25.56006732368493317 ) ) ;
#12258=EDGE_CURVE ( 'NONE', #2743, #2896, #12386, .T. ) ;
#12265=EDGE_LOOP ( 'NONE', ( #8524, #13397, #4840, #9347 ) ) ;
#12269=CARTESIAN_POINT ( 'NONE',  ( 7.434948248173551377, 5.000000000000000888, -26.28946758364566705 ) ) ;
#12270=CARTESIAN_POINT ( 'NONE',  ( 0.2073968263107874854, 3.339926503753445797, 2.349187686996549562 ) ) ;
#12271=AXIS2_PLACEMENT_3D ( 'NONE', #12246, #6369, #14966 ) ;
#12274=CARTESIAN_POINT ( 'NONE',  ( -67.58763313223541047, 10.54847312031630580, -204.4506847024756837 ) ) ;
#12275=PLANE ( 'NONE',  #7672 ) ;
#12282=CARTESIAN_POINT ( 'NONE',  ( -12.27209645382209580, 4.336808689942017736E-16, -127.2227734861304782 ) ) ;
#12287=CARTESIAN_POINT ( 'NONE',  ( -3.711477763885599135, 9.806857087768287684, -47.72551489695253224 ) ) ;
#12289=CARTESIAN_POINT ( 'NONE',  ( 4.391429576616724617, 15.00018009634376170, -1.240770632640158411 ) ) ;
#12291=DIRECTION ( 'NONE',  ( 0.08794243244722413366, 0.000000000000000000, 0.9961255586397056438 ) ) ;
#12297=DIRECTION ( 'NONE',  ( 0.9972730031336837220, 0.000000000000000000, -0.07380079417407094111 ) ) ;
#12300=CARTESIAN_POINT ( 'NONE',  ( -3.482821260068073688, 10.52211603452352939, -46.42594311958101372 ) ) ;
#12303=CARTESIAN_POINT ( 'NONE',  ( -63.72167557989842379, 15.00000000000000000, -200.9893488412410250 ) ) ;
#12304=CARTESIAN_POINT ( 'NONE',  ( -8.090126491280004828, -1.779437631024875872E-15, -136.8653377734624996 ) ) ;
#12311=CARTESIAN_POINT ( 'NONE',  ( -25.66911763371813038, 5.000000000000000888, -138.9799121221676046 ) ) ;
#12312=ORIENTED_EDGE ( 'NONE', *, *, #12337, .T. ) ;
#12319=EDGE_CURVE ( 'NONE', #12098, #13498, #12018, .T. ) ;
#12321=ADVANCED_FACE ( 'NONE', ( #15185 ), #6884, .F. ) ;
#12323=CARTESIAN_POINT ( 'NONE',  ( -4.710171483686392158, 15.00000000000000178, -103.4584432832766794 ) ) ;
#12332=VERTEX_POINT ( 'NONE', #3408 ) ;
#12333=PRODUCT_DEFINITION_FORMATION_WITH_SPECIFIED_SOURCE ( 'ANY', '', #12881, .NOT_KNOWN. ) ;
#12337=EDGE_CURVE ( 'NONE', #6374, #10593, #89, .T. ) ;
#12338=LINE ( 'NONE', #2998, #1217 ) ;
#12339=CARTESIAN_POINT ( 'NONE',  ( 0.1512067241414354890, 2.824897904590649933, 1.712721360606747956 ) ) ;
#12344=DIRECTION ( 'NONE',  ( 0.7220210382022057560, 0.000000000000000000, -0.6918711009959940261 ) ) ;
#12345=B_SPLINE_CURVE_WITH_KNOTS ( 'NONE', 3,
 ( #5573, #8902, #5350, #13854 ),
 .UNSPECIFIED., .F., .F.,
 ( 4, 4 ),
 ( 0.06025750390222917030, 0.06449836217413487671 ),
 .UNSPECIFIED. ) ;
#12351=CARTESIAN_POINT ( 'NONE',  ( 2.530298019944476451, 2.500000000000000888, 0.2330448234422073106 ) ) ;
#12360=FACE_OUTER_BOUND ( 'NONE', #7977, .T. ) ;
#12366=VECTOR ( 'NONE', #1929, 1000.000000000000114 ) ;
#12380=SHAPE_REPRESENTATION ( 'PruningShears-Part2_Predeterminado', ( #9419 ), #11867 ) ;
#12381=CARTESIAN_POINT ( 'NONE',  ( -68.36774365628944850, 15.00000000000000000, -202.8408623584168140 ) ) ;
#12386=LINE ( 'NONE', #13714, #10723 ) ;
#12391=ORIENTED_EDGE ( 'NONE', *, *, #8870, .T. ) ;
#12392=FACE_OUTER_BOUND ( 'NONE', #6798, .T. ) ;
#12397=ORIENTED_EDGE ( 'NONE', *, *, #9125, .F. ) ;
#12399=LINE ( 'NONE', #11167, #7153 ) ;
#12407=EDGE_LOOP ( 'NONE', ( #7547, #15036, #3595, #195 ) ) ;
#12415=TOROIDAL_SURFACE ( 'NONE', #3048, 2.250000000000003553, 1.000000000000000000 ) ;
#12416=DIRECTION ( 'NONE',  ( 0.000000000000000000, 0.000000000000000000, -1.000000000000000000 ) ) ;
#12417=CARTESIAN_POINT ( 'NONE',  ( 0.1555198618414440070, 0.03945862746746779670, 1.761576351096415749 ) ) ;
#12425=CIRCLE ( 'NONE', #5764, 3.500000000000003109 ) ;
#12426=EDGE_CURVE ( 'NONE', #411, #15277, #2715, .T. ) ;
#12428=AXIS2_PLACEMENT_3D ( 'NONE', #12168, #3908, #1586 ) ;
#12431=CARTESIAN_POINT ( 'NONE',  ( -4.050120478506952004, 15.00000000000000000, -103.2318605270664591 ) ) ;
#12438=CARTESIAN_POINT ( 'NONE',  ( -3.803032749128815837, 10.37790251371667694, -43.21158422952260736 ) ) ;
#12441=CARTESIAN_POINT ( 'NONE',  ( 3.136841903360915396, 9.999999999999998224, -104.4936450199714955 ) ) ;
#12446=EDGE_CURVE ( 'NONE', #8293, #9274, #9128, .T. ) ;
#12450=CARTESIAN_POINT ( 'NONE',  ( -32.01906953552002477, 9.999999999999998224, -156.2419951537547718 ) ) ;
#12457=CIRCLE ( 'NONE', #3556, 2.000000000000011546 ) ;
#12458=DIRECTION ( 'NONE',  ( 0.000000000000000000, 0.000000000000000000, 1.000000000000000000 ) ) ;
#12462=CARTESIAN_POINT ( 'NONE',  ( -68.68211634215907679, 9.999999999999998224, -201.9941738952850017 ) ) ;
#12463=DIRECTION ( 'NONE',  ( -0.000000000000000000, 1.000000000000000000, -0.000000000000000000 ) ) ;
#12468=DIRECTION ( 'NONE',  ( -0.9961255586397056438, 0.000000000000000000, 0.08794243244722428632 ) ) ;
#12476=ORIENTED_EDGE ( 'NONE', *, *, #10940, .T. ) ;
#12486=B_SPLINE_CURVE_WITH_KNOTS ( 'NONE', 3,
 ( #6804, #11738, #4345, #3169, #936, #7880, #10353, #15174, #15095, #4567 ),
 .UNSPECIFIED., .F., .F.,
 ( 4, 2, 2, 2, 4 ),
 ( 8.673617379884035472E-19, 0.009142429936519546468, 0.01828485987303909294, 0.02742728980955863941, 0.03656971974607818587 ),
 .UNSPECIFIED. ) ;
#12487=VERTEX_POINT ( 'NONE', #1471 ) ;
#12491=VERTEX_POINT ( 'NONE', #7340 ) ;
#12492=DIRECTION ( 'NONE',  ( 0.000000000000000000, 0.000000000000000000, -1.000000000000000000 ) ) ;
#12494=EDGE_CURVE ( 'NONE', #333, #6670, #6785, .T. ) ;
#12496=CARTESIAN_POINT ( 'NONE',  ( 7.379366129813715425, 4.011723206745021031, -25.58330403907983097 ) ) ;
#12497=CARTESIAN_POINT ( 'NONE',  ( 0.05436568487884790857, 2.499999997174701338, 0.6158011180084422831 ) ) ;
#12501=ORIENTED_EDGE ( 'NONE', *, *, #6964, .F. ) ;
#12502=CARTESIAN_POINT ( 'NONE',  ( 6.089666224640343017, 5.000000000000000000, -124.6062682140657074 ) ) ;
#12505=CARTESIAN_POINT ( 'NONE',  ( -7.302595107033178046, 4.336808689942017736E-16, -125.2751219642074290 ) ) ;
#12512=LINE ( 'NONE', #6793, #12366 ) ;
#12520=FACE_OUTER_BOUND ( 'NONE', #14866, .T. ) ;
#12521=CARTESIAN_POINT ( 'NONE',  ( -42.91596092834496545, 15.00000000000000000, -158.7990843558665688 ) ) ;
#12526=CARTESIAN_POINT ( 'NONE',  ( -3.357927367646159844, 10.63007073917650125, -45.36065389210889975 ) ) ;
#12531=EDGE_CURVE ( 'NONE', #3493, #6134, #121, .T. ) ;
#12534=CARTESIAN_POINT ( 'NONE',  ( -67.56077634536279675, 14.99999999999568701, -204.5805788361718953 ) ) ;
#12539=DIRECTION ( 'NONE',  ( -8.673617379884027583E-16, 0.000000000000000000, -1.000000000000000000 ) ) ;
#12542=CARTESIAN_POINT ( 'NONE',  ( 2.759717552616797409, 0.1596090954753005553, 1.516153802207580670 ) ) ;
#12543=CARTESIAN_POINT ( 'NONE',  ( 5.086353367585286556, 5.000000000000000888, -108.2668836821857639 ) ) ;
#12545=VERTEX_POINT ( 'NONE', #13963 ) ;
#12551=VERTEX_POINT ( 'NONE', #4374 ) ;
#12556=CARTESIAN_POINT ( 'NONE',  ( -8.886921396801787054, 9.999999999999998224, -105.5168766094550250 ) ) ;
#12561=CARTESIAN_POINT ( 'NONE',  ( -13.68460728451510455, 7.499999999999991118, -92.46488696946715891 ) ) ;
#12565=DIRECTION ( 'NONE',  ( -0.9961255586397050887, -0.000000000000000000, 0.08794243244723005948 ) ) ;
#12570=CARTESIAN_POINT ( 'NONE',  ( 7.434948248173551377, 5.000000000000000888, -26.28946758364566705 ) ) ;
#12579=ORIENTED_EDGE ( 'NONE', *, *, #997, .F. ) ;
#12587=ORIENTED_EDGE ( 'NONE', *, *, #12923, .T. ) ;
#12588=CARTESIAN_POINT ( 'NONE',  ( -3.897142427203911463, 10.21175642837406272, -43.91020597716068607 ) ) ;
#12591=CARTESIAN_POINT ( 'NONE',  ( -4.601444581690889102, 4.336808689942017736E-16, -120.9301509763419205 ) ) ;
#12593=CARTESIAN_POINT ( 'NONE',  ( 9.939878312292615092, 15.00000000000000000, -115.2320631035898373 ) ) ;
#12597=CARTESIAN_POINT ( 'NONE',  ( -50.19288965985742834, 14.99999999999999467, -165.3052356887086773 ) ) ;
#12605=DIRECTION ( 'NONE',  ( -0.05964429961207245307, 0.000000000000000000, -0.9982196940171964572 ) ) ;
#12606=AXIS2_PLACEMENT_3D ( 'NONE', #11955, #1216, #13130 ) ;
#12621=PLANE ( 'NONE',  #2963 ) ;
#12622=ORIENTED_EDGE ( 'NONE', *, *, #14043, .F. ) ;
#12629=CARTESIAN_POINT ( 'NONE',  ( -8.225432057702189326, -2.789143762251152850E-12, -106.0978137655278459 ) ) ;
#12634=CARTESIAN_POINT ( 'NONE',  ( -8.105667775294676858, 13.14512866495358345, -104.3119030511063556 ) ) ;
#12649=CARTESIAN_POINT ( 'NONE',  ( -1.242343264599803376, 7.379999999999995453, -42.49973277364670565 ) ) ;
#12664=CARTESIAN_POINT ( 'NONE',  ( -66.07114055912228423, 14.98244587632921387, -194.2582470785968383 ) ) ;
#12667=CARTESIAN_POINT ( 'NONE',  ( -5.753797509970949520, 4.336808689942017736E-16, -122.9860260041494229 ) ) ;
#12671=AXIS2_PLACEMENT_3D ( 'NONE', #13026, #10700, #5827 ) ;
#12674=CARTESIAN_POINT ( 'NONE',  ( -1.990360824022270991, 6.321094445766561876, -22.54485386122858515 ) ) ;
#12675=CARTESIAN_POINT ( 'NONE',  ( -40.58904132556775579, 15.00000000000000000, -152.2044608390405074 ) ) ;
#12686=EDGE_CURVE ( 'NONE', #8123, #13993, #5310, .T. ) ;
#12687=CARTESIAN_POINT ( 'NONE',  ( -4.348254188330000325, 7.379999999999995453, -49.25275560300654831 ) ) ;
#12691=CARTESIAN_POINT ( 'NONE',  ( 5.844703153020811115, 15.00000000000000000, -103.2023327213425432 ) ) ;
#12692=CARTESIAN_POINT ( 'NONE',  ( 4.586756373948224663, 15.00000000000000178, -116.5615908754608228 ) ) ;
#12694=CARTESIAN_POINT ( 'NONE',  ( 3.821260581353220331, 12.94577194562833533, 4.081242289023049530 ) ) ;
#12697=CARTESIAN_POINT ( 'NONE',  ( 8.219148137521692377, 5.000000000000000888, -129.9861206050398721 ) ) ;
#12704=CARTESIAN_POINT ( 'NONE',  ( -0.3733149413592447008, 15.00000000000000000, -108.7489923163346361 ) ) ;
#12705=ORIENTED_EDGE ( 'NONE', *, *, #8181, .F. ) ;
#12710=CARTESIAN_POINT ( 'NONE',  ( -8.738531072872435246, 12.15659329382392606, -104.5057571303798483 ) ) ;
#12716=CARTESIAN_POINT ( 'NONE',  ( 2.752881441477233349, 15.00000000000000000, 2.754251355355158637 ) ) ;
#12718=AXIS2_PLACEMENT_3D ( 'NONE', #13391, #1629, #11354 ) ;
#12727=ORIENTED_EDGE ( 'NONE', *, *, #2408, .T. ) ;
#12735=CARTESIAN_POINT ( 'NONE',  ( -25.82983890416511841, 15.00000000000000000, -152.2527639562405000 ) ) ;
#12736=EDGE_CURVE ( 'NONE', #6670, #6539, #3906, .T. ) ;
#12740=DIRECTION ( 'NONE',  ( -0.9961255586397049777, -0.000000000000000000, 0.08794243244723005948 ) ) ;
#12746=CARTESIAN_POINT ( 'NONE',  ( -64.07341370074516362, 14.99999999999997691, -182.2352504702354565 ) ) ;
#12747=ORIENTED_EDGE ( 'NONE', *, *, #56, .T. ) ;
#12753=LINE ( 'NONE', #11659, #8480 ) ;
#12757=CARTESIAN_POINT ( 'NONE',  ( -57.99932148896577644, 15.00000000000000000, -167.8682911189483775 ) ) ;
#12760=CARTESIAN_POINT ( 'NONE',  ( 10.01939027896081313, 5.000000000000000888, -127.6977514918621637 ) ) ;
#12762=CIRCLE ( 'NONE', #5841, 3.250000000000003553 ) ;
#12766=LINE ( 'NONE', #8496, #7923 ) ;
#12768=DIRECTION ( 'NONE',  ( 0.000000000000000000, 0.000000000000000000, -1.000000000000000000 ) ) ;
#12772=CARTESIAN_POINT ( 'NONE',  ( -11.55141596728015507, 9.999999999999996447, -126.4706876245357279 ) ) ;
#12775=CARTESIAN_POINT ( 'NONE',  ( 2.862287955980151732, 14.99999999999999822, -24.43344328180646485 ) ) ;
#12776=FACE_OUTER_BOUND ( 'NONE', #14911, .T. ) ;
#12777=ORIENTED_EDGE ( 'NONE', *, *, #557, .T. ) ;
#12786=CARTESIAN_POINT ( 'NONE',  ( -57.71664061951929625, 9.999999999999998224, -153.6990377947290369 ) ) ;
#12787=DIRECTION ( 'NONE',  ( 1.076984184057255515E-17, 1.000000000000000000, 1.219901976936984599E-16 ) ) ;
#12796=ORIENTED_EDGE ( 'NONE', *, *, #6013, .T. ) ;
#12810=CARTESIAN_POINT ( 'NONE',  ( -59.43466587753848529, 15.00000000000000000, -167.4626871265230648 ) ) ;
#12811=DIRECTION ( 'NONE',  ( 0.000000000000000000, -1.000000000000000000, 0.000000000000000000 ) ) ;
#12814=EDGE_CURVE ( 'NONE', #745, #1429, #5933, .T. ) ;
#12819=CARTESIAN_POINT ( 'NONE',  ( -65.23046657217157929, 14.71819778739303963, -193.2613010425793334 ) ) ;
#12823=CARTESIAN_POINT ( 'NONE',  ( -2.864308947300851838, 4.336808689942017243E-16, -115.9303594865754121 ) ) ;
#12825=LINE ( 'NONE', #5559, #4815 ) ;
#12829=CARTESIAN_POINT ( 'NONE',  ( -55.44729830678861049, 9.999999999999998224, -173.4678552873548654 ) ) ;
#12833=EDGE_CURVE ( 'NONE', #2807, #6301, #515, .T. ) ;
#12834=CARTESIAN_POINT ( 'NONE',  ( -3.520407287333055635, 7.379999999999995453, -45.56125597433126018 ) ) ;
#12839=CIRCLE ( 'NONE', #5667, 3.000000000000010214 ) ;
#12845=CARTESIAN_POINT ( 'NONE',  ( -5.808150136390151097, 15.00000000000030020, -117.3161822536942793 ) ) ;
#12848=VECTOR ( 'NONE', #15106, 1000.000000000000227 ) ;
#12849=FACE_OUTER_BOUND ( 'NONE', #11313, .T. ) ;
#12852=ORIENTED_EDGE ( 'NONE', *, *, #13032, .F. ) ;
#12856=CARTESIAN_POINT ( 'NONE',  ( -5.647163608656509126, 4.336808689942017736E-16, -105.1820076059687636 ) ) ;
#12862=VECTOR ( 'NONE', #3021, 1000.000000000000227 ) ;
#12863=CARTESIAN_POINT ( 'NONE',  ( -8.886921396742344825, 10.34875921370766072, -105.5168766095049193 ) ) ;
#12869=CARTESIAN_POINT ( 'NONE',  ( -1.760020797288979866, 14.99999999999999645, -120.7474935399611837 ) ) ;
#12878=ORIENTED_EDGE ( 'NONE', *, *, #2408, .F. ) ;
#12879=DIRECTION ( 'NONE',  ( 0.7995711366325320979, 5.548139285719649595E-16, 0.6005713924789963798 ) ) ;
#12881=PRODUCT ( 'PruningShears-Part2_Predeterminado', 'PruningShears-Part2_Predeterminado', '', ( #6067 ) ) ;
#12890=CARTESIAN_POINT ( 'NONE',  ( -54.80563802043110400, 15.00000000000000178, -158.4804275959015172 ) ) ;
#12897=CARTESIAN_POINT ( 'NONE',  ( -67.61879412477036055, 13.23091809662344964, -201.4429213360547521 ) ) ;
#12898=DIRECTION ( 'NONE',  ( 0.05964429961207246000, -0.000000000000000000, 0.9982196940171965682 ) ) ;
#12900=CARTESIAN_POINT ( 'NONE',  ( -9.651007058052471166, -2.046300565911432839E-31, -128.1008536839752878 ) ) ;
#12904=ORIENTED_EDGE ( 'NONE', *, *, #2433, .T. ) ;
#12907=CARTESIAN_POINT ( 'NONE',  ( -61.97126637942644578, 9.999999999999998224, -193.9440536785060374 ) ) ;
#12910=CARTESIAN_POINT ( 'NONE',  ( -2.208383803796207356, 15.00000000000000000, -121.8037055012923986 ) ) ;
#12919=CIRCLE ( 'NONE', #4767, 10.00000000000000888 ) ;
#12920=CARTESIAN_POINT ( 'NONE',  ( -25.82983890416511841, 15.00000000000000000, -157.2527639562405000 ) ) ;
#12921=FACE_OUTER_BOUND ( 'NONE', #7319, .T. ) ;
#12923=EDGE_CURVE ( 'NONE', #6272, #1043, #1580, .T. ) ;
#12928=CARTESIAN_POINT ( 'NONE',  ( -8.134741379327362409, 13.10967652946907336, -104.3206942789991274 ) ) ;
#12929=CARTESIAN_POINT ( 'NONE',  ( -64.12212600112349037, 13.16643233163841487, -201.2225177097709263 ) ) ;
#12930=ORIENTED_EDGE ( 'NONE', *, *, #8286, .F. ) ;
#12934=AXIS2_PLACEMENT_3D ( 'NONE', #4718, #12041, #8261 ) ;
#12942=DIRECTION ( 'NONE',  ( 0.08794243244723004560, 0.000000000000000000, 0.9961255586397049777 ) ) ;
#12943=DIRECTION ( 'NONE',  ( 1.000000000000000000, 0.000000000000000000, 0.000000000000000000 ) ) ;
#12945=CIRCLE ( 'NONE', #1594, 1.000000000000000888 ) ;
#12947=CARTESIAN_POINT ( 'NONE',  ( -49.91314714375069173, 15.00000000000000000, -125.9106517931341500 ) ) ;
#12967=ORIENTED_EDGE ( 'NONE', *, *, #13094, .T. ) ;
#12973=CARTESIAN_POINT ( 'NONE',  ( -64.70583122420893574, 13.98401442962929586, -198.8283618626409179 ) ) ;
#12978=CARTESIAN_POINT ( 'NONE',  ( -1.376260179405567108, 15.00000000000000000, -106.6458321843530683 ) ) ;
#12983=CARTESIAN_POINT ( 'NONE',  ( -6.984815280171007501, 2.369024761733573552E-09, -104.2451759018677251 ) ) ;
#12986=CARTESIAN_POINT ( 'NONE',  ( -2.113448244030541989, 15.00000000000000000, -105.7248292520770008 ) ) ;
#12987=DIRECTION ( 'NONE',  ( 0.08794243244722413366, 0.000000000000000000, 0.9961255586397056438 ) ) ;
#12989=CARTESIAN_POINT ( 'NONE',  ( 6.089666224640342129, 15.00000000000000000, -124.6062682140657216 ) ) ;
#12996=CARTESIAN_POINT ( 'NONE',  ( -10.84779165590732752, 4.999999999999999112, -149.7094178749453590 ) ) ;
#12997=CARTESIAN_POINT ( 'NONE',  ( -28.38930394846588001, 9.999999999999998224, -151.9126338648069066 ) ) ;
#13001=CARTESIAN_POINT ( 'NONE',  ( -7.917878791739701327, 13.35826822666819425, -104.2553089158425905 ) ) ;
#13002=CARTESIAN_POINT ( 'NONE',  ( -64.17593475674455306, 14.99370959519457536, -182.8799376562455450 ) ) ;
#13005=CARTESIAN_POINT ( 'NONE',  ( -2.612926366062044981, 4.336808689942017736E-16, -113.5913750124458801 ) ) ;
#13009=DIRECTION ( 'NONE',  ( -0.000000000000000000, -1.000000000000000000, -0.000000000000000000 ) ) ;
#13011=ADVANCED_FACE ( 'NONE', ( #5134 ), #10872, .T. ) ;
#13015=CARTESIAN_POINT ( 'NONE',  ( -45.22661540093461952, 15.00000000000000000, -146.2291324070019982 ) ) ;
#13024=ORIENTED_EDGE ( 'NONE', *, *, #3760, .T. ) ;
#13025=ORIENTED_EDGE ( 'NONE', *, *, #13593, .T. ) ;
#13026=CARTESIAN_POINT ( 'NONE',  ( -25.82983890416511841, 15.00000000000000000, -142.4527639562402328 ) ) ;
#13032=EDGE_CURVE ( 'NONE', #1429, #7022, #3471, .T. ) ;
#13033=CARTESIAN_POINT ( 'NONE',  ( -5.402767302556228834, 2.500000000000000000, -110.8935206225344388 ) ) ;
#13034=CARTESIAN_POINT ( 'NONE',  ( -38.89145998711707364, 9.999999999999998224, -156.9532850668581716 ) ) ;
#13042=CARTESIAN_POINT ( 'NONE',  ( -63.42958736446724544, 11.57753352781592504, -203.1186045345161801 ) ) ;
#13048=CARTESIAN_POINT ( 'NONE',  ( -7.942089414655052693, 7.499999999999991118, -89.96019367200776173 ) ) ;
#13052=CARTESIAN_POINT ( 'NONE',  ( -8.562056237857618157, 0.7968074793529829059, -104.5167437574517919 ) ) ;
#13054=ORIENTED_EDGE ( 'NONE', *, *, #4803, .F. ) ;
#13055=CARTESIAN_POINT ( 'NONE',  ( -0.2812006908208667388, 15.00000000000000000, -110.9708452933458176 ) ) ;
#13063=CARTESIAN_POINT ( 'NONE',  ( 4.739705316375511401, 14.53460293427037620, 1.305582433210761062 ) ) ;
#13064=CARTESIAN_POINT ( 'NONE',  ( -3.802759337645547522, 10.36768682443087286, -43.20025118941907749 ) ) ;
#13066=ADVANCED_FACE ( 'NONE', ( #4282 ), #15066, .T. ) ;
#13069=CARTESIAN_POINT ( 'NONE',  ( -4.090890948359609425, 15.00000000000000000, -103.1929727064838289 ) ) ;
#13074=CARTESIAN_POINT ( 'NONE',  ( -6.279162093004023504, 4.336808689942017736E-16, -108.6370948588635912 ) ) ;
#13083=CARTESIAN_POINT ( 'NONE',  ( -62.69788784789734137, 15.00000000000000000, -176.6065371158525181 ) ) ;
#13090=ADVANCED_FACE ( 'NONE', ( #5651 ), #11868, .F. ) ;
#13094=EDGE_CURVE ( 'NONE', #973, #9864, #4631, .T. ) ;
#13095=CARTESIAN_POINT ( 'NONE',  ( -0.6328346815827367022, 15.00000000000000000, -109.3684695446412007 ) ) ;
#13097=ORIENTED_EDGE ( 'NONE', *, *, #7385, .F. ) ;
#13104=CARTESIAN_POINT ( 'NONE',  ( -19.94423925787080520, 9.999999999999998224, -150.2885610952392597 ) ) ;
#13107=AXIS2_PLACEMENT_3D ( 'NONE', #14693, #4094, #12344 ) ;
#13109=CARTESIAN_POINT ( 'NONE',  ( -5.211827599098144859, 2.500000000000000888, -114.7762467949656582 ) ) ;
#13110=CARTESIAN_POINT ( 'NONE',  ( -38.28777827158674540, 9.999999999999994671, -156.7712049258111620 ) ) ;
#13120=AXIS2_PLACEMENT_3D ( 'NONE', #6321, #4010, #293 ) ;
#13124=CARTESIAN_POINT ( 'NONE',  ( -63.98308214666035809, 12.44470469654490330, -210.8813308483144908 ) ) ;
#13130=DIRECTION ( 'NONE',  ( 0.000000000000000000, 0.000000000000000000, -1.000000000000000000 ) ) ;
#13135=CARTESIAN_POINT ( 'NONE',  ( -9.262026962547025732, 2.111446349724324101, -105.1717885830827441 ) ) ;
#13139=ORIENTED_EDGE ( 'NONE', *, *, #12319, .F. ) ;
#13140=CARTESIAN_POINT ( 'NONE',  ( -7.230047174082840478, 9.999999999999998224, -120.6008656444815585 ) ) ;
#13141=CARTESIAN_POINT ( 'NONE',  ( 3.014182204252355390, 14.56766260765297361, 0.5812518486166803333 ) ) ;
#13147=CARTESIAN_POINT ( 'NONE',  ( -4.019421728525986559, 11.03613295220510615, -46.74835841341517551 ) ) ;
#13149=CARTESIAN_POINT ( 'NONE',  ( 1.439432938296930198, 13.23249829686945311, 4.644450407911167034 ) ) ;
#13150=CARTESIAN_POINT ( 'NONE',  ( -3.881302238640954361, 11.25545205242913127, -45.78502156705464898 ) ) ;
#13151=CIRCLE ( 'NONE', #6481, 2.500000000000000444 ) ;
#13155=( BOUNDED_SURFACE ( )  B_SPLINE_SURFACE ( 3, 1, ( 
 ( #4055, #1881 ),
 ( #4129, #11228 ),
 ( #7588, #12304 ),
 ( #5282, #8906 ) ),
 .UNSPECIFIED., .F., .F., .T. ) 
 B_SPLINE_SURFACE_WITH_KNOTS ( ( 4, 4 ),
 ( 2, 2 ),
 ( 0.000000000000000000, 1.000000000000000000 ),
 ( 0.000000000000000000, 1.000000000000000000 ),
 .UNSPECIFIED. ) 
 GEOMETRIC_REPRESENTATION_ITEM ( )  RATIONAL_B_SPLINE_SURFACE ( (
 ( 1.000000000000000000, 1.000000000000000000),
 ( 0.9748717492153319286, 0.9748717492153319286),
 ( 0.9748717492153319286, 0.9748717492153319286),
 ( 1.000000000000000000, 1.000000000000000000) ) ) 
 REPRESENTATION_ITEM ( '' )  SURFACE ( )  );
#13157=CYLINDRICAL_SURFACE ( 'NONE', #6160, 5.000000000000000888 ) ;
#13158=ORIENTED_EDGE ( 'NONE', *, *, #5630, .T. ) ;
#13160=VERTEX_POINT ( 'NONE', #11384 ) ;
#13161=CARTESIAN_POINT ( 'NONE',  ( -5.462587733787561461, 4.336808689942017736E-16, -110.6302725851879529 ) ) ;
#13166=ORIENTED_EDGE ( 'NONE', *, *, #4195, .F. ) ;
#13169=CARTESIAN_POINT ( 'NONE',  ( -70.10710660206702016, 15.00000000000000000, -192.1972859456651861 ) ) ;
#13173=CARTESIAN_POINT ( 'NONE',  ( -25.66911763371813038, -5.000000000000000888, -138.9799121221676046 ) ) ;
#13179=CARTESIAN_POINT ( 'NONE',  ( -8.205916711996726676, 7.499999999999991118, -92.94857034792688921 ) ) ;
#13180=VECTOR ( 'NONE', #2333, 1000.000000000000000 ) ;
#13182=ORIENTED_EDGE ( 'NONE', *, *, #9427, .T. ) ;
#13191=ADVANCED_FACE ( 'NONE', ( #655 ), #8224, .T. ) ;
#13193=CIRCLE ( 'NONE', #9732, 5.000000000000004441 ) ;
#13194=CARTESIAN_POINT ( 'NONE',  ( -7.490046183253692647, 0.1222994804349853415, -104.2926538792397508 ) ) ;
#13195=CARTESIAN_POINT ( 'NONE',  ( -52.88346389043234552, 9.999999999999996447, -169.0946036997559929 ) ) ;
#13196=CARTESIAN_POINT ( 'NONE',  ( -76.20282042307043469, 5.000000000000000888, -188.4633497277649496 ) ) ;
#13199=ORIENTED_EDGE ( 'NONE', *, *, #10642, .F. ) ;
#13205=ADVANCED_FACE ( 'NONE', ( #11902 ), #5872, .T. ) ;
#13206=ADVANCED_FACE ( 'NONE', ( #12849 ), #5454, .T. ) ;
#13207=CARTESIAN_POINT ( 'NONE',  ( -63.55690675229147502, 11.98211585306279581, -202.8120525166195875 ) ) ;
#13214=CARTESIAN_POINT ( 'NONE',  ( -16.72147566907574756, 0.2067131101362160162, -130.8524528097921404 ) ) ;
#13218=CARTESIAN_POINT ( 'NONE',  ( -8.943845545880508396, 1.244574210897673616, -105.0375473151879362 ) ) ;
#13221=CARTESIAN_POINT ( 'NONE',  ( -0.2151733755447025886, 15.00000000000000000, -115.1395769290326427 ) ) ;
#13226=ADVANCED_FACE ( 'NONE', ( #5804 ), #8343, .T. ) ;
#13230=CARTESIAN_POINT ( 'NONE',  ( 0.2177290144686464812, 3.455212393055724807, 2.466220573332666088 ) ) ;
#13232=CARTESIAN_POINT ( 'NONE',  ( 0.5471942990909076654, 10.82315019902009290, 5.691692885981924022 ) ) ;
#13234=CARTESIAN_POINT ( 'NONE',  ( -6.683304552674626642, 0.000000000000000000, -104.1296019027811894 ) ) ;
#13239=CARTESIAN_POINT ( 'NONE',  ( -63.21422130130007133, 9.999999999999998224, -203.6040552426024703 ) ) ;
#13243=CARTESIAN_POINT ( 'NONE',  ( -5.145745206718213893, 2.650598460978550256E-13, -112.5500021907200363 ) ) ;
#13248=ORIENTED_EDGE ( 'NONE', *, *, #14514, .T. ) ;
#13252=CARTESIAN_POINT ( 'NONE',  ( -69.57949925813656478, 15.00000000000227907, -184.9351518006187121 ) ) ;
#13253=PLANE ( 'NONE',  #13833 ) ;
#13270=VECTOR ( 'NONE', #8500, 1000.000000000000000 ) ;
#13271=CARTESIAN_POINT ( 'NONE',  ( -8.887479029472178382, 1.222969012369685915, -104.5864904545480556 ) ) ;
#13272=CARTESIAN_POINT ( 'NONE',  ( -60.26128208755820026, 10.00000000000000178, -186.2863115604802431 ) ) ;
#13277=AXIS2_PLACEMENT_3D ( 'NONE', #10840, #8909, #12539 ) ;
#13278=ORIENTED_EDGE ( 'NONE', *, *, #7883, .T. ) ;
#13279=EDGE_CURVE ( 'NONE', #6539, #114, #14786, .T. ) ;
#13284=CARTESIAN_POINT ( 'NONE',  ( -65.68091296275530055, 15.20918062550879313, -202.8221454773010635 ) ) ;
#13285=CARTESIAN_POINT ( 'NONE',  ( -13.50872241962065701, 7.499999999999991118, -90.47263585218773585 ) ) ;
#13289=CARTESIAN_POINT ( 'NONE',  ( -65.69798262610476058, 14.93413372664151595, -187.7077297338020969 ) ) ;
#13294=EDGE_CURVE ( 'NONE', #973, #12551, #8658, .T. ) ;
#13295=CARTESIAN_POINT ( 'NONE',  ( -67.73240446793354863, 10.00000000000000000, -176.0047139660857169 ) ) ;
#13298=CARTESIAN_POINT ( 'NONE',  ( -3.366457130219030702, 15.00000000000000000, -104.0285275769127651 ) ) ;
#13300=FACE_OUTER_BOUND ( 'NONE', #10495, .T. ) ;
#13305=CARTESIAN_POINT ( 'NONE',  ( -4.002681499858608660, 10.63006427533628440, -45.31489617893276289 ) ) ;
#13307=CARTESIAN_POINT ( 'NONE',  ( 1.208030854046586722, 12.86766912361566817, 4.923196339896195539 ) ) ;
#13317=CARTESIAN_POINT ( 'NONE',  ( -6.654685604018685474, 2.500000000000000444, -108.0058818678391077 ) ) ;
#13322=ORIENTED_EDGE ( 'NONE', *, *, #2215, .T. ) ;
#13328=CARTESIAN_POINT ( 'NONE',  ( -66.67437826168175263, 9.999999999999998224, -172.5466827975655235 ) ) ;
#13338=EDGE_LOOP ( 'NONE', ( #14263, #13025, #9066, #4672, #11629, #14770 ) ) ;
#13339=ORIENTED_EDGE ( 'NONE', *, *, #7139, .F. ) ;
#13344=ORIENTED_EDGE ( 'NONE', *, *, #13557, .F. ) ;
#13350=CARTESIAN_POINT ( 'NONE',  ( -57.00133116092639796, 10.00000000000000000, -176.8568458259982776 ) ) ;
#13352=DIRECTION ( 'NONE',  ( 0.9961255586397055328, 0.000000000000000000, -0.08794243244722427244 ) ) ;
#13363=AXIS2_PLACEMENT_3D ( 'NONE', #8685, #13420, #6366 ) ;
#13364=CARTESIAN_POINT ( 'NONE',  ( -63.26674631656910464, 10.78987469582507508, -203.4893414402424412 ) ) ;
#13365=CARTESIAN_POINT ( 'NONE',  ( -17.32624372123753886, 5.000000000000000000, -122.3796757791585321 ) ) ;
#13367=AXIS2_PLACEMENT_3D ( 'NONE', #11021, #5146, #9857 ) ;
#13369=DIRECTION ( 'NONE',  ( 0.000000000000000000, 0.000000000000000000, 1.000000000000000000 ) ) ;
#13374=CARTESIAN_POINT ( 'NONE',  ( -9.285933597860747568, 2.305077891771167398, -105.1819416472893494 ) ) ;
#13385=CARTESIAN_POINT ( 'NONE',  ( -3.345600617387282760, 10.60900084060682147, -45.14673711435018078 ) ) ;
#13387=CARTESIAN_POINT ( 'NONE',  ( 3.292862661403878732, 11.00682189581027615, 5.097845610625860502 ) ) ;
#13391=CARTESIAN_POINT ( 'NONE',  ( -17.32624372123753886, 9.999999999999998224, -134.3796757791585037 ) ) ;
#13397=ORIENTED_EDGE ( 'NONE', *, *, #8752, .F. ) ;
#13398=DIRECTION ( 'NONE',  ( 0.000000000000000000, -1.000000000000000000, 0.000000000000000000 ) ) ;
#13409=CARTESIAN_POINT ( 'NONE',  ( -69.61556017099954374, 14.99999999999885425, -198.3353672693050385 ) ) ;
#13410=ADVANCED_FACE ( 'NONE', ( #3096 ), #4484, .T. ) ;
#13411=ADVANCED_FACE ( 'NONE', ( #8326 ), #14478, .T. ) ;
#13418=EDGE_LOOP ( 'NONE', ( #15054, #15262, #7851, #1174 ) ) ;
#13420=DIRECTION ( 'NONE',  ( 0.9961255586397056438, 0.000000000000000000, -0.08794243244722427244 ) ) ;
#13421=CARTESIAN_POINT ( 'NONE',  ( 10.01939027896081313, 9.999999999999998224, -127.6977514918621637 ) ) ;
#13433=FACE_OUTER_BOUND ( 'NONE', #6442, .T. ) ;
#13434=CARTESIAN_POINT ( 'NONE',  ( -25.82983890416511841, 15.00000000000000000, -142.4527639562402328 ) ) ;
#13436=CIRCLE ( 'NONE', #3791, 2.500000000000000888 ) ;
#13438=PLANE ( 'NONE',  #6018 ) ;
#13444=CIRCLE ( 'NONE', #8239, 1.000000000000000888 ) ;
#13450=CARTESIAN_POINT ( 'NONE',  ( -67.63669501819022400, 12.89019592428436845, -202.2218604853389934 ) ) ;
#13452=DIRECTION ( 'NONE',  ( -0.000000000000000000, 1.000000000000000000, -0.000000000000000000 ) ) ;
#13453=ORIENTED_EDGE ( 'NONE', *, *, #10521, .T. ) ;
#13455=DIRECTION ( 'NONE',  ( -0.08794243244722436958, 0.000000000000000000, -0.9961255586397055328 ) ) ;
#13460=CARTESIAN_POINT ( 'NONE',  ( 3.890350893699055401, 5.000000000000000000, -1.782295516753907849 ) ) ;
#13466=CARTESIAN_POINT ( 'NONE',  ( -3.803734620756425322, 11.03678359822948885, -44.30700079492977039 ) ) ;
#13473=ADVANCED_FACE ( 'NONE', ( #10886 ), #10803, .T. ) ;
#13475=EDGE_CURVE ( 'NONE', #6134, #4565, #14218, .T. ) ;
#13483=ORIENTED_EDGE ( 'NONE', *, *, #906, .F. ) ;
#13492=DIRECTION ( 'NONE',  ( -0.000000000000000000, -1.000000000000000000, -0.000000000000000000 ) ) ;
#13497=B_SPLINE_CURVE_WITH_KNOTS ( 'NONE', 3,
 ( #2871, #4333, #9037, #5705, #3235, #11727, #4628, #10339, #15305, #994, #8026, #9265, #15082, #4476, #3316, #8172, #7013, #12823, #3539, #9186, #6719, #12591, #13989, #14062, #12667, #11577, #2008, #10424, #12900, #4557 ),
 .UNSPECIFIED., .F., .F.,
 ( 4, 2, 2, 2, 2, 2, 2, 2, 2, 2, 2, 2, 2, 2, 4 ),
 ( 2.602085213965210642E-18, 0.003534236666671877487, 0.004417795833339854122, 0.005301355000007830325, 0.007068473333343742830, 0.007952032500011699950, 0.008835591666679656203, 0.01060271000001552708, 0.01236982833335139795, 0.01413694666668726882, 0.01767118333335897587, 0.01943830166669482593, 0.02120542000003067598, 0.02473965666670241773, 0.02827389333337415600 ),
 .UNSPECIFIED. ) ;
#13498=VERTEX_POINT ( 'NONE', #6554 ) ;
#13499=EDGE_CURVE ( 'NONE', #14034, #14091, #1512, .T. ) ;
#13506=ORIENTED_EDGE ( 'NONE', *, *, #3452, .T. ) ;
#13509=CARTESIAN_POINT ( 'NONE',  ( -6.243492141569531917, 14.55944995895985450, -103.9608192963590625 ) ) ;
#13511=CARTESIAN_POINT ( 'NONE',  ( -57.52695389842154583, 14.99999999999999822, -167.0767265278727791 ) ) ;
#13514=ORIENTED_EDGE ( 'NONE', *, *, #8286, .T. ) ;
#13517=EDGE_CURVE ( 'NONE', #13758, #14016, #8905, .T. ) ;
#13523=CARTESIAN_POINT ( 'NONE',  ( 0.2508056121593058019, 4.191234989200504302, 2.840879807056750472 ) ) ;
#13524=CARTESIAN_POINT ( 'NONE',  ( 7.434948248173551377, 5.000000000000000888, -26.28946758364566705 ) ) ;
#13526=CARTESIAN_POINT ( 'NONE',  ( -67.09168088980882771, 14.54755436366324695, -195.2977458324043596 ) ) ;
#13527=CARTESIAN_POINT ( 'NONE',  ( 2.850044070969222521, 15.00000000000000000, -103.0233998225063345 ) ) ;
#13530=DIRECTION ( 'NONE',  ( 0.9961255586397056438, 0.000000000000000000, -0.08794243244722427244 ) ) ;
#13533=DIRECTION ( 'NONE',  ( -0.08794243244723005948, -0.000000000000000000, -0.9961255586397049777 ) ) ;
#13534=CARTESIAN_POINT ( 'NONE',  ( -8.818042780597295405, 4.336808689942017736E-16, -127.1624902446298364 ) ) ;
#13541=CARTESIAN_POINT ( 'NONE',  ( -25.82983890416511841, 9.999999999999998224, -157.2527639562405000 ) ) ;
#13545=DIRECTION ( 'NONE',  ( 0.003262051938530752433, 0.000000000000000000, 0.9999946794944213346 ) ) ;
#13546=CARTESIAN_POINT ( 'NONE',  ( -44.82692087594050179, 15.00000000000000000, -154.1244306586370101 ) ) ;
#13552=CARTESIAN_POINT ( 'NONE',  ( -3.395817407829019530, 10.62992890784805766, -45.78935231847124498 ) ) ;
#13555=DIRECTION ( 'NONE',  ( 0.000000000000000000, 0.000000000000000000, -1.000000000000000000 ) ) ;
#13556=CYLINDRICAL_SURFACE ( 'NONE', #1233, 3.187847681061608540 ) ;
#13557=EDGE_CURVE ( 'NONE', #4119, #14756, #10385, .T. ) ;
#13561=DIRECTION ( 'NONE',  ( 0.000000000000000000, 0.000000000000000000, 1.000000000000000000 ) ) ;
#13563=CARTESIAN_POINT ( 'NONE',  ( -7.234633885585873614, 9.999999999999998224, -146.9955140158000404 ) ) ;
#13564=CARTESIAN_POINT ( 'NONE',  ( -3.520407287333057855, 7.379999999999995453, -45.56125597433126018 ) ) ;
#13566=CARTESIAN_POINT ( 'NONE',  ( 7.788671722263534214, 5.321094445766561876, -20.36947622874119546 ) ) ;
#13567=CARTESIAN_POINT ( 'NONE',  ( -17.32624372123753886, 9.999999999999998224, -122.3796757791585321 ) ) ;
#13572=( BOUNDED_SURFACE ( )  B_SPLINE_SURFACE ( 3, 1, ( 
 ( #11589, #6873 ),
 ( #11668, #4638 ),
 ( #8035, #4342 ),
 ( #3166, #2171 ) ),
 .UNSPECIFIED., .F., .F., .F. ) 
 B_SPLINE_SURFACE_WITH_KNOTS ( ( 4, 4 ),
 ( 2, 2 ),
 ( 0.000000000000000000, 1.000000000000000000 ),
 ( 0.000000000000000000, 1.000000000000000000 ),
 .UNSPECIFIED. ) 
 GEOMETRIC_REPRESENTATION_ITEM ( )  RATIONAL_B_SPLINE_SURFACE ( (
 ( 1.000000000000000000, 1.000000000000000000),
 ( 0.9863449930132133225, 0.9863449930132133225),
 ( 0.9863449930132133225, 0.9863449930132133225),
 ( 1.000000000000000000, 1.000000000000000000) ) ) 
 REPRESENTATION_ITEM ( '' )  SURFACE ( )  );
#13584=DIRECTION ( 'NONE',  ( 0.000000000000000000, 0.000000000000000000, -1.000000000000000000 ) ) ;
#13586=ORIENTED_EDGE ( 'NONE', *, *, #11695, .T. ) ;
#13592=CARTESIAN_POINT ( 'NONE',  ( -67.58382170693636226, 9.999999999999998224, -204.5178482451962623 ) ) ;
#13593=EDGE_CURVE ( 'NONE', #2743, #7043, #14852, .T. ) ;
#13594=CARTESIAN_POINT ( 'NONE',  ( 0.09748540496241393793, 2.577905345474640342, 1.104218984803364778 ) ) ;
#13600=CARTESIAN_POINT ( 'NONE',  ( -67.59778896351508592, 11.06839609948164060, -204.2590688364760467 ) ) ;
#13608=AXIS2_PLACEMENT_3D ( 'NONE', #14013, #6886, #4581 ) ;
#13616=CARTESIAN_POINT ( 'NONE',  ( -3.842608339013799057, 9.819420005877756097, -43.36399912072333507 ) ) ;
#13625=CARTESIAN_POINT ( 'NONE',  ( -28.38930394846588001, 15.00000000000000000, -151.9126338648069066 ) ) ;
#13628=DIRECTION ( 'NONE',  ( 0.07380050482453413829, -0.002800241259227994727, 0.9972690931421338556 ) ) ;
#13632=CARTESIAN_POINT ( 'NONE',  ( 10.01939027896081313, 5.000000000000000888, -127.6977514918621637 ) ) ;
#13634=CARTESIAN_POINT ( 'NONE',  ( -68.36774365772026840, 9.999999999999998224, -202.8408623589480442 ) ) ;
#13635=FACE_OUTER_BOUND ( 'NONE', #4402, .T. ) ;
#13640=CARTESIAN_POINT ( 'NONE',  ( -16.94138229547579400, 9.999999999999998224, -154.2864167784019287 ) ) ;
#13641=CARTESIAN_POINT ( 'NONE',  ( 8.881449363785039353, 9.999999999999998224, -2.080517014814270205 ) ) ;
#13661=ORIENTED_EDGE ( 'NONE', *, *, #320, .T. ) ;
#13667=DIRECTION ( 'NONE',  ( 0.08794243244723003172, 0.000000000000000000, 0.9961255586397049777 ) ) ;
#13669=VECTOR ( 'NONE', #2062, 1000.000000000000114 ) ;
#13670=CARTESIAN_POINT ( 'NONE',  ( 7.229955861305157327, 3.179325318140356682, -23.98019230486299236 ) ) ;
#13671=CARTESIAN_POINT ( 'NONE',  ( 2.653424689224152644, 0.03126846220630731532, 0.8711017884127576494 ) ) ;
#13677=CIRCLE ( 'NONE', #15176, 0.5000000000000004441 ) ;
#13678=CARTESIAN_POINT ( 'NONE',  ( -28.38930394846591909, 15.00000000000000000, -151.9126338648069918 ) ) ;
#13682=EDGE_CURVE ( 'NONE', #10654, #9540, #14028, .T. ) ;
#13684=CARTESIAN_POINT ( 'NONE',  ( -25.97807323962435078, 5.000000000000000000, -142.5647913107548277 ) ) ;
#13693=CARTESIAN_POINT ( 'NONE',  ( 3.230086961373113130, 5.000000000000000888, 5.208283729180105404 ) ) ;
#13696=DIRECTION ( 'NONE',  ( 0.000000000000000000, -1.000000000000000000, 0.000000000000000000 ) ) ;
#13697=CARTESIAN_POINT ( 'NONE',  ( -34.35934156840468745, 9.999999999999998224, -156.1669470277516041 ) ) ;
#13704=CARTESIAN_POINT ( 'NONE',  ( -3.589007869510364657, 10.29140990637095854, -47.02124496736357173 ) ) ;
#13710=CARTESIAN_POINT ( 'NONE',  ( -63.95352844018274396, 15.00000000000000000, -200.3649080088305539 ) ) ;
#13714=CARTESIAN_POINT ( 'NONE',  ( -17.32624372123753886, 15.00000000000000000, -129.3796757791584753 ) ) ;
#13719=CARTESIAN_POINT ( 'NONE',  ( 7.784015231764366938, 5.104710470816894663, -20.44740824490198960 ) ) ;
#13727=CARTESIAN_POINT ( 'NONE',  ( -8.963920885435754826, 11.76682784975604434, -105.0444811867494224 ) ) ;
#13734=EDGE_LOOP ( 'NONE', ( #2488, #5881, #14965, #444 ) ) ;
#13738=ORIENTED_EDGE ( 'NONE', *, *, #12494, .F. ) ;
#13740=LINE ( 'NONE', #1542, #359 ) ;
#13743=DIRECTION ( 'NONE',  ( -0.000000000000000000, -1.000000000000000000, -0.000000000000000000 ) ) ;
#13744=ADVANCED_FACE ( 'NONE', ( #441 ), #7549, .F. ) ;
#13749=FACE_OUTER_BOUND ( 'NONE', #10238, .T. ) ;
#13754=CARTESIAN_POINT ( 'NONE',  ( -10.71664336931383588, 2.500000000000000444, -125.5340273011801884 ) ) ;
#13757=DIRECTION ( 'NONE',  ( 0.000000000000000000, 0.000000000000000000, -1.000000000000000000 ) ) ;
#13758=VERTEX_POINT ( 'NONE', #14596 ) ;
#13762=CARTESIAN_POINT ( 'NONE',  ( 27.95136620086945456, 7.321094445766561876, -28.22695831649836151 ) ) ;
#13768=CARTESIAN_POINT ( 'NONE',  ( -50.19288965972938854, 9.999999999999998224, -165.3052356888205168 ) ) ;
#13770=VERTEX_POINT ( 'NONE', #5231 ) ;
#13783=CARTESIAN_POINT ( 'NONE',  ( -8.484577415225384556, 9.999999999999996447, -105.8546082955197392 ) ) ;
#13784=CARTESIAN_POINT ( 'NONE',  ( 4.728979099990255897, 14.51970457313589513, 1.390952412700756868 ) ) ;
#13786=CARTESIAN_POINT ( 'NONE',  ( 4.349367571369147534, 0.000000000000000000, -126.8184404512878984 ) ) ;
#13789=EDGE_LOOP ( 'NONE', ( #9564, #13097, #13944, #13738 ) ) ;
#13796=DIRECTION ( 'NONE',  ( 0.9961255586397054218, -0.000000000000000000, -0.08794243244722428632 ) ) ;
#13797=CARTESIAN_POINT ( 'NONE',  ( -8.068063733882274491, 13.23099846074044095, -104.6727491793208600 ) ) ;
#13802=CARTESIAN_POINT ( 'NONE',  ( 3.220286340258128543, 14.96835584425696730, -12.99882895025039531 ) ) ;
#13803=EDGE_LOOP ( 'NONE', ( #3551, #5194, #3272, #10400 ) ) ;
#13808=CARTESIAN_POINT ( 'NONE',  ( -1.528156170053301510, 7.379999999999995453, -45.73714083922575213 ) ) ;
#13815=CARTESIAN_POINT ( 'NONE',  ( 0.2330829912941287385, 3.741858015452750319, 2.640135352774355404 ) ) ;
#13824=CARTESIAN_POINT ( 'NONE',  ( -17.32624372123753886, 2.500000000000000444, -122.3796757791585321 ) ) ;
#13828=CARTESIAN_POINT ( 'NONE',  ( -65.80676792586451995, 14.98942443719950113, -191.1849550162216929 ) ) ;
#13833=AXIS2_PLACEMENT_3D ( 'NONE', #10838, #3815, #12942 ) ;
#13840=CARTESIAN_POINT ( 'NONE',  ( -41.55509581777007355, 9.999999999999998224, -158.0567977603521115 ) ) ;
#13844=CARTESIAN_POINT ( 'NONE',  ( -7.699506734510488393, 15.00000000000000000, -129.6777018991784018 ) ) ;
#13845=AXIS2_PLACEMENT_3D ( 'NONE', #9825, #9752, #14715 ) ;
#13854=CARTESIAN_POINT ( 'NONE',  ( -29.69515346086420138, 9.999999999999998224, -156.7390981038714983 ) ) ;
#13856=FACE_OUTER_BOUND ( 'NONE', #2364, .T. ) ;
#13858=CARTESIAN_POINT ( 'NONE',  ( -4.090890948359609425, 15.00000000000000000, -103.1929727064838289 ) ) ;
#13860=CARTESIAN_POINT ( 'NONE',  ( -5.507086477070941122, 10.00000000000000178, -116.3025817345989168 ) ) ;
#13861=CARTESIAN_POINT ( 'NONE',  ( 4.856804767890306351, 14.90536770052033866, -1.840041787218210878 ) ) ;
#13870=CARTESIAN_POINT ( 'NONE',  ( -7.218906882868092012, 2.500000000000000444, -107.2047439207351829 ) ) ;
#13873=EDGE_CURVE ( 'NONE', #14924, #10654, #14360, .T. ) ;
#13878=DIRECTION ( 'NONE',  ( 0.000000000000000000, 0.000000000000000000, -1.000000000000000000 ) ) ;
#13879=( NAMED_UNIT ( * ) PLANE_ANGLE_UNIT ( ) SI_UNIT ( $, .RADIAN. ) );
#13889=ORIENTED_EDGE ( 'NONE', *, *, #2712, .F. ) ;
#13896=DIRECTION ( 'NONE',  ( 0.000000000000000000, -1.000000000000000000, 0.000000000000000000 ) ) ;
#13903=DIRECTION ( 'NONE',  ( -0.000000000000000000, -1.000000000000000000, -0.000000000000000000 ) ) ;
#13914=CARTESIAN_POINT ( 'NONE',  ( -64.36898479267240702, 13.53642980808444563, -200.3260915304600189 ) ) ;
#13918=DIRECTION ( 'NONE',  ( 0.000000000000000000, -1.000000000000000000, 0.000000000000000000 ) ) ;
#13920=CARTESIAN_POINT ( 'NONE',  ( -3.284464116416026425, 9.999999999999996447, -42.88872331408225591 ) ) ;
#13921=ORIENTED_EDGE ( 'NONE', *, *, #3173, .T. ) ;
#13924=CARTESIAN_POINT ( 'NONE',  ( -58.73854075876246128, 9.999999999999998224, -181.3184243508228519 ) ) ;
#13926=ORIENTED_EDGE ( 'NONE', *, *, #10937, .F. ) ;
#13931=VECTOR ( 'NONE', #840, 1000.000000000000114 ) ;
#13937=CARTESIAN_POINT ( 'NONE',  ( -7.250352174397651339, 10.00000000000000355, -120.6338660983546589 ) ) ;
#13938=ADVANCED_FACE ( 'NONE', ( #7915 ), #4236, .T. ) ;
#13939=CARTESIAN_POINT ( 'NONE',  ( 4.075001113472075609, 13.47049942401578448, 3.499674426787218184 ) ) ;
#13942=CARTESIAN_POINT ( 'NONE',  ( -9.240119717576689595, 9.999999999999998224, -104.6630069175297564 ) ) ;
#13943=CARTESIAN_POINT ( 'NONE',  ( 4.053227644665166274, 5.000000000000000000, -106.4152912718141266 ) ) ;
#13944=ORIENTED_EDGE ( 'NONE', *, *, #1841, .F. ) ;
#13949=DIRECTION ( 'NONE',  ( 0.000000000000000000, 0.000000000000000000, -1.000000000000000000 ) ) ;
#13953=CARTESIAN_POINT ( 'NONE',  ( -53.51085313097401297, 15.00000000000000000, -156.4046016528996859 ) ) ;
#13955=SHAPE_REPRESENTATION_RELATIONSHIP ( 'NONE' , 'NONE' ,  #12380, #10006 ) ;
#13960=CARTESIAN_POINT ( 'NONE',  ( 1.855481649321436777, 15.00000000000000000, -35.83830032691820122 ) ) ;
#13961=ORIENTED_EDGE ( 'NONE', *, *, #10461, .F. ) ;
#13963=CARTESIAN_POINT ( 'NONE',  ( -24.86990227130816322, 15.00000000000000000, -145.8847246090277281 ) ) ;
#13965=ORIENTED_EDGE ( 'NONE', *, *, #14661, .T. ) ;
#13968=CARTESIAN_POINT ( 'NONE',  ( -3.724891368794482904, 9.650666666666662508, -47.87745094654707145 ) ) ;
#13976=FACE_OUTER_BOUND ( 'NONE', #10482, .T. ) ;
#13981=EDGE_LOOP ( 'NONE', ( #735, #7920, #35, #8071 ) ) ;
#13986=FACE_OUTER_BOUND ( 'NONE', #3324, .T. ) ;
#13989=CARTESIAN_POINT ( 'NONE',  ( -4.873992731081242091, 4.336808689942016750E-16, -121.4575503408599957 ) ) ;
#13993=VERTEX_POINT ( 'NONE', #7663 ) ;
#13996=CARTESIAN_POINT ( 'NONE',  ( -61.70104298247990471, 9.999999999999998224, -192.5140885290205119 ) ) ;
#14007=CARTESIAN_POINT ( 'NONE',  ( -4.878500514246746356, 4.999999999999999112, -144.3544516087390264 ) ) ;
#14008=CARTESIAN_POINT ( 'NONE',  ( -8.445519633954337024, 12.12030021904079113, -105.2770060228727118 ) ) ;
#14013=CARTESIAN_POINT ( 'NONE',  ( 20.38723710659885313, 5.321094445766561876, -31.17704722822712426 ) ) ;
#14014=CARTESIAN_POINT ( 'NONE',  ( 7.359540121889097897, 5.000000000000000888, -111.8458898531363275 ) ) ;
#14016=VERTEX_POINT ( 'NONE', #12687 ) ;
#14020=CARTESIAN_POINT ( 'NONE',  ( 8.595858757291594543, 9.999999999999998224, -113.5677547687719624 ) ) ;
#14025=CARTESIAN_POINT ( 'NONE',  ( 5.844703153020811115, 5.000000000000000888, -103.2023327213425432 ) ) ;
#14028=B_SPLINE_CURVE_WITH_KNOTS ( 'NONE', 3,
 ( #13678, #3078, #1688, #6632, #11340, #4097, #5149, #6145, #14674, #10783, #6308, #12178, #200, #11092, #8539, #7220, #11940, #3998, #4910, #4996, #1518, #13511, #2678, #2760, #9625, #3918, #6066, #363 ),
 .UNSPECIFIED., .F., .F.,
 ( 4, 2, 2, 2, 2, 2, 2, 2, 2, 2, 2, 2, 2, 4 ),
 ( 2.081668171172168513E-17, 0.006221094506044410298, 0.007776368132555515691, 0.009331641759066621952, 0.01244218901208886917, 0.01555273626511111638, 0.01866328351813336187, 0.02177383077115560908, 0.02488437802417785977, 0.03110547253022235420, 0.03421601978324460835, 0.03732656703626685557, 0.04354766154231135000, 0.04976875604835584443 ),
 .UNSPECIFIED. ) ;
#14034=VERTEX_POINT ( 'NONE', #10361 ) ;
#14040=ORIENTED_EDGE ( 'NONE', *, *, #12124, .T. ) ;
#14043=EDGE_CURVE ( 'NONE', #6374, #6272, #12345, .T. ) ;
#14045=EDGE_CURVE ( 'NONE', #7043, #14756, #4967, .T. ) ;
#14054=EDGE_CURVE ( 'NONE', #13993, #10578, #6057, .T. ) ;
#14059=CARTESIAN_POINT ( 'NONE',  ( -64.16515357636237127, 13.23091809669857888, -201.0642910017739950 ) ) ;
#14062=CARTESIAN_POINT ( 'NONE',  ( -5.449692324012782585, 4.336808689942018722E-16, -122.4844380376194835 ) ) ;
#14066=DIRECTION ( 'NONE',  ( 0.6527336816407247611, 0.000000000000000000, -0.7575874476598360996 ) ) ;
#14068=CARTESIAN_POINT ( 'NONE',  ( -52.59034431208613114, 15.00000000000000000, -168.6389827469745910 ) ) ;
#14071=CARTESIAN_POINT ( 'NONE',  ( -6.178332509695485086, 9.999999999999998224, -118.3334666058101448 ) ) ;
#14080=CARTESIAN_POINT ( 'NONE',  ( -47.48189921986828210, 9.999999999999998224, -141.5723758807981483 ) ) ;
#14081=LINE ( 'NONE', #10816, #3994 ) ;
#14086=CIRCLE ( 'NONE', #11363, 3.187847681061608540 ) ;
#14088=CARTESIAN_POINT ( 'NONE',  ( -8.678274320079829351, 12.27452600300057028, -104.4870831087946783 ) ) ;
#14089=DIRECTION ( 'NONE',  ( -0.9982196940171965682, 0.000000000000000000, 0.05964429961207161346 ) ) ;
#14091=VERTEX_POINT ( 'NONE', #13632 ) ;
#14096=CARTESIAN_POINT ( 'NONE',  ( 0.7552767017676234040, 15.00000000000000000, -110.7727649483481400 ) ) ;
#14097=ORIENTED_EDGE ( 'NONE', *, *, #5137, .F. ) ;
#14101=CARTESIAN_POINT ( 'NONE',  ( -52.78575432782729848, 15.00000000000000000, -155.3001835197910907 ) ) ;
#14107=CARTESIAN_POINT ( 'NONE',  ( 1.893911505664648054, 9.999999999999998224, -1.663006917529762152 ) ) ;
#14109=ORIENTED_EDGE ( 'NONE', *, *, #2433, .F. ) ;
#14110=CARTESIAN_POINT ( 'NONE',  ( -6.917334924218488723, 14.99999999999999822, -128.7878144224694950 ) ) ;
#14118=ORIENTED_EDGE ( 'NONE', *, *, #1446, .T. ) ;
#14129=ORIENTED_EDGE ( 'NONE', *, *, #10253, .T. ) ;
#14136=CARTESIAN_POINT ( 'NONE',  ( -65.68254623362582834, 14.99155785633053384, -190.1707496129446611 ) ) ;
#14139=CARTESIAN_POINT ( 'NONE',  ( 6.049910241306248437, 0.000000000000000000, -118.3734240199295300 ) ) ;
#14147=AXIS2_PLACEMENT_3D ( 'NONE', #3940, #1541, #14543 ) ;
#14149=CARTESIAN_POINT ( 'NONE',  ( -58.73854075889047976, 14.99999999999204370, -181.3184243507722613 ) ) ;
#14151=ORIENTED_EDGE ( 'NONE', *, *, #10521, .F. ) ;
#14152=CARTESIAN_POINT ( 'NONE',  ( -5.997216956047667580, 15.00000000000000000, -109.1002327432083945 ) ) ;
#14154=CARTESIAN_POINT ( 'NONE',  ( 3.891364641103949307, 14.90536770052033688, -1.768596708628434211 ) ) ;
#14161=VECTOR ( 'NONE', #8695, 1000.000000000000000 ) ;
#14163=CARTESIAN_POINT ( 'NONE',  ( -3.803627870483841100, 11.02901697934978031, -44.28669749208544459 ) ) ;
#14164=LINE ( 'NONE', #4499, #13270 ) ;
#14167=EDGE_CURVE ( 'NONE', #9845, #6034, #8265, .T. ) ;
#14169=CARTESIAN_POINT ( 'NONE',  ( -64.47248607232361906, 14.98344778719946291, -184.4559935446063434 ) ) ;
#14172=CARTESIAN_POINT ( 'NONE',  ( -3.049680038147720484, 4.336808689942017736E-16, -109.9638061509243272 ) ) ;
#14175=CIRCLE ( 'NONE', #3543, 5.000000000000004441 ) ;
#14177=CARTESIAN_POINT ( 'NONE',  ( 6.049910241306251990, 15.00000000000000000, -118.3734240199295300 ) ) ;
#14181=FACE_OUTER_BOUND ( 'NONE', #8366, .T. ) ;
#14189=DIRECTION ( 'NONE',  ( 5.478074134663627674E-15, 0.000000000000000000, -1.000000000000000000 ) ) ;
#14200=CARTESIAN_POINT ( 'NONE',  ( -5.390763419087000408, 2.500000000000000444, -115.8096991919675673 ) ) ;
#14201=CARTESIAN_POINT ( 'NONE',  ( -51.48498151979637782, 10.00000000000000000, -167.0076196043950745 ) ) ;
#14206=DIRECTION ( 'NONE',  ( -0.9961255586397050887, 0.000000000000000000, 0.08794243244723005948 ) ) ;
#14208=DIRECTION ( 'NONE',  ( -0.7575874476598363216, 0.000000000000000000, -0.6527336816407245390 ) ) ;
#14210=CARTESIAN_POINT ( 'NONE',  ( -64.84685337185132425, 15.24184988518138084, -207.0200216268500810 ) ) ;
#14211=CARTESIAN_POINT ( 'NONE',  ( 3.890350893699057178, 9.999999999999998224, -1.782295516753907849 ) ) ;
#14215=CARTESIAN_POINT ( 'NONE',  ( -33.91109452335874153, 10.00000000000000178, -156.1716796081737471 ) ) ;
#14218=B_SPLINE_CURVE_WITH_KNOTS ( 'NONE', 3,
 ( #6008, #9808, #14294, #4856, #1617, #14465, #14539, #3861, #3694, #7324, #10733, #217, #12036, #9567, #13295, #6164, #8403, #2698, #7247, #2546, #4933, #12120, #1538, #6252, #10968, #1766, #7632, #766, #1920, #5394, #11113, #3006 ),
 .UNSPECIFIED., .F., .F.,
 ( 4, 2, 2, 2, 2, 2, 2, 2, 2, 2, 2, 2, 2, 2, 2, 4 ),
 ( 0.000000000000000000, 0.004332673798796619555, 0.008665347597593239110, 0.01299802139638985866, 0.01733069519518647822, 0.02599604279277973121, 0.03466139039037297725, 0.04332673798796622677, 0.04549307488736457211, 0.04765941178676291051, 0.05199208558555958731, 0.05632475938435627105, 0.06065743318315294785, 0.06499010698194963853, 0.06715644388134797693, 0.06932278078074631533 ),
 .UNSPECIFIED. ) ;
#14219=ORIENTED_EDGE ( 'NONE', *, *, #532, .T. ) ;
#14222=CARTESIAN_POINT ( 'NONE',  ( -61.97126637937648752, 15.00000000000265032, -193.9440536784921960 ) ) ;
#14225=CARTESIAN_POINT ( 'NONE',  ( -0.1096517733176519821, 15.00000000000000000, -113.0403960504791314 ) ) ;
#14228=CARTESIAN_POINT ( 'NONE',  ( -0.3498759111043971970, 15.00000000000000000, -139.6126861214085011 ) ) ;
#14234=CARTESIAN_POINT ( 'NONE',  ( 4.703427927161452970, 14.48245223617349531, 1.488206399065538532 ) ) ;
#14236=CARTESIAN_POINT ( 'NONE',  ( -3.822077182119589800, 11.22755171044550160, -45.02879370139852711 ) ) ;
#14237=CARTESIAN_POINT ( 'NONE',  ( -7.791963050599854945, 0.3085994142892563574, -104.8053269544278123 ) ) ;
#14239=CARTESIAN_POINT ( 'NONE',  ( 2.752881441477233349, 5.000000000000000888, 2.754251355355158193 ) ) ;
#14240=DIRECTION ( 'NONE',  ( 0.08794243244723005948, 0.000000000000000000, 0.9961255586397049777 ) ) ;
#14243=CARTESIAN_POINT ( 'NONE',  ( -3.665430453447521497, 4.336808689942017736E-16, -108.2557784285269946 ) ) ;
#14244=LINE ( 'NONE', #11686, #3768 ) ;
#14248=ORIENTED_EDGE ( 'NONE', *, *, #9712, .F. ) ;
#14253=CIRCLE ( 'NONE', #12271, 5.000000000000000888 ) ;
#14263=ORIENTED_EDGE ( 'NONE', *, *, #12258, .F. ) ;
#14264=CARTESIAN_POINT ( 'NONE',  ( -0.1986981485396748237, 15.00000000000000000, -111.2607621713454193 ) ) ;
#14271=VERTEX_POINT ( 'NONE', #10742 ) ;
#14274=CARTESIAN_POINT ( 'NONE',  ( -10.86141109878643718, 2.499999999999999556, -125.6973785677633373 ) ) ;
#14281=CARTESIAN_POINT ( 'NONE',  ( 6.049910241306248437, 15.00000000000000000, -118.3734240199295300 ) ) ;
#14282=CARTESIAN_POINT ( 'NONE',  ( -67.58669624565897038, 10.46432717369429888, -204.4673446941004045 ) ) ;
#14289=EDGE_CURVE ( 'NONE', #882, #602, #12766, .T. ) ;
#14290=EDGE_LOOP ( 'NONE', ( #6387, #5584, #7534, #11540, #7295, #8871, #9588, #5320, #4806, #1005, #14760, #9343, #11283, #9146, #2150 ) ) ;
#14293=EDGE_CURVE ( 'NONE', #11348, #12551, #1103, .T. ) ;
#14294=CARTESIAN_POINT ( 'NONE',  ( -49.63713232248656482, 9.999999999999998224, -143.5380774856291168 ) ) ;
#14299=CARTESIAN_POINT ( 'NONE',  ( -5.254015288425265773, 15.00000000000000178, -115.0648584343368555 ) ) ;
#14300=CARTESIAN_POINT ( 'NONE',  ( 0.2625675448779695720, 9.999999999999998224, 2.974107436473218957 ) ) ;
#14301=CARTESIAN_POINT ( 'NONE',  ( -4.827681327704948622, 9.999999999999998224, -144.0483944136971388 ) ) ;
#14307=CARTESIAN_POINT ( 'NONE',  ( 0.9668478293219275876, 12.62857015536147998, 2.475663031890364962 ) ) ;
#14316=ADVANCED_FACE ( 'NONE', ( #14630 ), #7045, .T. ) ;
#14319=CARTESIAN_POINT ( 'NONE',  ( -6.038383048961361688, 2.500000000000000444, -118.0543633390209806 ) ) ;
#14324=CARTESIAN_POINT ( 'NONE',  ( -17.99773676121543176, 1.745015017355616038, -129.4573227159242776 ) ) ;
#14328=CARTESIAN_POINT ( 'NONE',  ( -59.94788933422542954, 9.999999999999998224, -157.3141654284602851 ) ) ;
#14334=CIRCLE ( 'NONE', #8899, 9.800000000000252953 ) ;
#14339=CARTESIAN_POINT ( 'NONE',  ( -2.133154950264692040, 15.00000000000000711, -105.7915708274213955 ) ) ;
#14342=EDGE_CURVE ( 'NONE', #13160, #7022, #7723, .T. ) ;
#14348=ORIENTED_EDGE ( 'NONE', *, *, #2712, .T. ) ;
#14350=AXIS2_PLACEMENT_3D ( 'NONE', #12502, #535, #10192 ) ;
#14356=CARTESIAN_POINT ( 'NONE',  ( -5.344111538902212466, 2.500000000000000444, -111.1470454227235365 ) ) ;
#14360=CIRCLE ( 'NONE', #4724, 9.800000000000252953 ) ;
#14370=CARTESIAN_POINT ( 'NONE',  ( -63.51383849574869345, 11.85838142801650186, -202.9177410002877764 ) ) ;
#14378=ORIENTED_EDGE ( 'NONE', *, *, #4158, .T. ) ;
#14381=CARTESIAN_POINT ( 'NONE',  ( -9.147714614026110524, 1.812406719287864121, -104.6428665161372749 ) ) ;
#14384=CARTESIAN_POINT ( 'NONE',  ( -5.574230463510377653, 14.99999999999939604, -116.5593450232588424 ) ) ;
#14391=CARTESIAN_POINT ( 'NONE',  ( 0.1752993268022353945, 3.004311909859588070, 1.985618716487552726 ) ) ;
#14393=CARTESIAN_POINT ( 'NONE',  ( 4.414185141403890178, 14.05584352489653632, 2.594153855646779583 ) ) ;
#14402=VERTEX_POINT ( 'NONE', #776 ) ;
#14404=EDGE_LOOP ( 'NONE', ( #14668, #74, #9835, #240, #14694, #2038, #14895, #8312, #10933, #6994, #4227, #12852, #10735 ) ) ;
#14405=CARTESIAN_POINT ( 'NONE',  ( -6.701857729407779019, 2.500000000000000444, -119.5348842627718398 ) ) ;
#14409=CARTESIAN_POINT ( 'NONE',  ( -17.94289163462782710, 1.572396511098281158, -129.5251036616920430 ) ) ;
#14412=AXIS2_PLACEMENT_3D ( 'NONE', #3296, #8938, #13667 ) ;
#14416=CARTESIAN_POINT ( 'NONE',  ( -69.17701953972918716, 14.99999999999999645, -200.3386666625191879 ) ) ;
#14420=PLANE ( 'NONE',  #4623 ) ;
#14424=ORIENTED_EDGE ( 'NONE', *, *, #9025, .T. ) ;
#14427=VECTOR ( 'NONE', #6881, 1000.000000000000000 ) ;
#14430=ORIENTED_EDGE ( 'NONE', *, *, #8870, .F. ) ;
#14441=CARTESIAN_POINT ( 'NONE',  ( -5.125635908759425874, 2.499999999999999556, -112.7029199983815602 ) ) ;
#14442=EDGE_CURVE ( 'NONE', #11957, #4481, #12512, .T. ) ;
#14443=CARTESIAN_POINT ( 'NONE',  ( -57.93401690343701205, 10.00000000000000178, -179.1696213049108053 ) ) ;
#14447=LINE ( 'NONE', #11027, #1344 ) ;
#14448=ORIENTED_EDGE ( 'NONE', *, *, #4158, .F. ) ;
#14450=AXIS2_PLACEMENT_3D ( 'NONE', #9478, #15225, #4839 ) ;
#14454=CARTESIAN_POINT ( 'NONE',  ( -67.62515672639226239, 11.98211585291473469, -203.5224559347309992 ) ) ;
#14455=FACE_OUTER_BOUND ( 'NONE', #350, .T. ) ;
#14465=CARTESIAN_POINT ( 'NONE',  ( -54.39630486114151608, 9.999999999999996447, -148.9727485570832926 ) ) ;
#14468=CARTESIAN_POINT ( 'NONE',  ( -7.267596910904561724, 9.999999999999998224, -107.1579542029217720 ) ) ;
#14474=CARTESIAN_POINT ( 'NONE',  ( -3.910513648578280321, 11.22738257010117557, -46.03033150271466667 ) ) ;
#14476=CARTESIAN_POINT ( 'NONE',  ( 4.086606960750444273, 13.49296761167366476, 3.472055327930651636 ) ) ;
#14478=( BOUNDED_SURFACE ( )  B_SPLINE_SURFACE ( 3, 2, ( 
 ( #7020, #1154, #10576 ),
 ( #9423, #12983, #15315 ),
 ( #3549, #11516, #931 ),
 ( #11044, #9649, #14620 ),
 ( #11883, #460, #5018 ),
 ( #13052, #3937, #7397 ),
 ( #5095, #6086, #1457 ),
 ( #386, #304, #8638 ),
 ( #5170, #13218, #1306 ),
 ( #1385, #9882, #4018 ),
 ( #14381, #2464, #3780 ),
 ( #9736, #13135, #11961 ),
 ( #146, #13374, #12201 ),
 ( #2779, #6329, #7483 ) ),
 .UNSPECIFIED., .F., .F., .F. ) 
 B_SPLINE_SURFACE_WITH_KNOTS ( ( 4, 2, 2, 2, 2, 2, 4 ),
 ( 3, 3 ),
 ( -8.724106040071283679E-06, 0.0006126034624112808996, 0.001233931030862633156, 0.001544594815088309175, 0.001855258599313985412, 0.002165922383539661648, 0.002476586167765337451 ),
 ( 0.000000000000000000, 1.000000000000000000 ),
 .UNSPECIFIED. ) 
 GEOMETRIC_REPRESENTATION_ITEM ( )  RATIONAL_B_SPLINE_SURFACE ( (
 ( 1.000000000000000000, 1.000000000000000000, 1.000000000000000000),
 ( 1.000000000000000000, 0.9999955273081105878, 1.000000000000000000),
 ( 1.000000000000000000, 0.9954486024702557945, 1.000000000000000000),
 ( 1.000000000000000000, 0.9776029025031673925, 1.000000000000000000),
 ( 1.000000000000000000, 0.9647625072224111920, 1.000000000000000000),
 ( 1.000000000000000000, 0.9425905009577734139, 1.000000000000000000),
 ( 1.000000000000000000, 0.9349995798840151640, 1.000000000000000000),
 ( 1.000000000000000000, 0.9203396985081793158, 1.000000000000000000),
 ( 1.000000000000000000, 0.9132096254797749113, 1.000000000000000000),
 ( 1.000000000000000000, 0.9008818398987329390, 1.000000000000000000),
 ( 1.000000000000000000, 0.8958246136694008044, 1.000000000000000000),
 ( 1.000000000000000000, 0.8888068886117856948, 1.000000000000000000),
 ( 1.000000000000000000, 0.8868507700907835023, 1.000000000000000000),
 ( 1.000000000000000000, 0.8868705507870304761, 1.000000000000000000) ) ) 
 REPRESENTATION_ITEM ( '' )  SURFACE ( )  );
#14481=CARTESIAN_POINT ( 'NONE',  ( -25.68053481550299111, 15.00000000000000000, -142.4798935003980773 ) ) ;
#14483=CARTESIAN_POINT ( 'NONE',  ( 4.047901359269184596, 1.717432757859984984E-11, -106.4041221357184668 ) ) ;
#14486=ORIENTED_EDGE ( 'NONE', *, *, #6065, .T. ) ;
#14487=CARTESIAN_POINT ( 'NONE',  ( -5.223664414336186113, 2.500000000000000444, -111.8183263698799266 ) ) ;
#14496=CARTESIAN_POINT ( 'NONE',  ( -67.50271866739358018, 14.99999999999315037, -175.2102855836816673 ) ) ;
#14497=CARTESIAN_POINT ( 'NONE',  ( -47.48189921986828210, 9.999999999999998224, -141.5723758807981483 ) ) ;
#14499=DIRECTION ( 'NONE',  ( 0.000000000000000000, 1.000000000000000000, -0.000000000000000000 ) ) ;
#14513=ORIENTED_EDGE ( 'NONE', *, *, #12686, .T. ) ;
#14514=EDGE_CURVE ( 'NONE', #2651, #12098, #8921, .T. ) ;
#14521=DIRECTION ( 'NONE',  ( 0.000000000000000000, 0.000000000000000000, -1.000000000000000000 ) ) ;
#14529=CARTESIAN_POINT ( 'NONE',  ( -64.78057553730850771, 15.17580650425065514, -207.3219553479909507 ) ) ;
#14536=ORIENTED_EDGE ( 'NONE', *, *, #5630, .F. ) ;
#14539=CARTESIAN_POINT ( 'NONE',  ( -55.26439141815399836, 9.999999999999998224, -150.1289833821797970 ) ) ;
#14543=DIRECTION ( 'NONE',  ( 0.000000000000000000, 0.000000000000000000, -1.000000000000000000 ) ) ;
#14546=EDGE_CURVE ( 'NONE', #3511, #10578, #5346, .T. ) ;
#14547=DIRECTION ( 'NONE',  ( -0.9961255586397049777, -0.000000000000000000, 0.08794243244723005948 ) ) ;
#14551=CARTESIAN_POINT ( 'NONE',  ( 0.05457537653413515460, 2.500000000000001332, 0.6181762992656862910 ) ) ;
#14553=CARTESIAN_POINT ( 'NONE',  ( 1.476973400873566433, 13.35568666265236537, 2.081368828687825800 ) ) ;
#14555=CARTESIAN_POINT ( 'NONE',  ( 7.788671722263528885, 7.321094445766561876, -20.36947622874119546 ) ) ;
#14559=ORIENTED_EDGE ( 'NONE', *, *, #7883, .F. ) ;
#14566=CARTESIAN_POINT ( 'NONE',  ( -3.190623165655964488, 7.379999999999996341, -41.82578512943236149 ) ) ;
#14570=CARTESIAN_POINT ( 'NONE',  ( -64.76906036162762348, 15.00000000000000000, -167.3305518093332296 ) ) ;
#14571=DIRECTION ( 'NONE',  ( 3.540251991789310798E-15, 0.000000000000000000, -1.000000000000000000 ) ) ;
#14573=FACE_OUTER_BOUND ( 'NONE', #1566, .T. ) ;
#14588=DIRECTION ( 'NONE',  ( 0.7575874476598363216, 0.000000000000000000, 0.6527336816407246500 ) ) ;
#14595=DIRECTION ( 'NONE',  ( -0.000000000000000000, -1.000000000000000000, -0.000000000000000000 ) ) ;
#14596=CARTESIAN_POINT ( 'NONE',  ( -3.688685944975817144, 7.379999999999996341, -41.78181391320875093 ) ) ;
#14598=CARTESIAN_POINT ( 'NONE',  ( -26.78870578381917866, 5.000000000000000000, -139.1599602021251769 ) ) ;
#14603=CIRCLE ( 'NONE', #13367, 5.000000000000000000 ) ;
#14604=AXIS2_PLACEMENT_3D ( 'NONE', #3544, #2694, #10727 ) ;
#14609=DIRECTION ( 'NONE',  ( 0.000000000000000000, -1.000000000000000000, 0.000000000000000000 ) ) ;
#14611=CIRCLE ( 'NONE', #9902, 14.80000000000025651 ) ;
#14615=DIRECTION ( 'NONE',  ( 0.000000000000000000, 1.000000000000000000, 0.000000000000000000 ) ) ;
#14618=EDGE_LOOP ( 'NONE', ( #14118, #13661, #7806, #14109 ) ) ;
#14620=CARTESIAN_POINT ( 'NONE',  ( -7.760546158192966892, 0.2897469121590799390, -104.7856241544137958 ) ) ;
#14625=DIRECTION ( 'NONE',  ( 0.000000000000000000, -1.000000000000000000, 0.000000000000000000 ) ) ;
#14630=FACE_OUTER_BOUND ( 'NONE', #5114, .T. ) ;
#14632=CARTESIAN_POINT ( 'NONE',  ( 3.759523211377189700, 14.85715077771003578, -0.7426300787629251943 ) ) ;
#14637=CARTESIAN_POINT ( 'NONE',  ( 7.719042654902918521, 10.85333879869827278, -21.53480312112609596 ) ) ;
#14647=ORIENTED_EDGE ( 'NONE', *, *, #3936, .F. ) ;
#14651=CARTESIAN_POINT ( 'NONE',  ( -67.78894975818599278, 14.99999999999827693, -204.1377247862654372 ) ) ;
#14652=DIRECTION ( 'NONE',  ( 0.000000000000000000, -0.6972771395097939751, 0.7168016397282022112 ) ) ;
#14655=CARTESIAN_POINT ( 'NONE',  ( -6.483256266768061771, 10.00000000000000178, -108.2602118674242888 ) ) ;
#14661=EDGE_CURVE ( 'NONE', #5270, #4145, #2762, .T. ) ;
#14668=ORIENTED_EDGE ( 'NONE', *, *, #10644, .F. ) ;
#14669=( BOUNDED_CURVE ( )  B_SPLINE_CURVE ( 3, ( #14873, #1940, #7658, #7879 ),
 .UNSPECIFIED., .F., .F. ) 
 B_SPLINE_CURVE_WITH_KNOTS ( ( 4, 4 ),
 ( 0.1758562950254942969, 0.7234361084260857444 ),
 .UNSPECIFIED. ) 
 CURVE ( )  GEOMETRIC_REPRESENTATION_ITEM ( )  RATIONAL_B_SPLINE_CURVE ( ( 1.000000000000000000, 0.9751687266833821699, 0.9751687266833821699, 1.000000000000000000 ) ) 
 REPRESENTATION_ITEM ( '' )  );
#14672=CARTESIAN_POINT ( 'NONE',  ( -5.309889193474533364, 14.88217507572605491, -103.7269406991748184 ) ) ;
#14674=CARTESIAN_POINT ( 'NONE',  ( -39.71273995388224165, 15.00000000000000355, -151.9652294113466837 ) ) ;
#14684=AXIS2_PLACEMENT_3D ( 'NONE', #4717, #3553, #12987 ) ;
#14685=AXIS2_PLACEMENT_3D ( 'NONE', #692, #9739, #3864 ) ;
#14687=CARTESIAN_POINT ( 'NONE',  ( 7.301969087183287854, 3.176662348976181605, -22.75718819171553520 ) ) ;
#14688=CARTESIAN_POINT ( 'NONE',  ( 0.4942027541975256288, 3.793956966360130689, 5.597843736040499785 ) ) ;
#14692=CIRCLE ( 'NONE', #9984, 14.80000000000025651 ) ;
#14693=CARTESIAN_POINT ( 'NONE',  ( -8.661991262811106651, 9.999999999999998224, -130.6821289911104316 ) ) ;
#14694=ORIENTED_EDGE ( 'NONE', *, *, #14293, .T. ) ;
#14704=AXIS2_PLACEMENT_3D ( 'NONE', #8577, #10747, #10902 ) ;
#14710=CARTESIAN_POINT ( 'NONE',  ( 3.906635893048721275, 14.90393432339122093, -1.513038254126030990 ) ) ;
#14715=DIRECTION ( 'NONE',  ( 0.000000000000000000, 0.000000000000000000, -1.000000000000000000 ) ) ;
#14717=CARTESIAN_POINT ( 'NONE',  ( -35.54172072645641833, 9.999999999999998224, -156.2450653135776975 ) ) ;
#14736=DIRECTION ( 'NONE',  ( -0.000000000000000000, -1.000000000000000000, -0.000000000000000000 ) ) ;
#14737=CARTESIAN_POINT ( 'NONE',  ( 6.049910241306247549, 9.999999999999998224, -118.3734240199295300 ) ) ;
#14745=VERTEX_POINT ( 'NONE', #12191 ) ;
#14756=VERTEX_POINT ( 'NONE', #5086 ) ;
#14760=ORIENTED_EDGE ( 'NONE', *, *, #11504, .T. ) ;
#14761=CARTESIAN_POINT ( 'NONE',  ( 5.844703153020811115, 5.000000000000000888, -103.2023327213425432 ) ) ;
#14764=CARTESIAN_POINT ( 'NONE',  ( 7.265156645817275383, 3.132533400630292952, -23.06457822180372119 ) ) ;
#14765=CARTESIAN_POINT ( 'NONE',  ( 3.200329101915443175, 3.382469978819814038, 4.943050645478439087 ) ) ;
#14770=ORIENTED_EDGE ( 'NONE', *, *, #5327, .T. ) ;
#14772=DIRECTION ( 'NONE',  ( 0.7575874476598360996, -0.000000000000000000, 0.6527336816407247611 ) ) ;
#14776=FACE_OUTER_BOUND ( 'NONE', #1866, .T. ) ;
#14782=CARTESIAN_POINT ( 'NONE',  ( -3.315923205871639468, 9.650666666666662508, -43.24506100211545601 ) ) ;
#14784=CARTESIAN_POINT ( 'NONE',  ( 3.882360952064769943, 14.89515687073112460, -1.256691955966320329 ) ) ;
#14786=B_SPLINE_CURVE_WITH_KNOTS ( 'NONE', 3,
 ( #13069, #3571, #8198, #7179, #8273, #9288, #3410, #4650, #1326, #13001, #12928, #6029, #1245, #14088, #5951, #9211, #4804, #3491, #9518, #13942 ),
 .UNSPECIFIED., .F., .F.,
 ( 4, 2, 2, 2, 2, 2, 2, 2, 2, 4 ),
 ( -1.586017202738188953E-05, 0.001008001390798507393, 0.002031862953624396628, 0.003055724516450285862, 0.004079586079276174664, 0.005103447642102064766, 0.005615378423515009383, 0.006127309204927953133, 0.007151170767753843235, 0.008175032330579735940 ),
 .UNSPECIFIED. ) ;
#14788=EDGE_CURVE ( 'NONE', #5990, #4897, #4480, .T. ) ;
#14789=CARTESIAN_POINT ( 'NONE',  ( -8.205916711996726676, 7.499999999999991118, -92.94857034792688921 ) ) ;
#14792=CARTESIAN_POINT ( 'NONE',  ( -41.27834176925853882, 14.99999999999932676, -157.9203444101418938 ) ) ;
#14794=ORIENTED_EDGE ( 'NONE', *, *, #11695, .F. ) ;
#14798=CARTESIAN_POINT ( 'NONE',  ( -3.329342754288864281, 9.806926398386266897, -43.39706447520367050 ) ) ;
#14803=DIRECTION ( 'NONE',  ( 0.000000000000000000, -1.000000000000000000, 0.000000000000000000 ) ) ;
#14808=CYLINDRICAL_SURFACE ( 'NONE', #5056, 3.500000000000003109 ) ;
#14810=DIRECTION ( 'NONE',  ( 0.08794243244722413366, 0.000000000000000000, 0.9961255586397056438 ) ) ;
#14811=CARTESIAN_POINT ( 'NONE',  ( -63.21422130130007133, 9.999999999999998224, -203.6040552426024703 ) ) ;
#14818=ORIENTED_EDGE ( 'NONE', *, *, #14043, .T. ) ;
#14821=CARTESIAN_POINT ( 'NONE',  ( -4.090890948359604984, 15.00000000000000000, -103.1929727064838147 ) ) ;
#14826=EDGE_CURVE ( 'NONE', #119, #12332, #5962, .T. ) ;
#14829=ORIENTED_EDGE ( 'NONE', *, *, #13682, .F. ) ;
#14833=ORIENTED_EDGE ( 'NONE', *, *, #12833, .F. ) ;
#14838=CARTESIAN_POINT ( 'NONE',  ( 7.492004171561701398, 3.557029191498670695, -21.78040058436872428 ) ) ;
#14839=CARTESIAN_POINT ( 'NONE',  ( 0.06906476797019409086, 2.515634231730215831, 0.7822979040126908368 ) ) ;
#14845=CIRCLE ( 'NONE', #10608, 5.000000000000000000 ) ;
#14846=ADVANCED_FACE ( 'NONE', ( #14455 ), #8623, .T. ) ;
#14852=CIRCLE ( 'NONE', #8159, 6.999999999999950262 ) ;
#14854=AXIS2_PLACEMENT_3D ( 'NONE', #14481, #8816, #13545 ) ;
#14859=ORIENTED_EDGE ( 'NONE', *, *, #935, .F. ) ;
#14866=EDGE_LOOP ( 'NONE', ( #11928, #3187, #8589, #3206 ) ) ;
#14869=CARTESIAN_POINT ( 'NONE',  ( -40.71937926017810838, 9.999999999999998224, -157.6611590844387365 ) ) ;
#14873=CARTESIAN_POINT ( 'NONE',  ( -18.09353981420494151, 5.000000000000000000, -129.3374956033359240 ) ) ;
#14874=FACE_OUTER_BOUND ( 'NONE', #1904, .T. ) ;
#14879=FACE_OUTER_BOUND ( 'NONE', #8844, .T. ) ;
#14888=ORIENTED_EDGE ( 'NONE', *, *, #11774, .F. ) ;
#14894=EDGE_CURVE ( 'NONE', #6134, #8293, #4315, .T. ) ;
#14895=ORIENTED_EDGE ( 'NONE', *, *, #15218, .T. ) ;
#14899=CARTESIAN_POINT ( 'NONE',  ( -7.072992149635495274, 2.500000000000000888, -107.3904655700100648 ) ) ;
#14905=CIRCLE ( 'NONE', #7966, 2.500000000000000444 ) ;
#14907=ORIENTED_EDGE ( 'NONE', *, *, #9281, .F. ) ;
#14911=EDGE_LOOP ( 'NONE', ( #4159, #14513, #11667, #9494, #516, #1084, #5895, #11705, #14486, #8282 ) ) ;
#14916=AXIS2_PLACEMENT_3D ( 'NONE', #13460, #9888, #3011 ) ;
#14918=CARTESIAN_POINT ( 'NONE',  ( 7.442588453438189866, 4.718804654235878360, -26.16159948206511032 ) ) ;
#14919=CARTESIAN_POINT ( 'NONE',  ( 0.1113112812214025055, 2.624162859069118170, 1.260824940869380573 ) ) ;
#14924=VERTEX_POINT ( 'NONE', #12735 ) ;
#14925=CARTESIAN_POINT ( 'NONE',  ( -17.32624372123753886, 9.999999999999998224, -122.3796757791585321 ) ) ;
#14929=CARTESIAN_POINT ( 'NONE',  ( -10.71664336910952819, 4.336808689942017736E-16, -125.5340273013442527 ) ) ;
#14931=ADVANCED_FACE ( 'NONE', ( #8156 ), #9662, .T. ) ;
#14938=CARTESIAN_POINT ( 'NONE',  ( -33.91109452337774854, 10.00000000000000178, -156.1716796081737471 ) ) ;
#14944=CARTESIAN_POINT ( 'NONE',  ( -32.01906953551642943, 15.00000000000000000, -156.2419951536765836 ) ) ;
#14948=CARTESIAN_POINT ( 'NONE',  ( -14.68073284315481253, 7.499999999999991118, -92.37694453701993780 ) ) ;
#14959=B_SPLINE_CURVE_WITH_KNOTS ( 'NONE', 3,
 ( #4353, #13783, #3181, #12238, #9922, #14655, #1720, #574, #8832, #4202, #7671, #6516, #11231, #9133, #11599, #11679, #4423, #6743, #13860, #1096, #11455, #3336, #10522, #13937, #1021, #10293, #9285, #5648, #12772, #1167 ),
 .UNSPECIFIED., .F., .F.,
 ( 4, 2, 2, 2, 2, 2, 2, 2, 2, 2, 2, 2, 2, 2, 4 ),
 ( 5.419449386414208742E-17, 0.001566971827987180023, 0.003133943655974308004, 0.004700915483961435118, 0.005484401397954979593, 0.006267887311948524935, 0.009401830967922705437, 0.01018531688191624124, 0.01096880279590977531, 0.01253577462389684344, 0.01410274645188391504, 0.01566971827987098317, 0.01880366193584512291, 0.02193760559181925918, 0.02507154924779336769 ),
 .UNSPECIFIED. ) ;
#14960=CYLINDRICAL_SURFACE ( 'NONE', #2641, 14.80000000000025651 ) ;
#14961=CARTESIAN_POINT ( 'NONE',  ( 4.890948729886716251, 14.76960206134759090, 0.2075543622030249502 ) ) ;
#14963=CARTESIAN_POINT ( 'NONE',  ( 6.089666224640342129, 0.000000000000000000, -124.6062682140657216 ) ) ;
#14965=ORIENTED_EDGE ( 'NONE', *, *, #4385, .F. ) ;
#14966=DIRECTION ( 'NONE',  ( 0.9026204165532970558, 0.000000000000000000, 0.4304374328763154733 ) ) ;
#14974=CARTESIAN_POINT ( 'NONE',  ( -32.22662898424438538, 15.00000000000000000, -135.0284069691736306 ) ) ;
#14978=( BOUNDED_SURFACE ( )  B_SPLINE_SURFACE ( 3, 1, ( 
 ( #10651, #66 ),
 ( #4775, #11877 ),
 ( #3688, #9492 ),
 ( #14215, #4851 ) ),
 .UNSPECIFIED., .F., .F., .T. ) 
 B_SPLINE_SURFACE_WITH_KNOTS ( ( 4, 4 ),
 ( 2, 2 ),
 ( 0.000000000000000000, 1.000000000000000000 ),
 ( 0.000000000000000000, 1.000000000000000000 ),
 .UNSPECIFIED. ) 
 GEOMETRIC_REPRESENTATION_ITEM ( )  RATIONAL_B_SPLINE_SURFACE ( (
 ( 1.000000000000000000, 1.000000000000000000),
 ( 0.9983030522886272573, 0.9983030522886272573),
 ( 0.9983030522886272573, 0.9983030522886272573),
 ( 1.000000000000000000, 1.000000000000000000) ) ) 
 REPRESENTATION_ITEM ( '' )  SURFACE ( )  );
#14986=CARTESIAN_POINT ( 'NONE',  ( 7.429600267620980247, 5.211846493442712003, -26.37897252452876984 ) ) ;
#14989=CARTESIAN_POINT ( 'NONE',  ( 3.230086961653170885, 4.671585941591766655, 5.208283729125869677 ) ) ;
#14993=EDGE_CURVE ( 'NONE', #9880, #2807, #12016, .T. ) ;
#15000=CARTESIAN_POINT ( 'NONE',  ( 3.891364641103949307, 14.90536770052033688, -1.768596708628434211 ) ) ;
#15001=ORIENTED_EDGE ( 'NONE', *, *, #14514, .F. ) ;
#15012=ADVANCED_FACE ( 'NONE', ( #7000 ), #9252, .F. ) ;
#15013=CARTESIAN_POINT ( 'NONE',  ( -29.89610458603408105, 15.00000000000000000, -151.5049534636450801 ) ) ;
#15014=ADVANCED_FACE ( 'NONE', ( #13976 ), #12135, .T. ) ;
#15027=CARTESIAN_POINT ( 'NONE',  ( -29.69515346086420138, 9.999999999999998224, -156.7390981038714983 ) ) ;
#15033=CARTESIAN_POINT ( 'NONE',  ( 2.806001675047999022, 0.2533870648575867746, 1.824864976002073202 ) ) ;
#15034=CARTESIAN_POINT ( 'NONE',  ( 8.602821479119551640, 5.000000000000001776, -113.5763767534210587 ) ) ;
#15036=ORIENTED_EDGE ( 'NONE', *, *, #10815, .F. ) ;
#15037=DIRECTION ( 'NONE',  ( -0.000000000000000000, 1.000000000000000000, -0.000000000000000000 ) ) ;
#15045=CARTESIAN_POINT ( 'NONE',  ( -8.735813531966259760, 12.24413591761513054, -104.9486082961802680 ) ) ;
#15051=AXIS2_PLACEMENT_3D ( 'NONE', #5336, #9898, #2942 ) ;
#15054=ORIENTED_EDGE ( 'NONE', *, *, #3564, .F. ) ;
#15065=CARTESIAN_POINT ( 'NONE',  ( -4.843886036682795826, 10.00000000000000178, -144.0640150611854438 ) ) ;
#15066=( BOUNDED_SURFACE ( )  B_SPLINE_SURFACE ( 3, 2, ( 
 ( #14963, #8836, #8988 ),
 ( #13786, #5359, #12697 ),
 ( #11304, #6668, #3042 ),
 ( #6596, #10296, #6520 ),
 ( #2034, #4356, #11459 ),
 ( #5507, #10151, #947 ) ),
 .UNSPECIFIED., .F., .F., .T. ) 
 B_SPLINE_SURFACE_WITH_KNOTS ( ( 4, 2, 4 ),
 ( 3, 3 ),
 ( -2.081668171172168513E-17, 0.008318652500447831777, 0.01663730500089568437 ),
 ( 0.000000000000000000, 1.000000000000000000 ),
 .UNSPECIFIED. ) 
 GEOMETRIC_REPRESENTATION_ITEM ( )  RATIONAL_B_SPLINE_SURFACE ( (
 ( 1.000000000000000000, 0.7071067811865475727, 1.000000000000000000),
 ( 1.000000000000000000, 0.7071067811865475727, 1.000000000000000000),
 ( 1.000000000000000000, 0.7071067811865475727, 1.000000000000000000),
 ( 1.000000000000000000, 0.7071067811865475727, 1.000000000000000000),
 ( 1.000000000000000000, 0.7071067811865475727, 1.000000000000000000),
 ( 1.000000000000000000, 0.7071067811865475727, 1.000000000000000000) ) ) 
 REPRESENTATION_ITEM ( '' )  SURFACE ( )  );
#15078=CARTESIAN_POINT ( 'NONE',  ( -66.14848843925153687, 14.98207687019956680, -197.4208877442913206 ) ) ;
#15081=AXIS2_PLACEMENT_3D ( 'NONE', #1716, #14803, #13555 ) ;
#15082=CARTESIAN_POINT ( 'NONE',  ( -2.739138985622725286, 4.336808689942017736E-16, -111.5297549026598176 ) ) ;
#15083=VECTOR ( 'NONE', #5744, 1000.000000000000000 ) ;
#15089=CARTESIAN_POINT ( 'NONE',  ( -52.20743557211550723, 15.00000000000133049, -168.0633964594969143 ) ) ;
#15091=AXIS2_PLACEMENT_3D ( 'NONE', #8601, #5290, #1426 ) ;
#15094=CARTESIAN_POINT ( 'NONE',  ( -8.431010172942514203, 9.999999999999998224, -122.5582262043254076 ) ) ;
#15095=CARTESIAN_POINT ( 'NONE',  ( -17.48539614069081694, 15.00000000000000178, -148.4416824785454878 ) ) ;
#15103=DIRECTION ( 'NONE',  ( 0.08794243244723007336, 0.000000000000000000, 0.9961255586397049777 ) ) ;
#15104=EDGE_CURVE ( 'NONE', #2695, #6374, #5398, .T. ) ;
#15106=DIRECTION ( 'NONE',  ( 0.08794243244722425856, 0.000000000000000000, 0.9961255586397054218 ) ) ;
#15112=CARTESIAN_POINT ( 'NONE',  ( -8.886921396801799489, 9.999999999999998224, -105.5168766094550250 ) ) ;
#15113=VERTEX_POINT ( 'NONE', #8306 ) ;
#15114=PRODUCT_DEFINITION_SHAPE ( 'NONE', 'NONE',  #8846 ) ;
#15119=CARTESIAN_POINT ( 'NONE',  ( 7.353370788917347411, 14.99999999999197264, -111.8370434415751475 ) ) ;
#15124=CARTESIAN_POINT ( 'NONE',  ( -9.285933603414303406, 9.999999999999996447, -105.1819416496436475 ) ) ;
#15146=CARTESIAN_POINT ( 'NONE',  ( 8.058837131447921465, 10.00000000000000000, -130.1898991670217640 ) ) ;
#15155=( BOUNDED_SURFACE ( )  B_SPLINE_SURFACE ( 3, 2, ( 
 ( #3246, #6729, #864 ),
 ( #3100, #7958, #13844 ),
 ( #6653, #6803, #11519 ),
 ( #5494, #10213, #10352 ),
 ( #15094, #10806, #11737 ),
 ( #13140, #5021, #9502 ),
 ( #7023, #10736, #12910 ),
 ( #14071, #7327, #10579 ),
 ( #9571, #9653, #2324 ),
 ( #150, #2550, #8408 ),
 ( #3474, #12845, #6089 ),
 ( #11809, #14384, #10890 ),
 ( #1225, #8329, #221 ),
 ( #5936, #14299, #10660 ),
 ( #307, #4714, #13221 ),
 ( #75, #8186, #11965 ),
 ( #4860, #4787, #14225 ),
 ( #3784, #8490, #3698 ),
 ( #3626, #1157, #13055 ),
 ( #2624, #2468, #7165 ),
 ( #11886, #12039, #6012 ),
 ( #5860, #7250, #1388 ),
 ( #1460, #4936, #6169 ),
 ( #9426, #14152, #3552 ),
 ( #1309, #8259, #12986 ),
 ( #2391, #7088, #5325 ),
 ( #14468, #10038, #13298 ),
 ( #7715, #8803, #2932 ),
 ( #6332, #1852, #12431 ),
 ( #6557, #9885, #2701 ),
 ( #539, #463, #7635 ),
 ( #11047, #11270, #5174 ) ),
 .UNSPECIFIED., .F., .F., .F. ) 
 B_SPLINE_SURFACE_WITH_KNOTS ( ( 4, 2, 2, 2, 2, 2, 2, 2, 2, 2, 2, 2, 2, 2, 2, 4 ),
 ( 3, 3 ),
 ( -6.938893903907228378E-18, 0.004113674805128861474, 0.008227349610257729887, 0.01234102441538659917, 0.01336944311666881519, 0.01439786181795103294, 0.01645469922051546671, 0.01851153662307990222, 0.02056837402564433426, 0.02262521142820876976, 0.02365363012949098925, 0.02468204883077320527, 0.02879572363590207282, 0.02982414233718429231, 0.03085256103846650833, 0.03290939844103094036 ),
 ( 0.000000000000000000, 1.000000000000000000 ),
 .UNSPECIFIED. ) 
 GEOMETRIC_REPRESENTATION_ITEM ( )  RATIONAL_B_SPLINE_SURFACE ( (
 ( 1.000000000000000000, 0.7071067811865475727, 1.000000000000000000),
 ( 1.000000000000000000, 0.7071067811865475727, 1.000000000000000000),
 ( 1.000000000000000000, 0.7071067811865475727, 1.000000000000000000),
 ( 1.000000000000000000, 0.7071067811865475727, 1.000000000000000000),
 ( 1.000000000000000000, 0.7071067811865475727, 1.000000000000000000),
 ( 1.000000000000000000, 0.7071067811865475727, 1.000000000000000000),
 ( 1.000000000000000000, 0.7071067811865475727, 1.000000000000000000),
 ( 1.000000000000000000, 0.7071067811865475727, 1.000000000000000000),
 ( 1.000000000000000000, 0.7071067811865475727, 1.000000000000000000),
 ( 1.000000000000000000, 0.7071067811865475727, 1.000000000000000000),
 ( 1.000000000000000000, 0.7071067811865475727, 1.000000000000000000),
 ( 1.000000000000000000, 0.7071067811865475727, 1.000000000000000000),
 ( 1.000000000000000000, 0.7071067811865473507, 1.000000000000000000),
 ( 1.000000000000000000, 0.7071067811865473507, 1.000000000000000000),
 ( 1.000000000000000000, 0.7071067811865475727, 1.000000000000000000),
 ( 1.000000000000000000, 0.7071067811865475727, 1.000000000000000000),
 ( 1.000000000000000000, 0.7071067811865474617, 1.000000000000000000),
 ( 1.000000000000000000, 0.7071067811865474617, 1.000000000000000000),
 ( 1.000000000000000000, 0.7071067811865475727, 1.000000000000000000),
 ( 1.000000000000000000, 0.7071067811865475727, 1.000000000000000000),
 ( 1.000000000000000000, 0.7071067811865472397, 1.000000000000000000),
 ( 1.000000000000000000, 0.7071067811865472397, 1.000000000000000000),
 ( 1.000000000000000000, 0.7071067811865475727, 1.000000000000000000),
 ( 1.000000000000000000, 0.7071067811865475727, 1.000000000000000000),
 ( 1.000000000000000000, 0.7071067811865481278, 1.000000000000000000),
 ( 1.000000000000000000, 0.7071067811865481278, 1.000000000000000000),
 ( 1.000000000000000000, 0.7071067811865467956, 1.000000000000000000),
 ( 1.000000000000000000, 0.7071067811865467956, 1.000000000000000000),
 ( 1.000000000000000000, 0.7071067811865467956, 1.000000000000000000),
 ( 1.000000000000000000, 0.7071067811865467956, 1.000000000000000000),
 ( 1.000000000000000000, 0.7071067811865475727, 1.000000000000000000),
 ( 1.000000000000000000, 0.7071067811865475727, 1.000000000000000000) ) ) 
 REPRESENTATION_ITEM ( '' )  SURFACE ( )  );
#15156=CARTESIAN_POINT ( 'NONE',  ( -31.09209721305616370, 5.000000000000000000, -156.3611406121567597 ) ) ;
#15157=CARTESIAN_POINT ( 'NONE',  ( -67.57161933043941815, 13.62327337447829656, -200.3246758838251083 ) ) ;
#15158=CARTESIAN_POINT ( 'NONE',  ( 0.1694250374747845456, 2.802173579811035431, -138.2948546871898259 ) ) ;
#15165=ORIENTED_EDGE ( 'NONE', *, *, #56, .F. ) ;
#15169=CARTESIAN_POINT ( 'NONE',  ( -55.44729830701660944, 15.00000000001072920, -173.4678552871688453 ) ) ;
#15170=EDGE_CURVE ( 'NONE', #14016, #13160, #6216, .T. ) ;
#15174=CARTESIAN_POINT ( 'NONE',  ( -15.11050069331331613, 15.00000000000000000, -146.5097068764998198 ) ) ;
#15176=AXIS2_PLACEMENT_3D ( 'NONE', #14566, #6507, #12458 ) ;
#15185=FACE_OUTER_BOUND ( 'NONE', #10849, .T. ) ;
#15187=CARTESIAN_POINT ( 'NONE',  ( 4.374104445798832508, 15.00089282178849182, -1.804052482945245783 ) ) ;
#15188=CARTESIAN_POINT ( 'NONE',  ( -17.32624372124044854, 0.6199615622964459449, -130.2318118670719116 ) ) ;
#15189=ORIENTED_EDGE ( 'NONE', *, *, #6455, .F. ) ;
#15199=CARTESIAN_POINT ( 'NONE',  ( -51.71514206936258518, 9.999999999999998224, -145.7302012135338884 ) ) ;
#15200=CARTESIAN_POINT ( 'NONE',  ( -9.243017000006215511, 10.73487358288918436, -105.1634759883721273 ) ) ;
#15218=EDGE_CURVE ( 'NONE', #10617, #1079, #10088, .T. ) ;
#15225=DIRECTION ( 'NONE',  ( -0.000000000000000000, 1.000000000000000000, -0.000000000000000000 ) ) ;
#15233=CARTESIAN_POINT ( 'NONE',  ( -64.24125335076371357, 14.99999999999999645, -182.1877858736318103 ) ) ;
#15243=CARTESIAN_POINT ( 'NONE',  ( -68.23215113762095996, 15.00000000000000000, -203.6364912936910798 ) ) ;
#15249=AXIS2_PLACEMENT_3D ( 'NONE', #4577, #3487, #3407 ) ;
#15254=FACE_OUTER_BOUND ( 'NONE', #1583, .T. ) ;
#15255=CARTESIAN_POINT ( 'NONE',  ( -3.782526895735879524, 9.999999999999998224, -42.84475209785865246 ) ) ;
#15262=ORIENTED_EDGE ( 'NONE', *, *, #9125, .T. ) ;
#15266=CARTESIAN_POINT ( 'NONE',  ( -65.53364736412717662, 10.00000000000000000, -205.7441351029432894 ) ) ;
#15272=CARTESIAN_POINT ( 'NONE',  ( 0.000000000000000000, 0.000000000000000000, 0.000000000000000000 ) ) ;
#15277=VERTEX_POINT ( 'NONE', #6612 ) ;
#15291=ADVANCED_FACE ( 'NONE', ( #11170 ), #11319, .T. ) ;
#15292=CIRCLE ( 'NONE', #8608, 3.000000000000010214 ) ;
#15302=CARTESIAN_POINT ( 'NONE',  ( -66.08772900935203154, 15.00301221266680862, -199.0286653353512634 ) ) ;
#15305=CARTESIAN_POINT ( 'NONE',  ( -3.184492023421114926, 4.336808689942017736E-16, -109.5142639673473468 ) ) ;
#15306=EDGE_CURVE ( 'NONE', #1079, #13758, #4978, .T. ) ;
#15309=CIRCLE ( 'NONE', #5665, 2.250000000000005773 ) ;
#15310=CARTESIAN_POINT ( 'NONE',  ( -1.376260179405567108, 15.00000000000000000, -106.6458321843530683 ) ) ;
#15312=VERTEX_POINT ( 'NONE', #7538 ) ;
#15315=CARTESIAN_POINT ( 'NONE',  ( -6.965072737286399196, 4.013953217152291696E-15, -104.2966754940355827 ) ) ;
#15325=COLOUR_RGB('Deep Blue', 0.66274510, 0.83137255, 0.94901961);
#15326=FILL_AREA_STYLE_COLOUR('',#15325);
#15327=FILL_AREA_STYLE('',(#15326));
#15328=SURFACE_STYLE_FILL_AREA(#15327);
#15329=SURFACE_SIDE_STYLE('',(#15328));
#15330=SURFACE_STYLE_USAGE(.BOTH.,#15329);
#15331=PRESENTATION_STYLE_ASSIGNMENT((#15330));
#15379=STYLED_ITEM('',(#15331),#12195);
#15380=MECHANICAL_DESIGN_GEOMETRIC_PRESENTATION_REPRESENTATION('',(#15379),#11867);
ENDSEC;
END-ISO-10303-21;
